ISO-10303-21;
HEADER;
/* Generated by software containing ST-Developer
 * from STEP Tools, Inc. (www.steptools.com) 
 */

FILE_DESCRIPTION(
/* description */ (''),
/* implementation_level */ '2;1');

FILE_NAME(
/* name */ 'Screw.step',
/* time_stamp */ '2026-11-14T03:52:36-08:00',
/* author */ (''),
/* organization */ (''),
/* preprocessor_version */ 'ST-DEVELOPER v20.2',
/* originating_system */ 'Autodesk Translation Framework v15.17.0.0',
/* authorisation */ '');

FILE_SCHEMA (('AUTOMOTIVE_DESIGN { 1 0 10303 214 3 1 1 }'));
ENDSEC;

DATA;
#10=MECHANICAL_DESIGN_GEOMETRIC_PRESENTATION_REPRESENTATION('',(#195),#19443);
#47=B_SPLINE_SURFACE_WITH_KNOTS('',3,3,((#18367,#18368,#18369,#18370,#18371,
#18372,#18373,#18374,#18375,#18376,#18377,#18378,#18379,#18380,#18381,#18382,
#18383,#18384,#18385,#18386,#18387,#18388,#18389,#18390,#18391,#18392,#18393,
#18394,#18395,#18396,#18397,#18398,#18399,#18400,#18401,#18402,#18403,#18404,
#18405,#18406,#18407,#18408,#18409,#18410,#18411,#18412,#18413,#18414,#18415,
#18416,#18417,#18418,#18419,#18420,#18421,#18422,#18423,#18424,#18425,#18426,
#18427,#18428,#18429,#18430,#18431,#18432,#18433,#18434),(#18435,#18436,
#18437,#18438,#18439,#18440,#18441,#18442,#18443,#18444,#18445,#18446,#18447,
#18448,#18449,#18450,#18451,#18452,#18453,#18454,#18455,#18456,#18457,#18458,
#18459,#18460,#18461,#18462,#18463,#18464,#18465,#18466,#18467,#18468,#18469,
#18470,#18471,#18472,#18473,#18474,#18475,#18476,#18477,#18478,#18479,#18480,
#18481,#18482,#18483,#18484,#18485,#18486,#18487,#18488,#18489,#18490,#18491,
#18492,#18493,#18494,#18495,#18496,#18497,#18498,#18499,#18500,#18501,#18502),
(#18503,#18504,#18505,#18506,#18507,#18508,#18509,#18510,#18511,#18512,
#18513,#18514,#18515,#18516,#18517,#18518,#18519,#18520,#18521,#18522,#18523,
#18524,#18525,#18526,#18527,#18528,#18529,#18530,#18531,#18532,#18533,#18534,
#18535,#18536,#18537,#18538,#18539,#18540,#18541,#18542,#18543,#18544,#18545,
#18546,#18547,#18548,#18549,#18550,#18551,#18552,#18553,#18554,#18555,#18556,
#18557,#18558,#18559,#18560,#18561,#18562,#18563,#18564,#18565,#18566,#18567,
#18568,#18569,#18570),(#18571,#18572,#18573,#18574,#18575,#18576,#18577,
#18578,#18579,#18580,#18581,#18582,#18583,#18584,#18585,#18586,#18587,#18588,
#18589,#18590,#18591,#18592,#18593,#18594,#18595,#18596,#18597,#18598,#18599,
#18600,#18601,#18602,#18603,#18604,#18605,#18606,#18607,#18608,#18609,#18610,
#18611,#18612,#18613,#18614,#18615,#18616,#18617,#18618,#18619,#18620,#18621,
#18622,#18623,#18624,#18625,#18626,#18627,#18628,#18629,#18630,#18631,#18632,
#18633,#18634,#18635,#18636,#18637,#18638)),.UNSPECIFIED.,.F.,.F.,.F.,(4,
4),(4,1,1,1,1,1,1,1,1,1,1,1,1,1,1,1,1,1,1,1,1,1,1,1,1,1,1,1,1,1,1,1,1,1,
1,1,1,1,1,1,1,1,1,1,1,1,1,1,1,1,1,1,1,1,1,1,1,1,1,1,1,1,1,1,1,4),(-0.000501830952949241,
0.0663068519672736),(8.30747755240111,9.30594664850426,10.3044157446074,
11.3028848407106,12.3013539368137,13.2998230329169,14.29829212902,15.2967612251232,
16.2952303212263,17.2936994173295,18.2921685134326,19.2906376095358,20.2891067056389,
21.2875758017421,22.2860448978452,23.2845139939484,24.2829830900515,25.2814521861547,
26.2799212822578,27.278390378361,28.2768594744641,29.2753285705673,30.2737976666704,
31.2722667627736,32.2707358588767,33.2692049549799,34.267674051083,35.2661431471862,
36.2646122432893,37.2630813393925,38.2615504354956,39.2600195315988,40.258488627702,
41.2569577238051,42.2554268199083,43.2538959160114,44.2523650121146,45.2508341082177,
46.2493032043209,47.247772300424,48.2462413965272,49.2447104926303,50.2431795887335,
51.2416486848366,52.2401177809398,53.2385868770429,54.2370559731461,55.2355250692492,
56.2339941653524,57.2324632614555,58.2309323575587,59.2294014536618,60.227870549765,
61.2263396458681,62.2248087419713,63.2232778380744,64.2217469341776,65.2202160302807,
66.2186851263839,67.217154222487,68.2156233185902,69.2140924146934,70.2125615107965,
71.2110306068997,72.2094997030028,73.208470630059),.UNSPECIFIED.);
#48=B_SPLINE_SURFACE_WITH_KNOTS('',3,3,((#18916,#18917,#18918,#18919,#18920,
#18921,#18922,#18923,#18924,#18925,#18926,#18927,#18928,#18929,#18930,#18931,
#18932,#18933,#18934,#18935,#18936,#18937,#18938,#18939,#18940,#18941,#18942,
#18943,#18944,#18945,#18946,#18947,#18948,#18949,#18950,#18951,#18952,#18953,
#18954,#18955,#18956,#18957,#18958,#18959,#18960,#18961,#18962,#18963,#18964,
#18965,#18966,#18967,#18968,#18969,#18970,#18971,#18972,#18973,#18974,#18975,
#18976,#18977,#18978,#18979,#18980,#18981,#18982,#18983),(#18984,#18985,
#18986,#18987,#18988,#18989,#18990,#18991,#18992,#18993,#18994,#18995,#18996,
#18997,#18998,#18999,#19000,#19001,#19002,#19003,#19004,#19005,#19006,#19007,
#19008,#19009,#19010,#19011,#19012,#19013,#19014,#19015,#19016,#19017,#19018,
#19019,#19020,#19021,#19022,#19023,#19024,#19025,#19026,#19027,#19028,#19029,
#19030,#19031,#19032,#19033,#19034,#19035,#19036,#19037,#19038,#19039,#19040,
#19041,#19042,#19043,#19044,#19045,#19046,#19047,#19048,#19049,#19050,#19051),
(#19052,#19053,#19054,#19055,#19056,#19057,#19058,#19059,#19060,#19061,
#19062,#19063,#19064,#19065,#19066,#19067,#19068,#19069,#19070,#19071,#19072,
#19073,#19074,#19075,#19076,#19077,#19078,#19079,#19080,#19081,#19082,#19083,
#19084,#19085,#19086,#19087,#19088,#19089,#19090,#19091,#19092,#19093,#19094,
#19095,#19096,#19097,#19098,#19099,#19100,#19101,#19102,#19103,#19104,#19105,
#19106,#19107,#19108,#19109,#19110,#19111,#19112,#19113,#19114,#19115,#19116,
#19117,#19118,#19119),(#19120,#19121,#19122,#19123,#19124,#19125,#19126,
#19127,#19128,#19129,#19130,#19131,#19132,#19133,#19134,#19135,#19136,#19137,
#19138,#19139,#19140,#19141,#19142,#19143,#19144,#19145,#19146,#19147,#19148,
#19149,#19150,#19151,#19152,#19153,#19154,#19155,#19156,#19157,#19158,#19159,
#19160,#19161,#19162,#19163,#19164,#19165,#19166,#19167,#19168,#19169,#19170,
#19171,#19172,#19173,#19174,#19175,#19176,#19177,#19178,#19179,#19180,#19181,
#19182,#19183,#19184,#19185,#19186,#19187)),.UNSPECIFIED.,.F.,.F.,.F.,(4,
4),(4,1,1,1,1,1,1,1,1,1,1,1,1,1,1,1,1,1,1,1,1,1,1,1,1,1,1,1,1,1,1,1,1,1,
1,1,1,1,1,1,1,1,1,1,1,1,1,1,1,1,1,1,1,1,1,1,1,1,1,1,1,1,1,1,1,4),(-0.000439241290791206,
0.0663646041699065),(11.6145150418495,12.6135019439215,13.6119710400246,
14.6104401361278,15.6089092322309,16.6073783283341,17.6058474244372,18.6043165205404,
19.6027856166435,20.6012547127467,21.5997238088498,22.598192904953,23.5966620010561,
24.5951310971593,25.5936001932624,26.5920692893656,27.5905383854687,28.5890074815719,
29.5874765776751,30.5859456737782,31.5844147698814,32.5828838659845,33.5813529620877,
34.5798220581908,35.578291154294,36.5767602503971,37.5752293465003,38.5736984426034,
39.5721675387066,40.5706366348097,41.5691057309129,42.567574827016,43.5660439231192,
44.5645130192223,45.5629821153255,46.5614512114286,47.5599203075318,48.5583894036349,
49.5568584997381,50.5553275958412,51.5537966919444,52.5522657880475,53.5507348841507,
54.5492039802538,55.547673076357,56.5461421724601,57.5446112685633,58.5430803646665,
59.5415494607696,60.5400185568728,61.5384876529759,62.5369567490791,63.5354258451822,
64.5338949412854,65.5323640373885,66.5308331334917,67.5293022295948,68.527771325698,
69.5262404218011,70.5247095179043,71.5231786140074,72.5216477101106,73.5201168062137,
74.5185859023169,75.51705499842,76.5155240945232),.UNSPECIFIED.);
#112=B_SPLINE_CURVE_WITH_KNOTS('',3,(#10944,#10945,#10946,#10947,#10948,
#10949,#10950,#10951,#10952,#10953,#10954,#10955,#10956,#10957,#10958,#10959,
#10960,#10961,#10962,#10963,#10964,#10965,#10966,#10967,#10968,#10969,#10970,
#10971,#10972,#10973,#10974,#10975,#10976,#10977,#10978,#10979,#10980,#10981,
#10982,#10983,#10984,#10985,#10986,#10987,#10988,#10989,#10990,#10991,#10992,
#10993,#10994,#10995,#10996,#10997,#10998,#10999,#11000,#11001,#11002,#11003,
#11004,#11005,#11006,#11007,#11008,#11009,#11010,#11011,#11012,#11013,#11014,
#11015,#11016,#11017,#11018,#11019,#11020,#11021,#11022,#11023,#11024,#11025,
#11026,#11027,#11028,#11029,#11030,#11031,#11032,#11033,#11034,#11035,#11036,
#11037,#11038,#11039,#11040,#11041,#11042,#11043,#11044,#11045,#11046),
 .UNSPECIFIED.,.F.,.F.,(4,3,3,3,3,3,3,3,3,3,3,3,3,3,3,3,3,3,3,3,3,3,3,3,
3,3,3,3,3,3,3,3,3,3,4),(10.3765483376485,10.4759402027806,10.5793082825219,
10.6784508692425,10.7775387594599,10.8766044822859,10.9756805342132,11.0748594189434,
11.1740994295162,11.2734971320225,11.3028848407106,11.4035366366706,11.5040458940526,
11.604441769589,11.7047757700553,11.8050789264824,11.9053822307961,12.0057869498693,
12.1062407367629,12.2068773510693,12.3013539368137,12.401784255105,12.5020682067574,
12.6022340752359,12.7023353147295,12.8024032837535,12.9024692992144,13.0026350854369,
13.102848654931,13.2032457178991,13.2998230329169,13.4003060369769,13.500661779787,
13.6009053515717,13.6618569927778),.UNSPECIFIED.);
#113=B_SPLINE_CURVE_WITH_KNOTS('',3,(#11049,#11050,#11051,#11052,#11053,
#11054,#11055,#11056,#11057,#11058,#11059,#11060,#11061,#11062,#11063,#11064,
#11065,#11066,#11067,#11068,#11069,#11070,#11071,#11072,#11073,#11074,#11075,
#11076,#11077,#11078,#11079,#11080,#11081,#11082,#11083,#11084,#11085,#11086,
#11087,#11088,#11089,#11090,#11091,#11092,#11093,#11094,#11095,#11096,#11097,
#11098,#11099,#11100,#11101,#11102,#11103,#11104,#11105,#11106,#11107,#11108,
#11109,#11110),.UNSPECIFIED.,.F.,.F.,(4,2,2,2,2,2,2,2,2,2,2,2,2,2,2,2,2,
2,2,2,2,2,2,2,2,2,2,2,2,2,4),(-2.46836400305217,-2.46588308991174,-2.46291917044417,
-2.45431065559104,-2.40639634652271,-2.37549128637183,-2.36524340856034,
-2.35781521258133,-2.34987427534677,-2.33687237436732,-2.28350253421887,
-2.25546994759335,-2.23986353138549,-2.23429474379311,-2.23045748204932,
-2.2261999437853,-2.21834822932595,-2.18055988226961,-2.14842269765427,
-2.12834892767817,-2.11983491881741,-2.11336504532106,-2.10622759505867,
-2.09412995748809,-2.03544976313569,-2.0132907412493,-1.99999034003753,
-1.99491712618401,-1.99124091634937,-1.98688475739941,-1.98168879881574),
 .UNSPECIFIED.);
#114=B_SPLINE_CURVE_WITH_KNOTS('',3,(#11116,#11117,#11118,#11119,#11120,
#11121,#11122,#11123,#11124,#11125,#11126,#11127,#11128,#11129,#11130,#11131,
#11132,#11133,#11134,#11135,#11136,#11137,#11138,#11139,#11140,#11141,#11142,
#11143,#11144,#11145,#11146,#11147,#11148,#11149,#11150,#11151,#11152,#11153,
#11154,#11155,#11156,#11157,#11158,#11159,#11160,#11161,#11162,#11163,#11164,
#11165,#11166,#11167,#11168,#11169,#11170,#11171,#11172,#11173,#11174,#11175,
#11176,#11177,#11178,#11179,#11180,#11181,#11182,#11183,#11184,#11185,#11186,
#11187,#11188,#11189,#11190,#11191,#11192,#11193,#11194,#11195,#11196,#11197,
#11198,#11199,#11200,#11201,#11202,#11203,#11204,#11205,#11206,#11207,#11208,
#11209,#11210,#11211,#11212,#11213,#11214,#11215,#11216,#11217,#11218,#11219,
#11220,#11221,#11222,#11223,#11224,#11225,#11226,#11227,#11228,#11229,#11230,
#11231,#11232,#11233,#11234,#11235,#11236,#11237,#11238,#11239,#11240,#11241),
 .UNSPECIFIED.,.F.,.F.,(4,2,2,2,2,2,2,2,2,2,2,2,2,2,2,2,2,2,2,2,2,2,2,2,
2,2,2,2,2,2,2,2,2,2,2,2,2,2,2,2,2,2,2,2,2,2,2,2,2,2,2,2,2,2,2,2,2,2,2,2,
2,2,4),(-1.00835904403323,-0.99080432518265,-0.979541237995393,-0.972419892514247,
-0.965629640897204,-0.956134910559768,-0.929577207527792,-0.87178313919011,
-0.860189047875725,-0.855600929406102,-0.851788747324675,-0.847415298956124,
-0.839155061266686,-0.80725024107116,-0.7536374572217,-0.742212215530873,
-0.73505894663375,-0.72828590554082,-0.718894415834214,-0.693305032052475,
-0.641545231070419,-0.624464424244031,-0.618620970061326,-0.614781665995942,
-0.610591430736765,-0.603228446918461,-0.593773860243074,-0.570735343768825,
-0.51583731359318,-0.504582215938246,-0.497462389170024,-0.490671169066672,
-0.481171007479902,-0.45456102090177,-0.396384905750253,-0.385199575897539,
-0.380625843033889,-0.376816003063609,-0.37243098244482,-0.364116119529149,
-0.352980305291608,-0.321986540625464,-0.280059878532716,-0.267946611621798,
-0.260655272635707,-0.253936992395149,-0.24491300455158,-0.222417392301592,
-0.18370927488101,-0.153741583092926,-0.145772864692122,-0.141411447447901,
-0.137597295400466,-0.132133015536881,-0.11702265733268,-0.0897952434469178,
-0.0736061524808066,-0.0388048341471226,-0.0285900550703762,-0.0223642361463906,
-0.0160654146575395,-0.00877331750423353,-0.000703244481836463),
 .UNSPECIFIED.);
#115=B_SPLINE_CURVE_WITH_KNOTS('',3,(#11242,#11243,#11244,#11245,#11246,
#11247,#11248,#11249,#11250,#11251,#11252,#11253,#11254,#11255,#11256,#11257,
#11258,#11259,#11260,#11261,#11262,#11263,#11264,#11265,#11266,#11267,#11268,
#11269,#11270,#11271,#11272,#11273,#11274,#11275,#11276,#11277,#11278,#11279,
#11280,#11281,#11282,#11283,#11284,#11285,#11286,#11287,#11288,#11289,#11290,
#11291,#11292,#11293,#11294,#11295,#11296,#11297,#11298,#11299,#11300,#11301,
#11302,#11303,#11304,#11305),.UNSPECIFIED.,.F.,.F.,(4,3,3,3,3,3,3,3,3,3,
3,3,3,3,3,3,3,3,3,3,3,4),(13.6618569927778,13.7620143384374,13.8621578175854,
13.9623186264353,14.0625906318973,14.1629275590632,14.2634284535134,14.29829212902,
14.3988099483912,14.4991826767506,14.5994388277011,14.6996312262565,14.7997911050727,
14.8999496560058,15.0002083164209,15.1005150980094,15.2010048401475,15.2967612251232,
15.4075012668598,15.5179191901853,15.6277924052815,15.7079632676322),
 .UNSPECIFIED.);
#116=B_SPLINE_CURVE_WITH_KNOTS('',3,(#11306,#11307,#11308,#11309,#11310,
#11311,#11312,#11313,#11314,#11315,#11316,#11317,#11318,#11319,#11320,#11321,
#11322,#11323,#11324,#11325,#11326,#11327,#11328,#11329,#11330,#11331,#11332,
#11333,#11334,#11335,#11336,#11337,#11338,#11339,#11340,#11341,#11342,#11343,
#11344,#11345,#11346,#11347,#11348,#11349,#11350,#11351,#11352,#11353,#11354,
#11355,#11356,#11357,#11358,#11359,#11360,#11361,#11362,#11363,#11364,#11365,
#11366,#11367,#11368,#11369,#11370,#11371,#11372,#11373,#11374,#11375,#11376,
#11377,#11378,#11379,#11380,#11381,#11382,#11383,#11384,#11385,#11386,#11387,
#11388,#11389,#11390,#11391,#11392,#11393,#11394,#11395,#11396,#11397,#11398,
#11399,#11400,#11401,#11402,#11403,#11404,#11405,#11406,#11407,#11408,#11409,
#11410,#11411,#11412,#11413,#11414,#11415,#11416,#11417,#11418,#11419,#11420,
#11421,#11422,#11423,#11424,#11425,#11426,#11427,#11428,#11429,#11430,#11431,
#11432,#11433,#11434,#11435,#11436,#11437,#11438,#11439,#11440,#11441,#11442,
#11443,#11444,#11445,#11446,#11447,#11448,#11449,#11450,#11451,#11452,#11453,
#11454,#11455,#11456,#11457,#11458,#11459,#11460,#11461,#11462,#11463,#11464,
#11465,#11466,#11467,#11468,#11469,#11470,#11471,#11472,#11473,#11474,#11475,
#11476,#11477),.UNSPECIFIED.,.F.,.F.,(4,2,2,2,2,2,2,2,2,2,2,2,2,2,2,2,2,
2,2,2,2,2,2,2,2,2,2,2,2,2,2,2,2,2,2,2,2,2,2,2,2,2,2,2,2,2,2,2,2,2,2,2,2,
2,2,2,2,2,2,2,2,2,2,2,2,2,2,2,2,2,2,2,2,2,2,2,2,2,2,2,2,2,2,2,2,4),(-1.98168879881574,
-1.97887615210958,-1.94763859892647,-1.91750028502234,-1.88895906587764,
-1.87922652020951,-1.87235989604258,-1.86607996514539,-1.85573719076576,
-1.81805038466509,-1.78930140312251,-1.76614687342023,-1.75988880532066,
-1.75589178010414,-1.7522609105256,-1.74576379723582,-1.71987712175649,
-1.67618535909901,-1.65232774742581,-1.64310538004146,-1.63632804398489,
-1.62905260467462,-1.61715236703276,-1.5584603952577,-1.529325622837,-1.52277530992381,
-1.51874396018361,-1.51473777456654,-1.50821172613658,-1.48084211855695,
-1.43823205474181,-1.41467185768912,-1.40553887080573,-1.39882989395385,
-1.39163476591018,-1.37989475655699,-1.32871001506904,-1.30350811173531,
-1.28907094117812,-1.28370631444398,-1.27991598457261,-1.27552160878638,
-1.2673955578436,-1.23470780118329,-1.18199872995672,-1.17044704656154,
-1.16326329378536,-1.15649326887355,-1.14715711654298,-1.12210693026197,
-1.07305330407891,-1.05330481821552,-1.04720582269474,-1.04366311903891,
-1.03965334388989,-1.03315660382362,-1.00491522444594,-0.944741791267324,
-0.933175037625585,-0.925990866835437,-0.919226630282932,-0.909909304104162,
-0.885015947841081,-0.836829692081973,-0.815988396769207,-0.809799160662296,
-0.806243751883766,-0.802263740017218,-0.79589476177324,-0.77019251672917,
-0.714439218864002,-0.698903405616671,-0.690865009860394,-0.684240285657257,
-0.676338717619893,-0.66103986211829,-0.640358067293166,-0.613034008915922,
-0.582012274920213,-0.574000962598554,-0.569632024595309,-0.565819837988581,
-0.560372936862727,-0.545416229054894,-0.518667185138567,-0.487365959345673),
 .UNSPECIFIED.);
#117=B_SPLINE_CURVE_WITH_KNOTS('',3,(#11482,#11483,#11484,#11485,#11486,
#11487,#11488,#11489,#11490,#11491,#11492,#11493,#11494,#11495,#11496,#11497,
#11498,#11499,#11500,#11501,#11502,#11503,#11504,#11505,#11506,#11507,#11508,
#11509,#11510,#11511,#11512,#11513,#11514,#11515,#11516,#11517,#11518,#11519,
#11520,#11521,#11522,#11523,#11524,#11525,#11526,#11527,#11528,#11529,#11530,
#11531,#11532,#11533,#11534,#11535,#11536,#11537,#11538,#11539,#11540,#11541,
#11542,#11543,#11544,#11545,#11546,#11547,#11548,#11549,#11550,#11551,#11552,
#11553,#11554,#11555,#11556,#11557,#11558,#11559,#11560,#11561,#11562,#11563,
#11564,#11565,#11566,#11567,#11568,#11569,#11570,#11571,#11572,#11573,#11574,
#11575,#11576,#11577,#11578,#11579,#11580,#11581,#11582,#11583,#11584,#11585,
#11586,#11587,#11588,#11589,#11590,#11591,#11592,#11593,#11594,#11595,#11596,
#11597,#11598,#11599,#11600,#11601,#11602,#11603,#11604,#11605,#11606,#11607,
#11608,#11609,#11610,#11611,#11612,#11613,#11614,#11615,#11616,#11617,#11618,
#11619,#11620,#11621,#11622,#11623,#11624,#11625,#11626,#11627,#11628,#11629,
#11630,#11631,#11632,#11633,#11634,#11635,#11636,#11637,#11638,#11639,#11640,
#11641,#11642,#11643,#11644,#11645,#11646,#11647,#11648,#11649,#11650,#11651,
#11652,#11653),.UNSPECIFIED.,.F.,.F.,(4,2,2,2,2,2,2,2,2,2,2,2,2,2,2,2,2,
2,2,2,2,2,2,2,2,2,2,2,2,2,2,2,2,2,2,2,2,2,2,2,2,2,2,2,2,2,2,2,2,2,2,2,2,
2,2,2,2,2,2,2,2,2,2,2,2,2,2,2,2,2,2,2,2,2,2,2,2,2,2,2,2,2,2,2,2,4),(-2.50248360392367,
-2.47407561568409,-2.43362224671165,-2.4106280150226,-2.40154232941611,
-2.39481673446982,-2.38755375233706,-2.37557629553376,-2.3274062717911,
-2.3006792603101,-2.28573081645583,-2.28028540735249,-2.27647339985178,
-2.27210190428346,-2.26408344307706,-2.23289114242665,-2.20312962726049,
-2.18392479930568,-2.16939974687355,-2.16164016004058,-2.15500739766369,
-2.14679799246234,-2.13366875304952,-2.07151403352715,-2.05672046938795,
-2.04652322403861,-2.04178596083641,-2.03802492531491,-2.03320405588648,
-2.02221873139686,-1.96346721147729,-1.93678737955585,-1.92728100569733,
-1.92048916122654,-1.91337198159745,-1.90212849778767,-1.84034195318542,
-1.81294625323171,-1.80649006407928,-1.80249113989479,-1.79845968512279,
-1.79184989845132,-1.76109069764411,-1.72111621940969,-1.69825538472261,
-1.68918569231159,-1.68246165023475,-1.67519069576965,-1.66317669953361,
-1.61558779393993,-1.5884891746718,-1.57341967181971,-1.56795870060941,
-1.56414404436843,-1.5597793596647,-1.55179473981675,-1.52137287980442,
-1.49522843980624,-1.46340422692845,-1.4532421942805,-1.44702344661142,
-1.44019064912493,-1.43044738461142,-1.40129855057202,-1.37210882441159,
-1.34110042213582,-1.33308932327228,-1.32871902116904,-1.32490586816934,
-1.31945606037215,-1.30447545475975,-1.2776517604171,-1.22967939510834,
-1.2176914828043,-1.2104256852885,-1.20369963412152,-1.19461672140066,-1.17165495127793,
-1.1313311826467,-1.10099204653433,-1.09438311962162,-1.09035179644238,
-1.08635237010884,-1.07989470399861,-1.05245728926926,-1.00835904403323),
 .UNSPECIFIED.);
#118=B_SPLINE_CURVE_WITH_KNOTS('',3,(#11655,#11656,#11657,#11658,#11659,
#11660,#11661,#11662,#11663,#11664,#11665,#11666,#11667,#11668,#11669,#11670,
#11671,#11672,#11673,#11674,#11675,#11676,#11677,#11678,#11679,#11680,#11681,
#11682,#11683,#11684,#11685,#11686,#11687,#11688,#11689,#11690,#11691,#11692,
#11693,#11694,#11695,#11696,#11697,#11698,#11699,#11700,#11701,#11702,#11703,
#11704,#11705,#11706,#11707,#11708,#11709,#11710),.UNSPECIFIED.,.F.,.F.,
(4,2,2,2,2,2,2,2,2,2,2,2,2,2,2,2,2,2,2,2,2,2,2,2,2,2,2,4),(-0.487365959345673,
-0.470564312664979,-0.45858267467034,-0.451317489371573,-0.444589955523596,
-0.435501767533371,-0.412503106109016,-0.372045361245167,-0.341899322545666,
-0.335291466812455,-0.33125982565294,-0.327259600048952,-0.320798823614071,
-0.293300890879341,-0.231752022206382,-0.220465684395158,-0.213339615594384,
-0.206551694911002,-0.197071738340952,-0.170658718302693,-0.113888329504335,
-0.101497710838403,-0.0967566905152996,-0.0929500858939294,-0.0886871136675097,
-0.0809723696866922,-0.0359502418557884,-0.000724551695920961),
 .UNSPECIFIED.);
#119=B_SPLINE_CURVE_WITH_KNOTS('',3,(#11711,#11712,#11713,#11714,#11715,
#11716,#11717,#11718,#11719,#11720,#11721,#11722,#11723,#11724,#11725,#11726,
#11727,#11728,#11729,#11730,#11731,#11732,#11733,#11734,#11735,#11736,#11737,
#11738,#11739,#11740,#11741,#11742,#11743,#11744,#11745,#11746,#11747,#11748,
#11749,#11750,#11751,#11752,#11753,#11754,#11755,#11756,#11757,#11758,#11759,
#11760,#11761,#11762,#11763,#11764,#11765,#11766,#11767,#11768,#11769,#11770,
#11771,#11772,#11773,#11774,#11775,#11776,#11777,#11778,#11779,#11780,#11781,
#11782,#11783,#11784,#11785,#11786,#11787,#11788,#11789,#11790,#11791,#11792,
#11793,#11794,#11795,#11796,#11797,#11798,#11799,#11800,#11801,#11802,#11803,
#11804,#11805,#11806,#11807,#11808,#11809,#11810,#11811,#11812,#11813,#11814,
#11815,#11816,#11817,#11818,#11819,#11820,#11821,#11822,#11823,#11824,#11825,
#11826,#11827,#11828,#11829,#11830,#11831,#11832,#11833,#11834,#11835,#11836,
#11837,#11838,#11839,#11840),.UNSPECIFIED.,.F.,.F.,(4,3,3,3,3,3,3,3,3,3,
3,3,3,3,3,3,3,3,3,3,3,3,3,3,3,3,3,3,3,3,3,3,3,3,3,3,3,3,3,3,3,3,3,4),(21.9911485751284,
22.0924387715178,22.193756115275,22.2952120703206,22.3967363325759,22.4984725473193,
22.598192904953,22.6986966926657,22.7990551040477,22.8992965748876,22.9994740790185,
23.099618869796,23.1997621595773,23.3000053923226,23.4002966302333,23.5007708150454,
23.5966620010561,23.6971657361334,23.7975240967797,23.8977655200214,23.9979429784857,
24.0980877255971,24.1982309737833,24.2984741685247,24.3987653703273,24.4992395227271,
24.5951310971593,24.6956346239705,24.7959927721852,24.8962339777079,24.9964112153343,
25.0965557387948,25.1966987608204,25.2969417270206,25.3972326986099,25.4977066206725,
25.5936001932624,25.6940877321455,25.7944386585383,25.8946844403876,25.9948602026975,
26.0949960613067,26.1951428401909,26.2274452731783),.UNSPECIFIED.);
#120=B_SPLINE_CURVE_WITH_KNOTS('',3,(#11846,#11847,#11848,#11849,#11850,
#11851,#11852,#11853,#11854,#11855,#11856,#11857,#11858,#11859,#11860,#11861,
#11862,#11863,#11864,#11865,#11866,#11867,#11868,#11869,#11870,#11871,#11872,
#11873,#11874,#11875,#11876,#11877,#11878,#11879,#11880,#11881,#11882,#11883,
#11884,#11885,#11886,#11887,#11888,#11889,#11890,#11891,#11892,#11893,#11894,
#11895,#11896,#11897,#11898,#11899,#11900,#11901,#11902,#11903,#11904,#11905,
#11906,#11907,#11908,#11909,#11910,#11911,#11912,#11913,#11914,#11915,#11916,
#11917,#11918,#11919,#11920,#11921,#11922,#11923,#11924,#11925,#11926,#11927,
#11928,#11929,#11930,#11931,#11932,#11933,#11934,#11935,#11936,#11937,#11938,
#11939,#11940,#11941,#11942,#11943,#11944,#11945,#11946,#11947,#11948,#11949,
#11950,#11951,#11952,#11953,#11954,#11955,#11956,#11957,#11958,#11959,#11960,
#11961,#11962,#11963,#11964,#11965),.UNSPECIFIED.,.F.,.F.,(4,2,2,2,2,2,
2,2,2,2,2,2,2,2,2,2,2,2,2,2,2,2,2,2,2,2,2,2,2,2,2,2,2,2,2,2,2,2,2,2,2,2,
2,2,2,2,2,2,2,2,2,2,2,2,2,2,2,2,2,4),(-1.00820552373846,-0.994394655396467,
-0.964367093019684,-0.956397307792939,-0.95203611858455,-0.948221008334916,
-0.942754775052995,-0.92763777284904,-0.900387708944509,-0.853103222565575,
-0.841079094213585,-0.83380675407602,-0.827084341129394,-0.818021404607694,
-0.795210534269092,-0.755413229545206,-0.724369871629825,-0.717757876824139,
-0.713726280876762,-0.7097283157445,-0.703275582533351,-0.675927265057406,
-0.614119784339548,-0.602891872297349,-0.595778241935107,-0.588985391579343,
-0.579470252263594,-0.552704008992778,-0.493339080634471,-0.48281535532095,
-0.47802143504235,-0.474261734505149,-0.469419969764229,-0.458614928601644,
-0.442535892350851,-0.413359955945697,-0.37497716390833,-0.364580875422495,
-0.358322661255733,-0.351524983470061,-0.341984473236009,-0.314975535735101,
-0.253664521276312,-0.244603215148044,-0.240073462999185,-0.236294017156018,
-0.23112069660227,-0.218197636048589,-0.197143057470757,-0.140704394456143,
-0.128693347609297,-0.121422883457909,-0.114698405766845,-0.105626784261932,
-0.0827548282764922,-0.0489820852688783,-0.0148892268915053,-0.00679760338978686,
-0.0030868104747884,-0.000701448731005652),.UNSPECIFIED.);
#121=B_SPLINE_CURVE_WITH_KNOTS('',3,(#11966,#11967,#11968,#11969,#11970,
#11971,#11972,#11973,#11974,#11975,#11976,#11977,#11978,#11979,#11980,#11981,
#11982,#11983,#11984,#11985,#11986,#11987,#11988,#11989,#11990,#11991,#11992,
#11993,#11994,#11995,#11996,#11997,#11998,#11999,#12000,#12001,#12002,#12003,
#12004,#12005,#12006,#12007,#12008,#12009,#12010,#12011,#12012,#12013,#12014,
#12015,#12016,#12017,#12018,#12019,#12020,#12021,#12022,#12023,#12024,#12025,
#12026,#12027),.UNSPECIFIED.,.F.,.F.,(4,2,2,2,2,2,2,2,2,2,2,2,2,2,2,2,2,
2,2,2,2,2,2,2,2,2,2,2,2,2,4),(-2.98912631766799,-2.98751883418936,-2.98455840277561,
-2.97785124353937,-2.94286544624325,-2.90819033764507,-2.88541989426223,
-2.87636340785528,-2.86964277554806,-2.86236951039912,-2.85033711273869,
-2.79391604009925,-2.76533872074448,-2.75744477062747,-2.75314566555994,
-2.74931046315851,-2.74460825162245,-2.73259768601139,-2.67547941493075,
-2.64902807190514,-2.63954623204563,-2.63275918542872,-2.62563592466837,
-2.61435833120269,-2.55275128036213,-2.52526815635112,-2.51880862834569,
-2.51480937113557,-2.51077943238742,-2.50417504631604,-2.50248360392367),
 .UNSPECIFIED.);
#122=B_SPLINE_CURVE_WITH_KNOTS('',3,(#12029,#12030,#12031,#12032,#12033,
#12034,#12035,#12036,#12037,#12038,#12039,#12040,#12041,#12042,#12043,#12044,
#12045,#12046,#12047,#12048,#12049,#12050,#12051,#12052,#12053,#12054,#12055,
#12056,#12057,#12058,#12059,#12060,#12061,#12062,#12063,#12064,#12065,#12066,
#12067,#12068,#12069,#12070,#12071,#12072,#12073,#12074,#12075,#12076,#12077,
#12078,#12079,#12080,#12081,#12082,#12083,#12084,#12085,#12086,#12087,#12088,
#12089,#12090,#12091,#12092),.UNSPECIFIED.,.F.,.F.,(4,3,3,3,3,3,3,3,3,3,
3,3,3,3,3,3,3,3,3,3,3,4),(26.2274452731783,26.3277007622098,26.4280132896588,
26.5284985271382,26.5920692893656,26.6925729202986,26.7929311743964,26.8931724879587,
26.993349834888,27.0934944687626,27.1936376021625,27.2938806804709,27.3941717647521,
27.4946457991629,27.5905383854687,27.6906601857262,27.7906431130241,27.8905190749967,
27.9903298046759,28.0900991503633,28.1898994323691,28.2743338823081),
 .UNSPECIFIED.);
#123=B_SPLINE_CURVE_WITH_KNOTS('',3,(#12093,#12094,#12095,#12096,#12097,
#12098,#12099,#12100),.UNSPECIFIED.,.F.,.F.,(4,1,1,1,1,4),(28.2743397907761,
28.5890074815719,29.5874765776751,30.5859456737782,31.5844147698814,32.5105812343903),
 .UNSPECIFIED.);
#124=B_SPLINE_CURVE_WITH_KNOTS('',3,(#12105,#12106,#12107,#12108,#12109,
#12110,#12111,#12112,#12113,#12114,#12115,#12116,#12117,#12118,#12119,#12120,
#12121,#12122,#12123,#12124,#12125,#12126,#12127,#12128,#12129,#12130,#12131,
#12132,#12133,#12134,#12135,#12136,#12137,#12138,#12139,#12140,#12141,#12142,
#12143,#12144,#12145,#12146,#12147,#12148,#12149,#12150,#12151,#12152,#12153,
#12154,#12155,#12156,#12157,#12158,#12159,#12160,#12161,#12162,#12163,#12164,
#12165,#12166,#12167,#12168,#12169,#12170,#12171,#12172,#12173,#12174,#12175,
#12176,#12177,#12178,#12179,#12180,#12181,#12182,#12183,#12184,#12185,#12186,
#12187,#12188,#12189,#12190,#12191,#12192,#12193,#12194,#12195,#12196,#12197,
#12198,#12199,#12200,#12201,#12202,#12203,#12204,#12205,#12206,#12207,#12208,
#12209,#12210,#12211,#12212,#12213,#12214,#12215,#12216,#12217,#12218,#12219,
#12220,#12221,#12222,#12223,#12224,#12225,#12226,#12227,#12228,#12229,#12230,
#12231,#12232,#12233,#12234,#12235,#12236,#12237,#12238,#12239,#12240,#12241,
#12242,#12243,#12244,#12245,#12246,#12247,#12248,#12249,#12250,#12251,#12252,
#12253,#12254,#12255,#12256,#12257,#12258,#12259,#12260,#12261,#12262,#12263,
#12264,#12265,#12266,#12267,#12268,#12269,#12270,#12271,#12272,#12273,#12274,
#12275,#12276,#12277,#12278,#12279,#12280),.UNSPECIFIED.,.F.,.F.,(4,2,2,
2,2,2,2,2,2,2,2,2,2,2,2,2,2,2,2,2,2,2,2,2,2,2,2,2,2,2,2,2,2,2,2,2,2,2,2,
2,2,2,2,2,2,2,2,2,2,2,2,2,2,2,2,2,2,2,2,2,2,2,2,2,2,2,2,2,2,2,2,2,2,2,2,
2,2,2,2,2,2,2,2,2,2,2,2,4),(-2.50227618064395,-2.50221031618583,-2.49511085044294,
-2.48838692323815,-2.47888098188334,-2.45415586689061,-2.45019422125873,
-2.39343165660622,-2.38243550829324,-2.37756186823823,-2.3738018866163,
-2.36903869793777,-2.3586916698933,-2.299140410664,-2.27235801894746,-2.26284180697172,
-2.25604882269738,-2.2489355661288,-2.23770951543795,-2.17585070840769,
-2.1484991948045,-2.14204557028241,-2.13804744023506,-2.13401595230376,
-2.12740478230582,-2.09625875089389,-2.05657381629794,-2.03379677424679,
-2.02473833428267,-2.01801644152752,-2.01074199026837,-1.998708063534,-1.95153972463943,
-1.92417756707742,-1.90902432058123,-1.90355335493176,-1.89973753583041,
-1.89537843826185,-1.88741900518663,-1.85763986376304,-1.81960101048182,
-1.79650307208403,-1.78740416934828,-1.78067648104849,-1.77341842257003,
-1.76146641508434,-1.71291183047518,-1.6864186691951,-1.67154640110459,
-1.66611042521617,-1.6622996595805,-1.65792317141145,-1.64988151233805,
-1.61828237014342,-1.58913375317463,-1.56054141440432,-1.55084962126549,
-1.54402632659974,-1.53779870408895,-1.52758149042831,-1.49464976787876,
-1.46662609649144,-1.43662311742018,-1.43001821341247,-1.4259881298695,
-1.42198877001731,-1.41552935017593,-1.38803673181588,-1.32650028384284,
-1.31521592394445,-1.30809112628313,-1.30130441968337,-1.29182613694663,
-1.26541683649065,-1.20864233642671,-1.19627393349039,-1.19153492520049,
-1.18772915185835,-1.1834658078535,-1.17574790073308,-1.13187886395141,
-1.09065937512701,-1.07854685912919,-1.07125705935137,-1.06454097600566,
-1.05552123687758,-1.03304537697851,-1.00820552373846),.UNSPECIFIED.);
#125=B_SPLINE_CURVE_WITH_KNOTS('',3,(#12282,#12283,#12284,#12285,#12286,
#12287),.UNSPECIFIED.,.F.,.F.,(4,1,1,4),(32.5105812343903,32.5828838659845,
33.5813529620877,34.5575158971517),.UNSPECIFIED.);
#126=B_SPLINE_CURVE_WITH_KNOTS('',3,(#12288,#12289,#12290,#12291,#12292,
#12293,#12294,#12295,#12296,#12297,#12298,#12299,#12300,#12301,#12302,#12303,
#12304,#12305,#12306,#12307,#12308,#12309,#12310,#12311,#12312,#12313,#12314,
#12315,#12316,#12317,#12318,#12319,#12320,#12321,#12322,#12323,#12324,#12325,
#12326,#12327,#12328,#12329,#12330,#12331,#12332,#12333,#12334,#12335,#12336,
#12337,#12338,#12339,#12340,#12341,#12342,#12343,#12344,#12345,#12346,#12347,
#12348,#12349,#12350,#12351,#12352,#12353,#12354,#12355,#12356,#12357,#12358,
#12359,#12360,#12361,#12362,#12363,#12364,#12365,#12366,#12367,#12368,#12369,
#12370,#12371,#12372,#12373,#12374,#12375,#12376,#12377,#12378,#12379,#12380,
#12381,#12382,#12383,#12384,#12385,#12386,#12387,#12388,#12389,#12390,#12391,
#12392,#12393,#12394,#12395,#12396,#12397,#12398,#12399,#12400,#12401,#12402,
#12403,#12404,#12405,#12406,#12407,#12408,#12409,#12410,#12411,#12412,#12413,
#12414,#12415,#12416,#12417,#12418,#12419,#12420,#12421),.UNSPECIFIED.,
 .F.,.F.,(4,2,2,2,2,2,2,2,2,2,2,2,2,2,2,2,2,2,2,2,2,2,2,2,2,2,2,2,2,2,2,
2,2,2,2,2,2,2,2,2,2,2,2,2,2,2,2,2,2,2,2,2,2,2,2,2,2,2,2,2,2,2,2,2,2,2,4),
(-2.98897146095825,-2.98680475232993,-2.98409231131325,-2.98026226214111,
-2.97452190165697,-2.95716116705099,-2.94078050496096,-2.94044016274882,
-2.94005081874297,-2.93960561978467,-2.93909679028486,-2.9157730436606,
-2.88185404587531,-2.87175045709343,-2.86485335052196,-2.85788709311,-2.84741594372294,
-2.80708950807851,-2.77238891293047,-2.75515336956069,-2.74944451178113,
-2.74559095123431,-2.74133712717431,-2.73366532113475,-2.69050030949775,
-2.66036552013097,-2.64683517615848,-2.6355905460972,-2.62847346753744,
-2.62175848489122,-2.61230914645226,-2.58817957147445,-2.58289050051513,
-2.53768979135037,-2.51822047228037,-2.51229363190855,-2.50840099718553,
-2.50422623847947,-2.4969352788314,-2.45006955833457,-2.40925058339837,
-2.39808685366484,-2.39098594421377,-2.3842626232963,-2.37476098691795,
-2.35008752542848,-2.34570132039808,-2.28919656736693,-2.27826620949104,
-2.27340346110922,-2.26964361913121,-2.26487013317789,-2.25446419911136,
-2.19498132596812,-2.16820617382707,-2.15869047903897,-2.1518974826795,
-2.14478390958373,-2.1335567581347,-2.07169372652836,-2.04433861218451,
-2.03788462421192,-2.03388636361375,-2.02985489347567,-2.02324406442263,
-1.99222806350273,-1.98152642259734),.UNSPECIFIED.);
#127=B_SPLINE_CURVE_WITH_KNOTS('',3,(#12427,#12428,#12429,#12430,#12431,
#12432,#12433,#12434,#12435,#12436,#12437,#12438,#12439,#12440,#12441,#12442,
#12443,#12444,#12445,#12446,#12447,#12448,#12449,#12450,#12451,#12452,#12453,
#12454,#12455,#12456,#12457,#12458,#12459,#12460,#12461,#12462,#12463,#12464,
#12465,#12466,#12467,#12468,#12469,#12470,#12471,#12472,#12473,#12474,#12475,
#12476,#12477,#12478,#12479,#12480,#12481,#12482,#12483,#12484,#12485,#12486,
#12487,#12488,#12489,#12490,#12491,#12492,#12493,#12494,#12495,#12496,#12497,
#12498,#12499,#12500,#12501,#12502,#12503,#12504,#12505,#12506,#12507,#12508,
#12509,#12510,#12511,#12512,#12513,#12514,#12515,#12516,#12517,#12518,#12519,
#12520,#12521,#12522,#12523,#12524,#12525,#12526,#12527,#12528,#12529,#12530,
#12531,#12532,#12533,#12534,#12535,#12536,#12537,#12538,#12539,#12540,#12541,
#12542),.UNSPECIFIED.,.F.,.F.,(4,2,2,2,2,2,2,2,2,2,2,2,2,2,2,2,2,2,2,2,
2,2,2,2,2,2,2,2,2,2,2,2,2,2,2,2,2,2,2,2,2,2,2,2,2,2,2,2,2,2,2,2,2,2,2,2,
2,4),(-1.00824895752189,-0.978795587655649,-0.973940169113513,-0.966704674974702,
-0.945174696752521,-0.93700967812232,-0.93025151137541,-0.923204056888826,
-0.91231847285143,-0.867841797615394,-0.824672539001548,-0.816995293844911,
-0.81273966388343,-0.808885312912722,-0.803176532559376,-0.785949046709813,
-0.751281937183289,-0.710926412153754,-0.700464721990181,-0.693498916050672,
-0.686597762763197,-0.676479896001568,-0.642383387295629,-0.598315198314666,
-0.583204394967097,-0.577592764607878,-0.573754519597351,-0.569458441085479,
-0.561584170030399,-0.533188963403702,-0.477360969638919,-0.464899553471184,
-0.457539130815347,-0.450842460305814,-0.441975954589279,-0.420658870141396,
-0.385677852086332,-0.350670892870582,-0.342538469709235,-0.338142265526879,
-0.334335627842033,-0.328934779346477,-0.314344315452468,-0.288702819073133,
-0.23873941513685,-0.226903572456554,-0.219667610225886,-0.212929340436927,
-0.203767220144369,-0.180172333038482,-0.137508455793972,-0.110186082098065,
-0.103649432251847,-0.09963317306983,-0.0956184774177959,-0.0890894222704663,
-0.0599963915802122,-0.000701990655493575),.UNSPECIFIED.);
#128=B_SPLINE_CURVE_WITH_KNOTS('',3,(#12543,#12544,#12545,#12546,#12547,
#12548,#12549,#12550,#12551,#12552,#12553,#12554,#12555,#12556,#12557,#12558,
#12559,#12560,#12561,#12562,#12563,#12564,#12565,#12566,#12567,#12568,#12569,
#12570,#12571,#12572,#12573,#12574,#12575,#12576,#12577,#12578,#12579,#12580,
#12581,#12582,#12583,#12584,#12585,#12586,#12587,#12588,#12589,#12590,#12591,
#12592,#12593,#12594,#12595,#12596,#12597,#12598,#12599,#12600,#12601,#12602,
#12603,#12604),.UNSPECIFIED.,.F.,.F.,(4,2,2,2,2,2,2,2,2,2,2,2,2,2,2,2,2,
2,2,2,2,2,2,2,2,2,2,2,2,2,4),(-2.9889610906993,-2.98169081755074,-2.97482435504751,
-2.96852395308731,-2.96229608080387,-2.95207870536583,-2.91726567422965,
-2.89846756409784,-2.8730710264003,-2.85856467034494,-2.8531752531943,-2.84937088471838,
-2.84497016143403,-2.83681363613837,-2.7743969501821,-2.7472719564497,-2.73772111086022,
-2.73092228619588,-2.72466711190907,-2.71428595266541,-2.67610581457717,
-2.63961713915945,-2.62194583976429,-2.61619183344614,-2.61233062219264,
-2.60809464247292,-2.60050865558634,-2.55632933181388,-2.52675714512438,
-2.51336724670804,-2.50227618064395),.UNSPECIFIED.);
#129=B_SPLINE_CURVE_WITH_KNOTS('',3,(#12605,#12606,#12607,#12608,#12609,
#12610,#12611,#12612,#12613,#12614,#12615,#12616,#12617,#12618,#12619,#12620,
#12621,#12622,#12623,#12624,#12625,#12626,#12627,#12628,#12629,#12630,#12631,
#12632,#12633,#12634,#12635,#12636,#12637,#12638,#12639,#12640,#12641,#12642,
#12643,#12644,#12645,#12646,#12647,#12648,#12649,#12650,#12651,#12652,#12653,
#12654,#12655,#12656,#12657,#12658,#12659,#12660,#12661,#12662,#12663,#12664,
#12665,#12666,#12667,#12668,#12669,#12670,#12671,#12672,#12673,#12674,#12675,
#12676,#12677,#12678,#12679,#12680,#12681,#12682,#12683,#12684,#12685,#12686,
#12687,#12688,#12689,#12690,#12691,#12692,#12693,#12694,#12695,#12696,#12697,
#12698,#12699,#12700,#12701,#12702,#12703,#12704,#12705,#12706,#12707,#12708,
#12709,#12710,#12711,#12712,#12713,#12714,#12715,#12716,#12717,#12718,#12719,
#12720,#12721,#12722,#12723,#12724,#12725,#12726,#12727,#12728,#12729,#12730,
#12731,#12732,#12733,#12734,#12735,#12736,#12737,#12738,#12739,#12740,#12741,
#12742,#12743,#12744,#12745,#12746,#12747,#12748,#12749,#12750,#12751,#12752,
#12753,#12754,#12755,#12756,#12757,#12758,#12759,#12760,#12761,#12762,#12763,
#12764,#12765,#12766,#12767,#12768,#12769,#12770,#12771,#12772,#12773,#12774,
#12775,#12776,#12777,#12778,#12779,#12780),.UNSPECIFIED.,.F.,.F.,(4,2,2,
2,2,2,2,2,2,2,2,2,2,2,2,2,2,2,2,2,2,2,2,2,2,2,2,2,2,2,2,2,2,2,2,2,2,2,2,
2,2,2,2,2,2,2,2,2,2,2,2,2,2,2,2,2,2,2,2,2,2,2,2,2,2,2,2,2,2,2,2,2,2,2,2,
2,2,2,2,2,2,2,2,2,2,2,2,4),(-1.98152642259734,-1.95244157766786,-1.92963461939331,
-1.92057219071929,-1.91384962433673,-1.90657662092182,-1.89455046241958,
-1.84720247251783,-1.81995006589501,-1.8048314609841,-1.79936466760284,
-1.7955493995533,-1.79118817423857,-1.78321899257226,-1.75318846779628,
-1.71457028264026,-1.69210445501782,-1.68308590132271,-1.6763696553837,
-1.66907869055357,-1.65696209223008,-1.61539805487165,-1.58408453932364,
-1.56774865696872,-1.56213809796925,-1.55830079296156,-1.55400606411838,
-1.54613499845678,-1.49509745297723,-1.45776168025704,-1.44741496758706,
-1.44116560817109,-1.43436175724332,-1.42478209254381,-1.39737502024553,
-1.36646285930353,-1.33509422145299,-1.3270655399389,-1.32269188956398,
-1.31888043228983,-1.31343942375725,-1.29852526984928,-1.27190382788032,
-1.22361058163178,-1.21164477923068,-1.20438411122893,-1.19765760916817,
-1.18856601883069,-1.16552854846227,-1.1276949671944,-1.09758961382633,
-1.08961651529104,-1.08525456388988,-1.08143959889417,-1.07597475536949,
-1.0608698118706,-1.03365869651685,-0.9863043273708,-0.974282737987403,
-0.967010801791594,-0.960288080398835,-0.95122370929373,-0.928402989711735,
-0.888574120991167,-0.857565200069573,-0.850953060173582,-0.846921378460218,
-0.842923378362021,-0.836470739668188,-0.809128628613734,-0.747298429882624,
-0.736073282028595,-0.728960099410305,-0.722166809630299,-0.712649634675957,
-0.685865629050649,-0.626374982746974,-0.61594420134626,-0.611166235284037,
-0.607406266658429,-0.602547753497168,-0.591643420466857,-0.535253948984027,
-0.530469855064616,-0.506035216613575,-0.496555676232774,-0.489835515447429,
-0.487400405256145),.UNSPECIFIED.);
#130=B_SPLINE_CURVE_WITH_KNOTS('',3,(#12785,#12786,#12787,#12788,#12789,
#12790,#12791,#12792,#12793,#12794,#12795,#12796,#12797,#12798,#12799,#12800,
#12801,#12802,#12803,#12804,#12805,#12806,#12807,#12808,#12809,#12810,#12811,
#12812,#12813,#12814,#12815,#12816,#12817,#12818,#12819,#12820,#12821,#12822,
#12823,#12824,#12825,#12826,#12827,#12828,#12829,#12830,#12831,#12832,#12833,
#12834,#12835,#12836,#12837,#12838,#12839,#12840,#12841,#12842,#12843,#12844,
#12845,#12846,#12847,#12848,#12849,#12850,#12851,#12852,#12853,#12854,#12855,
#12856,#12857,#12858,#12859,#12860,#12861,#12862,#12863,#12864,#12865,#12866,
#12867,#12868,#12869,#12870,#12871,#12872,#12873,#12874,#12875,#12876,#12877,
#12878,#12879,#12880,#12881,#12882,#12883,#12884,#12885,#12886,#12887,#12888,
#12889,#12890,#12891,#12892,#12893,#12894,#12895,#12896,#12897,#12898,#12899,
#12900,#12901,#12902,#12903,#12904,#12905,#12906,#12907,#12908,#12909,#12910,
#12911,#12912,#12913,#12914,#12915,#12916,#12917,#12918,#12919,#12920,#12921,
#12922,#12923,#12924,#12925,#12926,#12927,#12928,#12929,#12930,#12931,#12932,
#12933,#12934,#12935,#12936,#12937,#12938,#12939,#12940,#12941,#12942,#12943,
#12944,#12945,#12946,#12947,#12948,#12949,#12950,#12951,#12952,#12953,#12954,
#12955,#12956,#12957,#12958,#12959,#12960,#12961,#12962,#12963,#12964),
 .UNSPECIFIED.,.F.,.F.,(4,2,2,2,2,2,2,2,2,2,2,2,2,2,2,2,2,2,2,2,2,2,2,2,
2,2,2,2,2,2,2,2,2,2,2,2,2,2,2,2,2,2,2,2,2,2,2,2,2,2,2,2,2,2,2,2,2,2,2,2,
2,2,2,2,2,2,2,2,2,2,2,2,2,2,2,2,2,2,2,2,2,2,2,2,2,2,2,2,2,4),(-2.50223904448815,
-2.48458676113316,-2.47801768456686,-2.47399579738338,-2.46999039961284,
-2.46349942936955,-2.43714924866715,-2.39376260974356,-2.36999170754781,
-2.36081147857154,-2.35407294199949,-2.34684867933954,-2.3350605115819,
-2.28461561836689,-2.259239287865,-2.24924722624857,-2.2415749184917,-2.23732145384687,
-2.2335126908396,-2.22875832297729,-2.21888199985122,-2.16006375543227,
-2.13337966289093,-2.12387449951752,-2.11708412372897,-2.10996900842573,
-2.09872994063561,-2.03695034833215,-2.00956559254414,-2.00311117545505,
-1.99911326788349,-1.99508276237611,-1.98847440189447,-1.95768804202051,
-1.91774856834776,-1.89490047002733,-1.88583390262889,-1.87911163900697,
-1.87184210332913,-1.85982922941041,-1.80190931288493,-1.77454156250601,
-1.76678990618451,-1.7625197695934,-1.7587168541263,-1.75399040089237,-1.74177516473542,
-1.73034688350027,-1.68279669421211,-1.65805070817618,-1.64875458338047,
-1.6419971632621,-1.63481262276749,-1.62322843877648,-1.56311006788951,
-1.53480764040119,-1.52831133306707,-1.52430415051402,-1.52076970939507,
-1.51469218033872,-1.49505760547634,-1.44746378079865,-1.42145443285424,
-1.41179979094372,-1.40505046973743,-1.39799194662127,-1.38704595408075,
-1.37399162429497,-1.34573750542516,-1.29889194561219,-1.29159304919151,
-1.28741637886326,-1.28352409564388,-1.27760094847803,-1.25817374116419,
-1.2131921836749,-1.20672884800698,-1.18334970985123,-1.17398663189192,
-1.16721788917444,-1.16005469175799,-1.14858096152927,-1.10783532675572,
-1.06158033903093,-1.05421194259443,-1.05002054600416,-1.04613584139557,
-1.04025478538002,-1.02129088525616,-1.00824895752189),.UNSPECIFIED.);
#131=B_SPLINE_CURVE_WITH_KNOTS('',3,(#12966,#12967,#12968,#12969,#12970,
#12971,#12972,#12973,#12974,#12975,#12976,#12977,#12978,#12979,#12980,#12981,
#12982,#12983,#12984,#12985,#12986,#12987,#12988,#12989,#12990,#12991,#12992,
#12993,#12994,#12995,#12996,#12997,#12998,#12999,#13000,#13001,#13002,#13003,
#13004,#13005,#13006,#13007,#13008,#13009,#13010,#13011,#13012,#13013,#13014,
#13015,#13016,#13017,#13018,#13019,#13020,#13021,#13022,#13023,#13024,#13025,
#13026,#13027,#13028,#13029),.UNSPECIFIED.,.F.,.F.,(4,2,2,2,2,2,2,2,2,2,
2,2,2,2,2,2,2,2,2,2,2,2,2,2,2,2,2,2,2,2,2,4),(-0.487400405256145,-0.482727071494558,
-0.471527600046117,-0.458068493533978,-0.42822621030856,-0.384469184654347,
-0.37683819492679,-0.372592581288493,-0.368734932123639,-0.363003859966925,
-0.345557701741069,-0.310003822371837,-0.270911176796646,-0.260405860468918,
-0.253432618394381,-0.246540393641908,-0.236465943941031,-0.20302172959381,
-0.174759519540837,-0.14516598005652,-0.138565888098001,-0.134536618828129,
-0.13053592609133,-0.124071145062031,-0.0964725702842965,-0.0702072811410385,
-0.0488732556113054,-0.0294385074583665,-0.0207592877466262,-0.0142496064044319,
-0.00745404941009283,-0.000701089417020961),.UNSPECIFIED.);
#132=B_SPLINE_CURVE_WITH_KNOTS('',3,(#13030,#13031,#13032,#13033,#13034,
#13035,#13036,#13037,#13038,#13039,#13040,#13041,#13042,#13043,#13044,#13045,
#13046,#13047,#13048,#13049,#13050,#13051,#13052,#13053,#13054,#13055,#13056,
#13057,#13058,#13059,#13060,#13061,#13062,#13063,#13064,#13065,#13066,#13067,
#13068,#13069,#13070,#13071,#13072,#13073,#13074,#13075,#13076,#13077,#13078,
#13079,#13080,#13081,#13082,#13083,#13084,#13085,#13086,#13087,#13088,#13089,
#13090,#13091,#13092,#13093,#13094,#13095,#13096,#13097,#13098,#13099,#13100,
#13101,#13102,#13103,#13104,#13105,#13106,#13107,#13108,#13109,#13110,#13111,
#13112,#13113,#13114,#13115,#13116,#13117,#13118,#13119,#13120,#13121,#13122,
#13123,#13124,#13125,#13126,#13127,#13128,#13129,#13130,#13131,#13132,#13133,
#13134,#13135,#13136,#13137,#13138,#13139,#13140,#13141,#13142,#13143,#13144,
#13145),.UNSPECIFIED.,.F.,.F.,(4,2,2,2,2,2,2,2,2,2,2,2,2,2,2,2,2,2,2,2,
2,2,2,2,2,2,2,2,2,2,2,2,2,2,2,2,2,2,2,2,2,2,2,2,2,2,2,2,2,2,2,2,2,2,2,2,
2,4),(-2.98881319574078,-2.98092667063717,-2.91773801648977,-2.90229028970612,
-2.89178096031394,-2.88698970111545,-2.88360134363954,-2.87896353694705,
-2.86931929279196,-2.80884416450732,-2.78194543849523,-2.77241749892472,
-2.76562269829647,-2.7585132526015,-2.7473057944763,-2.68535417733898,-2.65804884168758,
-2.65159743128282,-2.64759983518693,-2.64356804408673,-2.63695512095839,
-2.60545508992586,-2.5660254796506,-2.54332177012797,-2.53427279780556,
-2.52755241270359,-2.52027442406673,-2.50822212404284,-2.46146920969877,
-2.43383328414512,-2.41859305924976,-2.41311148813477,-2.40929420224561,
-2.40494054174156,-2.39700638804516,-2.36791917182915,-2.32858257642323,
-2.30590602332798,-2.29686062427832,-2.290140835567,-2.28286155347665,-2.27080237774554,
-2.22423418412807,-2.19647729886502,-2.18119903840766,-2.17571287769436,
-2.17189496364491,-2.16754364149193,-2.15962028434921,-2.10943000586541,
-2.07430097796159,-2.06257364126141,-2.05536076730688,-2.04861603678536,
-2.03940062629956,-2.01710211576782,-2.00855411566961,-1.98138385324549),
 .UNSPECIFIED.);
#133=B_SPLINE_CURVE_WITH_KNOTS('',3,(#13151,#13152,#13153,#13154,#13155,
#13156,#13157,#13158),.UNSPECIFIED.,.F.,.F.,(4,1,1,1,1,4),(53.4070818023739,
54.2370559731461,55.2355250692492,56.2339941653524,57.2324632614555,57.6442142744167),
 .UNSPECIFIED.);
#134=B_SPLINE_CURVE_WITH_KNOTS('',3,(#13159,#13160,#13161,#13162,#13163,
#13164,#13165,#13166,#13167,#13168,#13169,#13170,#13171,#13172,#13173,#13174,
#13175,#13176,#13177,#13178,#13179,#13180,#13181,#13182,#13183,#13184,#13185,
#13186,#13187,#13188,#13189,#13190,#13191,#13192,#13193,#13194,#13195,#13196,
#13197,#13198,#13199,#13200,#13201,#13202,#13203,#13204,#13205,#13206,#13207,
#13208,#13209,#13210,#13211,#13212,#13213,#13214,#13215,#13216,#13217,#13218,
#13219,#13220,#13221,#13222),.UNSPECIFIED.,.F.,.F.,(4,2,2,2,2,2,2,2,2,2,
2,2,2,2,2,2,2,2,2,2,2,2,2,2,2,2,2,2,2,2,2,4),(-2.98851908576972,-2.95954428231633,
-2.95455224709358,-2.9508390566069,-2.9474336905644,-2.94296059961915,-2.93418670148345,
-2.89299194574678,-2.86155920997997,-2.86033142855133,-2.856013111439,-2.84636036089806,
-2.8364825166323,-2.82962843921203,-2.82261521908214,-2.81189060279604,
-2.75334077731679,-2.72440308382134,-2.71646874334363,-2.71216202486354,
-2.70833073623885,-2.70364384534931,-2.69173203180844,-2.64938273341975,
-2.62311596385264,-2.60516227090508,-2.59680265662696,-2.59022271380644,
-2.58260156877934,-2.56918037606721,-2.51480708332722,-2.50223904448815),
 .UNSPECIFIED.);
#135=B_SPLINE_CURVE_WITH_KNOTS('',3,(#13223,#13224,#13225,#13226,#13227,
#13228,#13229,#13230,#13231,#13232,#13233,#13234,#13235,#13236,#13237,#13238,
#13239,#13240,#13241,#13242,#13243,#13244,#13245,#13246,#13247,#13248,#13249,
#13250,#13251,#13252,#13253,#13254,#13255,#13256,#13257,#13258,#13259,#13260,
#13261,#13262,#13263,#13264,#13265,#13266,#13267,#13268,#13269,#13270,#13271,
#13272,#13273,#13274,#13275,#13276,#13277,#13278,#13279,#13280,#13281,#13282,
#13283,#13284,#13285,#13286,#13287,#13288,#13289,#13290,#13291,#13292,#13293,
#13294,#13295,#13296,#13297,#13298,#13299,#13300,#13301,#13302,#13303,#13304,
#13305,#13306,#13307,#13308,#13309,#13310,#13311,#13312,#13313,#13314,#13315,
#13316,#13317,#13318,#13319,#13320,#13321,#13322,#13323,#13324,#13325,#13326,
#13327,#13328,#13329,#13330,#13331,#13332,#13333,#13334,#13335,#13336,#13337,
#13338,#13339,#13340,#13341,#13342,#13343,#13344,#13345,#13346,#13347,#13348,
#13349,#13350,#13351,#13352,#13353,#13354,#13355,#13356,#13357,#13358,#13359,
#13360,#13361,#13362,#13363,#13364,#13365,#13366,#13367,#13368,#13369,#13370,
#13371,#13372,#13373,#13374,#13375,#13376,#13377,#13378,#13379,#13380,#13381,
#13382,#13383,#13384,#13385,#13386,#13387,#13388,#13389,#13390,#13391,#13392,
#13393,#13394,#13395,#13396,#13397,#13398,#13399,#13400),.UNSPECIFIED.,
 .F.,.F.,(4,2,2,2,2,2,2,2,2,2,2,2,2,2,2,2,2,2,2,2,2,2,2,2,2,2,2,2,2,2,2,
2,2,2,2,2,2,2,2,2,2,2,2,2,2,2,2,2,2,2,2,2,2,2,2,2,2,2,2,2,2,2,2,2,2,2,2,
2,2,2,2,2,2,2,2,2,2,2,2,2,2,2,2,2,2,2,2,2,4),(-1.98138385324549,-1.97081674774911,
-1.9456115031022,-1.93926934873765,-1.93529468115891,-1.9312378318781,-1.92450583382052,
-1.88725837866581,-1.85204981831191,-1.8306596161908,-1.82178498879674,
-1.81508884593133,-1.80773549980442,-1.79530299307739,-1.73493798628633,
-1.71685285639854,-1.70515227697233,-1.70016441332826,-1.69675925022926,
-1.69227524726658,-1.683450328206,-1.62185210143155,-1.59481934469136,-1.58527781096153,
-1.57848067581286,-1.57222376302594,-1.5618318534935,-1.5234865409652,-1.49454974399244,
-1.47081834938693,-1.46443489806573,-1.46084470323356,-1.45690518228799,
-1.45073603060133,-1.42823500353449,-1.37218900009806,-1.35430544979577,
-1.34595627659711,-1.33931539395311,-1.33166169327375,-1.31769264226281,
-1.28872018315684,-1.23726881319757,-1.22869734229427,-1.22426269971512,
-1.22046667708175,-1.21514026034268,-1.20111135939357,-1.17708927395995,
-1.12415994702007,-1.11265042717573,-1.1054808405156,-1.09871664157442,
-1.08937727067739,-1.06425345470384,-1.01491613517698,-0.995320747319436,
-0.989247653604348,-0.985714142538938,-0.981706116170247,-0.975205382501773,
-0.946776575961122,-0.886936276590112,-0.875304654848065,-0.868110874954834,
-0.861357978243554,-0.852089530397305,-0.827585822571833,-0.781153723671151,
-0.75834823461594,-0.752039233746843,-0.748462864296003,-0.744508571336025,
-0.738266620556866,-0.714699100119087,-0.685436100981927,-0.647033847847996,
-0.636636327204653,-0.630378203478102,-0.623581270756459,-0.614043093542911,
-0.587053645027215,-0.525906231617863,-0.516725698006973,-0.512173570137452,
-0.508397613106541,-0.503258511886453,-0.490568486782124,-0.487221889316969),
 .UNSPECIFIED.);
#136=B_SPLINE_CURVE_WITH_KNOTS('',3,(#13406,#13407,#13408,#13409,#13410,
#13411,#13412,#13413,#13414,#13415,#13416,#13417,#13418,#13419,#13420,#13421,
#13422,#13423,#13424,#13425,#13426,#13427,#13428,#13429,#13430,#13431,#13432,
#13433,#13434,#13435,#13436,#13437,#13438,#13439,#13440,#13441,#13442,#13443,
#13444,#13445,#13446,#13447,#13448,#13449,#13450,#13451,#13452,#13453,#13454,
#13455,#13456,#13457,#13458,#13459,#13460,#13461,#13462,#13463,#13464,#13465,
#13466,#13467,#13468,#13469,#13470,#13471,#13472,#13473,#13474,#13475,#13476,
#13477,#13478,#13479,#13480,#13481,#13482,#13483,#13484,#13485,#13486,#13487,
#13488,#13489,#13490,#13491,#13492,#13493,#13494,#13495,#13496,#13497,#13498,
#13499,#13500,#13501,#13502,#13503,#13504,#13505,#13506,#13507,#13508,#13509,
#13510,#13511,#13512,#13513,#13514,#13515,#13516,#13517,#13518,#13519,#13520,
#13521,#13522,#13523,#13524,#13525,#13526,#13527,#13528,#13529,#13530,#13531,
#13532,#13533,#13534,#13535),.UNSPECIFIED.,.F.,.F.,(4,3,3,3,3,3,3,3,3,3,
3,3,3,3,3,3,3,3,3,3,3,3,3,3,3,3,3,3,3,3,3,3,3,3,3,3,3,3,3,3,3,3,3,4),(59.690260418206,
59.7936358758742,59.9021945443469,60.0058912267106,60.1097115732471,60.2137481729558,
60.227870549765,60.3283743001658,60.4287326727968,60.5289741029433,60.6291515652241,
60.7292963130688,60.8294395589074,60.9296827464682,61.0299739384437,61.1304480766276,
61.2263396458681,61.3268434273722,61.427201833822,61.5274433016728,61.6276208039963,
61.7277655941466,61.8279088844805,61.9281521196312,62.0284433609616,62.1289175508793,
62.2248087419713,62.3253114183611,62.4256687161363,62.5259090751807,62.626085469101,
62.7262291527654,62.8263713400464,62.9266134853021,63.0269036421253,63.1273767696289,
63.2232778380744,63.3237600264403,63.4241074764649,63.5243516448779,63.6248681856545,
63.7250146750007,63.8257162414925,63.9264178079843),.UNSPECIFIED.);
#137=B_SPLINE_CURVE_WITH_KNOTS('',3,(#13536,#13537,#13538,#13539,#13540,
#13541),.UNSPECIFIED.,.F.,.F.,(4,1,1,4),(57.6442142744167,58.2309323575587,
59.2294014536618,59.6902576284875),.UNSPECIFIED.);
#138=B_SPLINE_CURVE_WITH_KNOTS('',3,(#13543,#13544,#13545,#13546,#13547,
#13548,#13549,#13550,#13551,#13552,#13553,#13554,#13555,#13556,#13557,#13558,
#13559,#13560,#13561,#13562,#13563,#13564,#13565,#13566,#13567,#13568,#13569,
#13570,#13571,#13572,#13573,#13574,#13575,#13576,#13577,#13578,#13579,#13580,
#13581,#13582,#13583,#13584,#13585,#13586,#13587,#13588,#13589,#13590,#13591,
#13592,#13593,#13594,#13595,#13596,#13597,#13598,#13599,#13600,#13601,#13602),
 .UNSPECIFIED.,.F.,.F.,(4,2,2,2,2,2,2,2,2,2,2,2,2,2,2,2,2,2,2,2,2,2,2,2,
2,2,2,2,2,4),(-0.487221889316969,-0.470103144983147,-0.416125571285123,
-0.402394763976587,-0.394708899705259,-0.38806972450983,-0.379761768066223,
-0.362136994090603,-0.336616220094698,-0.296396875014931,-0.281822048335411,
-0.276281493998449,-0.27245506965538,-0.268128720078924,-0.260102691018754,
-0.230367336116737,-0.173201352701178,-0.162268799704257,-0.155213065009728,
-0.148384337630516,-0.138661220765493,-0.10973105246942,-0.0542361797896722,
-0.0428673458297301,-0.0379842979785921,-0.0342207570513087,-0.0306022644981407,
-0.0259058737628287,-0.0168229950680565,-0.000700837973673536),
 .UNSPECIFIED.);
#139=B_SPLINE_CURVE_WITH_KNOTS('',3,(#13603,#13604,#13605,#13606,#13607,
#13608,#13609,#13610,#13611,#13612,#13613,#13614,#13615,#13616,#13617,#13618,
#13619,#13620,#13621,#13622,#13623,#13624,#13625,#13626,#13627,#13628,#13629,
#13630,#13631,#13632,#13633,#13634,#13635,#13636,#13637,#13638,#13639,#13640,
#13641,#13642,#13643,#13644,#13645,#13646,#13647,#13648,#13649,#13650,#13651,
#13652,#13653,#13654,#13655,#13656,#13657,#13658,#13659,#13660,#13661,#13662,
#13663,#13664,#13665,#13666,#13667,#13668,#13669,#13670,#13671,#13672,#13673,
#13674,#13675,#13676,#13677,#13678,#13679,#13680,#13681,#13682,#13683,#13684,
#13685,#13686,#13687,#13688,#13689,#13690,#13691,#13692,#13693,#13694,#13695,
#13696,#13697,#13698,#13699,#13700,#13701,#13702,#13703,#13704,#13705,#13706,
#13707,#13708,#13709,#13710,#13711,#13712,#13713,#13714,#13715,#13716,#13717,
#13718,#13719,#13720,#13721,#13722,#13723,#13724,#13725,#13726,#13727,#13728,
#13729,#13730,#13731,#13732),.UNSPECIFIED.,.F.,.F.,(4,3,3,3,3,3,3,3,3,3,
3,3,3,3,3,3,3,3,3,3,3,3,3,3,3,3,3,3,3,3,3,3,3,3,3,3,3,3,3,3,3,3,3,4),(59.6902604184509,
59.7891705930349,59.8879576408718,59.9866781469733,60.0853650263375,60.1840511466361,
60.2828331759564,60.3816669914442,60.4806673091668,60.5400185568728,60.6405221893055,
60.7408804445777,60.8411217588202,60.941299106129,61.0414437400829,61.1415868732625,
61.2418299508799,61.3421210342123,61.442595067247,61.5384876529759,61.6389912978506,
61.739349565851,61.8395908931883,61.9397682538086,62.0399129012705,62.1400560481343,
62.2402991396139,62.3405902369283,62.4410642839787,62.5369567490791,62.637460269328,
62.7378184124023,62.8380596149486,62.938236850914,63.0383813740269,63.1385243970175,
63.2387673662416,63.3390583419822,63.4395322700663,63.5354258451822,63.6359001279754,
63.7362475749873,63.8364882533271,63.9272632692833),.UNSPECIFIED.);
#140=B_SPLINE_CURVE_WITH_KNOTS('',3,(#13738,#13739,#13740,#13741,#13742,
#13743,#13744,#13745,#13746,#13747,#13748,#13749,#13750,#13751,#13752,#13753,
#13754,#13755,#13756,#13757,#13758,#13759,#13760,#13761,#13762,#13763,#13764,
#13765,#13766,#13767,#13768,#13769,#13770,#13771,#13772,#13773,#13774,#13775,
#13776,#13777,#13778,#13779,#13780,#13781,#13782,#13783,#13784,#13785,#13786,
#13787,#13788,#13789,#13790,#13791,#13792,#13793,#13794,#13795,#13796,#13797,
#13798,#13799,#13800,#13801,#13802,#13803,#13804,#13805,#13806,#13807,#13808,
#13809,#13810,#13811,#13812,#13813,#13814,#13815,#13816,#13817,#13818,#13819,
#13820,#13821,#13822,#13823,#13824,#13825,#13826,#13827,#13828,#13829,#13830,
#13831,#13832,#13833,#13834,#13835,#13836,#13837,#13838,#13839,#13840,#13841,
#13842,#13843,#13844,#13845,#13846,#13847,#13848,#13849,#13850,#13851,#13852,
#13853,#13854,#13855,#13856,#13857,#13858,#13859,#13860,#13861,#13862,#13863,
#13864),.UNSPECIFIED.,.F.,.F.,(4,3,3,3,3,3,3,3,3,3,3,3,3,3,3,3,3,3,3,3,
3,3,3,3,3,3,3,3,3,3,3,3,3,3,3,3,3,3,3,3,3,3,4),(65.9734457256259,66.1045621138705,
66.2186851263839,66.319204460379,66.4195783751114,66.5198352129705,66.6200279947471,
66.7201879536106,66.8203462816385,66.9206042438911,67.020910067048,67.1213984191851,
67.217154222487,67.3176605765936,67.4180217399506,67.5182662262134,67.6184469040974,
67.7185950211813,67.8187417841957,67.9189886942884,68.0192837268467,68.1197618581208,
68.2156233185902,68.3160501801306,68.4163314235567,68.5164957231465,68.6165960861905,
68.7166638700256,68.8167303910506,68.9168977673635,69.0171135203952,69.1175137527569,
69.2140924146934,69.3147586491318,69.4152792017634,69.5156814856034,69.6160189639454,
69.7163226726744,69.8166236057553,69.917020695783,70.0174643709433,70.1180849250332,
70.2101735890481),.UNSPECIFIED.);
#141=B_SPLINE_CURVE_WITH_KNOTS('',3,(#13865,#13866,#13867,#13868,#13869,
#13870,#13871,#13872,#13873,#13874,#13875,#13876,#13877,#13878,#13879,#13880,
#13881,#13882,#13883,#13884,#13885,#13886,#13887,#13888,#13889,#13890,#13891,
#13892,#13893,#13894,#13895,#13896,#13897,#13898,#13899,#13900,#13901,#13902,
#13903,#13904,#13905,#13906,#13907,#13908,#13909,#13910,#13911,#13912,#13913,
#13914,#13915,#13916,#13917,#13918,#13919,#13920,#13921,#13922,#13923,#13924,
#13925,#13926,#13927,#13928),.UNSPECIFIED.,.F.,.F.,(4,3,3,3,3,3,3,3,3,3,
3,3,3,3,3,3,3,3,3,3,3,4),(63.9264178079843,64.0267110513925,64.1271867727341,
64.2217469341776,64.3222514687351,64.4226106459022,64.5228529071813,64.6230312163507,
64.7231768255406,64.8233209458962,64.9235650222929,65.0238571123659,65.1243321534556,
65.2202160302807,65.3194873449581,65.4186277683698,65.5176701627707,65.6166472647161,
65.7156217782399,65.8145923419986,65.9136431342839,65.9734457253857),
 .UNSPECIFIED.);
#142=B_SPLINE_CURVE_WITH_KNOTS('',3,(#13930,#13931,#13932,#13933,#13934,
#13935,#13936,#13937,#13938,#13939,#13940,#13941,#13942,#13943,#13944,#13945,
#13946,#13947,#13948,#13949,#13950,#13951,#13952,#13953,#13954,#13955,#13956,
#13957,#13958,#13959,#13960,#13961,#13962,#13963,#13964,#13965,#13966,#13967,
#13968,#13969,#13970,#13971,#13972,#13973,#13974,#13975,#13976,#13977,#13978,
#13979,#13980,#13981,#13982,#13983,#13984,#13985,#13986,#13987,#13988,#13989,
#13990),.UNSPECIFIED.,.F.,.F.,(4,3,3,3,3,3,3,3,3,3,3,3,3,3,3,3,3,3,3,3,
4),(63.9272632692833,64.027409768621,64.1275518239694,64.2291376032984,
64.3294238753586,64.431659408322,64.5338949412854,64.6343987230996,64.7347571298614,
64.8349985980259,64.9351761006638,65.0353208911287,65.1354641817773,65.2357074172405,
65.3359986588827,65.4364728491071,65.5323640373885,65.6426344593317,65.7510908781998,
65.8622683016806,65.9734457251614),.UNSPECIFIED.);
#143=B_SPLINE_CURVE_WITH_KNOTS('',3,(#13991,#13992,#13993,#13994,#13995,
#13996,#13997,#13998,#13999,#14000,#14001,#14002,#14003,#14004,#14005,#14006,
#14007,#14008,#14009,#14010,#14011,#14012,#14013,#14014,#14015,#14016,#14017,
#14018,#14019,#14020,#14021,#14022,#14023,#14024,#14025,#14026,#14027,#14028,
#14029,#14030,#14031,#14032,#14033,#14034,#14035,#14036,#14037,#14038,#14039,
#14040,#14041,#14042,#14043,#14044,#14045,#14046,#14047,#14048,#14049,#14050,
#14051,#14052,#14053,#14054,#14055,#14056,#14057,#14058,#14059,#14060,#14061,
#14062,#14063,#14064,#14065,#14066,#14067,#14068,#14069,#14070,#14071,#14072,
#14073,#14074,#14075,#14076,#14077,#14078,#14079,#14080,#14081,#14082,#14083,
#14084,#14085,#14086,#14087,#14088,#14089,#14090,#14091,#14092,#14093,#14094,
#14095,#14096,#14097,#14098,#14099,#14100,#14101,#14102,#14103,#14104,#14105,
#14106,#14107,#14108,#14109,#14110,#14111,#14112,#14113,#14114),
 .UNSPECIFIED.,.F.,.F.,(4,2,2,2,2,2,2,2,2,2,2,2,2,2,2,2,2,2,2,2,2,2,2,2,
2,2,2,2,2,2,2,2,2,2,2,2,2,2,2,2,2,2,2,2,2,2,2,2,2,2,2,2,2,2,2,2,2,2,2,2,
2,4),(1.00824602608924,1.01205513967596,1.03667147698884,1.04617077086747,
1.05289638644987,1.0600033393827,1.07118494539582,1.08461203483999,1.11432236538005,
1.1582731364538,1.16588397620221,1.17012602038236,1.17398428622679,1.17972406798352,
1.19726737246127,1.23322199901602,1.27199065073597,1.28242399916394,1.28938061641006,
1.29627970850104,1.30640730244607,1.34074553538651,1.38569495102374,1.3998852090954,
1.40537117310134,1.40918795999741,1.41353750104416,1.42167990919704,1.45247726894626,
1.50791683688854,1.51910257343983,1.52620832597893,1.53300661870801,1.54255149865627,
1.56961368256385,1.63149630630471,1.64010845803438,1.64455166958707,1.64834654686455,
1.65366057885852,1.66759412848501,1.69134875213895,1.74485775571996,1.75630106280688,
1.76345772337208,1.77022861621261,1.77960834947042,1.80509733750006,1.85634316578921,
1.87390085041281,1.87979203383812,1.88363963617856,1.88781230588131,1.89509401479404,
1.93179614934836,1.94577129543914,1.96746683854864,1.9878688856724,1.99668867561983,
2.00326526097165,2.00959291509812,2.01574395093934),.UNSPECIFIED.);
#144=B_SPLINE_CURVE_WITH_KNOTS('',3,(#14122,#14123,#14124,#14125,#14126),
 .UNSPECIFIED.,.F.,.F.,(4,1,4),(0.,0.99846909610315,1.11730040836818),
 .UNSPECIFIED.);
#145=B_SPLINE_CURVE_WITH_KNOTS('',3,(#14128,#14129,#14130,#14131,#14132,
#14133,#14134,#14135,#14136,#14137,#14138,#14139,#14140,#14141,#14142,#14143,
#14144,#14145,#14146,#14147,#14148,#14149,#14150,#14151,#14152,#14153,#14154,
#14155,#14156,#14157,#14158,#14159,#14160,#14161,#14162,#14163,#14164,#14165,
#14166,#14167,#14168,#14169,#14170,#14171,#14172,#14173,#14174,#14175,#14176,
#14177,#14178,#14179,#14180,#14181,#14182,#14183,#14184,#14185,#14186,#14187,
#14188,#14189,#14190,#14191,#14192,#14193,#14194,#14195,#14196,#14197,#14198,
#14199,#14200,#14201,#14202,#14203,#14204,#14205,#14206,#14207,#14208,#14209,
#14210,#14211,#14212,#14213,#14214,#14215,#14216,#14217,#14218,#14219,#14220,
#14221,#14222,#14223,#14224,#14225,#14226,#14227,#14228,#14229,#14230,#14231,
#14232,#14233,#14234,#14235,#14236,#14237,#14238,#14239,#14240,#14241,#14242,
#14243,#14244,#14245,#14246,#14247,#14248,#14249,#14250,#14251,#14252,#14253,
#14254,#14255,#14256,#14257,#14258,#14259,#14260,#14261,#14262,#14263,#14264,
#14265,#14266,#14267,#14268,#14269,#14270,#14271,#14272,#14273,#14274,#14275,
#14276,#14277,#14278,#14279,#14280,#14281,#14282,#14283,#14284,#14285,#14286,
#14287,#14288,#14289,#14290,#14291,#14292,#14293,#14294,#14295,#14296,#14297,
#14298,#14299,#14300,#14301,#14302,#14303,#14304,#14305,#14306,#14307,#14308,
#14309,#14310,#14311,#14312,#14313,#14314,#14315,#14316,#14317,#14318,#14319,
#14320,#14321,#14322,#14323,#14324,#14325,#14326,#14327,#14328,#14329,#14330,
#14331,#14332,#14333,#14334,#14335),.UNSPECIFIED.,.F.,.F.,(4,3,3,3,3,3,
3,3,3,3,3,3,3,3,3,3,3,3,3,3,3,3,3,3,3,3,3,3,3,3,3,3,3,3,3,3,3,3,3,3,3,3,
3,3,3,3,3,3,3,3,3,3,3,3,3,3,3,3,3,3,3,3,3,3,3,3,3,3,3,4),(1.11730040836818,
1.21065985735401,1.30390194475301,1.39705744064107,1.4901678784628,1.58326153126441,
1.67636664830859,1.76956843076783,1.86282531823738,1.95623097050921,1.9969381922063,
2.09215365785623,2.18723546969277,2.28221324248444,2.37711927198641,2.47198876703138,
2.56684832311444,2.66172451959558,2.75670224342694,2.85173672319016,2.94692297821923,
2.99540728830945,3.09078086916065,3.18602566035351,3.28117100808536,3.37625073396202,
3.47129765490557,3.56633814252046,3.66139855523426,3.75656435213686,3.85178937367802,
3.94716814873181,3.9938763844126,4.08904010196092,4.18407158401662,4.27900049979211,
4.37386006033638,4.4686845838142,4.56350071865504,4.65833509850859,4.75327369195789,
4.84827050870551,4.94342174995638,4.99234548051575,5.08758258885795,5.18268824482578,
5.27769200953076,5.37262710940974,5.46752757297348,5.56241995503605,5.6573307958684,
5.75234570846594,5.8474188782428,5.94264577720095,5.99081457661891,6.08606120666011,
6.18117674991679,6.27619075171994,6.37113656826171,6.46604804239538,6.56095171605648,
6.65587411687473,6.75090092855928,6.8459862080092,6.94122542766207,6.98928367272206,
7.09421646824028,7.19886064554355,7.30299800135061,7.4004857153595),
 .UNSPECIFIED.);
#146=B_SPLINE_CURVE_WITH_KNOTS('',3,(#14337,#14338,#14339,#14340,#14341,
#14342,#14343,#14344,#14345,#14346,#14347,#14348,#14349,#14350,#14351,#14352,
#14353,#14354,#14355,#14356,#14357,#14358,#14359,#14360,#14361,#14362,#14363,
#14364,#14365,#14366,#14367,#14368,#14369,#14370,#14371,#14372,#14373,#14374,
#14375,#14376,#14377,#14378,#14379,#14380,#14381,#14382,#14383,#14384,#14385,
#14386,#14387,#14388,#14389,#14390,#14391,#14392,#14393,#14394,#14395,#14396,
#14397,#14398,#14399,#14400,#14401,#14402,#14403,#14404,#14405,#14406,#14407,
#14408,#14409,#14410,#14411,#14412,#14413,#14414,#14415,#14416,#14417,#14418,
#14419,#14420,#14421,#14422,#14423,#14424,#14425,#14426,#14427,#14428,#14429,
#14430,#14431,#14432,#14433,#14434,#14435,#14436,#14437,#14438,#14439,#14440,
#14441,#14442,#14443,#14444,#14445,#14446,#14447,#14448,#14449,#14450,#14451,
#14452,#14453,#14454,#14455,#14456,#14457,#14458,#14459,#14460,#14461,#14462,
#14463,#14464,#14465,#14466,#14467,#14468,#14469,#14470,#14471,#14472,#14473,
#14474,#14475,#14476,#14477,#14478,#14479,#14480,#14481,#14482,#14483,#14484,
#14485,#14486,#14487,#14488,#14489,#14490,#14491,#14492,#14493,#14494,#14495,
#14496,#14497,#14498,#14499,#14500,#14501,#14502,#14503,#14504,#14505,#14506,
#14507,#14508,#14509,#14510,#14511,#14512,#14513,#14514,#14515,#14516,#14517,
#14518,#14519,#14520,#14521,#14522,#14523,#14524,#14525,#14526,#14527,#14528,
#14529,#14530,#14531,#14532,#14533,#14534,#14535,#14536,#14537,#14538,#14539,
#14540,#14541,#14542,#14543,#14544),.UNSPECIFIED.,.F.,.F.,(4,3,3,3,3,3,
3,3,3,3,3,3,3,3,3,3,3,3,3,3,3,3,3,3,3,3,3,3,3,3,3,3,3,3,3,3,3,3,3,3,3,3,
3,3,3,3,3,3,3,3,3,3,3,3,3,3,3,3,3,3,3,3,3,3,3,3,3,3,3,4),(7.40048571554785,
7.49694862342332,7.59345175867044,7.69202701120913,7.78874679069572,7.88824977976047,
7.98775276882521,8.08298690953471,8.17808970347387,8.27309071538798,8.36802323803583,
8.46292123452626,8.55781126324666,8.65271986814037,8.74773273812048,8.84280397222948,
8.93802912200363,8.98622186492836,9.08145627199536,9.17655935994665,9.27156069298133,
9.36649357595562,9.46139195700295,9.55628239411369,9.6511914308544,9.74620476588071,
9.84127648461411,9.936502144916,9.98469096103151,10.0799232949096,10.1750242723557,
10.2700234607491,10.3649541572306,10.4598503266232,10.5547385296284,10.6496453125056,
10.7446563773396,10.8397258132155,10.934949193209,10.9831600571347,11.0783933910534,
11.1734953814528,11.2684955942089,11.3634273277133,11.4583245415938,11.5532137952553,
11.6481216336654,11.7431337549892,11.8382042494707,11.9334286810046,11.9816291532378,
12.0768624375003,12.1719643799482,12.2669645465182,12.3618962366793,12.4567934090009,
12.5516826229467,12.6465904235459,12.7416025102032,12.8366729717551,12.9318973734026,
12.980098249341,13.0746871478763,13.1691531641134,13.2635237606834,13.3578263005673,
13.4521042028511,13.54636740019,13.6406740486691,13.6836710227273),
 .UNSPECIFIED.);
#147=B_SPLINE_CURVE_WITH_KNOTS('',3,(#14546,#14547,#14548,#14549,#14550,
#14551,#14552,#14553,#14554,#14555,#14556,#14557,#14558,#14559,#14560,#14561,
#14562,#14563,#14564,#14565,#14566,#14567,#14568,#14569,#14570,#14571,#14572,
#14573,#14574,#14575,#14576,#14577,#14578,#14579,#14580,#14581,#14582,#14583,
#14584,#14585,#14586,#14587,#14588,#14589,#14590,#14591,#14592,#14593,#14594,
#14595,#14596,#14597,#14598,#14599,#14600,#14601,#14602,#14603,#14604,#14605,
#14606,#14607,#14608,#14609,#14610,#14611,#14612,#14613,#14614,#14615,#14616,
#14617,#14618,#14619,#14620,#14621,#14622,#14623,#14624,#14625,#14626,#14627,
#14628,#14629,#14630,#14631,#14632,#14633,#14634,#14635,#14636,#14637,#14638,
#14639,#14640,#14641,#14642,#14643,#14644,#14645,#14646,#14647,#14648,#14649,
#14650,#14651,#14652,#14653,#14654,#14655,#14656,#14657,#14658,#14659,#14660,
#14661,#14662,#14663,#14664,#14665,#14666,#14667,#14668,#14669,#14670,#14671,
#14672,#14673,#14674,#14675,#14676,#14677,#14678,#14679,#14680,#14681,#14682,
#14683,#14684,#14685,#14686,#14687,#14688,#14689,#14690,#14691,#14692,#14693,
#14694,#14695,#14696,#14697,#14698,#14699,#14700,#14701,#14702,#14703,#14704,
#14705,#14706,#14707,#14708,#14709,#14710,#14711,#14712,#14713,#14714,#14715,
#14716,#14717,#14718,#14719,#14720,#14721,#14722,#14723,#14724,#14725,#14726,
#14727,#14728,#14729,#14730,#14731,#14732,#14733,#14734,#14735,#14736,#14737,
#14738,#14739,#14740,#14741,#14742,#14743,#14744,#14745,#14746,#14747,#14748,
#14749,#14750,#14751,#14752,#14753),.UNSPECIFIED.,.F.,.F.,(4,3,3,3,3,3,
3,3,3,3,3,3,3,3,3,3,3,3,3,3,3,3,3,3,3,3,3,3,3,3,3,3,3,3,3,3,3,3,3,3,3,3,
3,3,3,3,3,3,3,3,3,3,3,3,3,3,3,3,3,3,3,3,3,3,3,3,3,3,3,4),(13.6836710230158,
13.7985703413321,13.9151166307046,13.9785673454441,14.0738005443357,14.1689023992021,
14.2639024761147,14.3588340738977,14.4537311521857,14.5486202705559,14.6435279741488,
14.7385399622103,14.8336103241159,14.9288346254482,14.9770364415473,15.0722696271906,
15.1673714688582,15.26237153264,15.3573031174507,15.4522001828701,15.5470892884921,
15.6419969794739,15.7370089552118,15.8320793049388,15.9273035944392,15.9755055376504,
16.0707387051867,16.1658405283805,16.26084057335,16.3557721389227,16.4506691848468,
16.5455582707402,16.6404659417835,16.7354778973849,16.8305482268328,16.9257724960296,
16.9739746337536,17.0692078134899,17.1643096490601,17.2593097065639,17.3542412848531,
17.4491383436021,17.5440274424128,17.6389351264502,17.7339470950829,17.8290174376026,
17.9242417198066,17.9724437298567,18.0676769073885,18.1627787407457,18.2577787960312,
18.3527103721036,18.4476074286378,18.5424965252383,18.637404207073,18.732416173528,
18.8274865138812,18.9227107939571,18.9709128259599,19.066102612376,19.1611610822308,
19.2561178627604,19.3510063526438,19.4458605160811,19.5407069670992,19.6355723055026,
19.7305419746598,19.8255703930562,19.9207520511273,19.966856329907),
 .UNSPECIFIED.);
#148=B_SPLINE_CURVE_WITH_KNOTS('',3,(#14755,#14756,#14757,#14758,#14759,
#14760,#14761,#14762,#14763,#14764,#14765,#14766,#14767,#14768,#14769,#14770,
#14771,#14772,#14773,#14774,#14775,#14776,#14777,#14778,#14779,#14780,#14781,
#14782,#14783,#14784,#14785,#14786,#14787,#14788,#14789,#14790,#14791,#14792,
#14793,#14794,#14795,#14796,#14797,#14798,#14799,#14800,#14801,#14802,#14803,
#14804,#14805,#14806,#14807,#14808,#14809,#14810,#14811,#14812,#14813,#14814,
#14815,#14816,#14817,#14818,#14819,#14820,#14821,#14822,#14823,#14824,#14825,
#14826,#14827,#14828,#14829,#14830,#14831,#14832,#14833,#14834,#14835,#14836,
#14837,#14838,#14839,#14840,#14841,#14842,#14843,#14844,#14845,#14846,#14847,
#14848,#14849,#14850,#14851,#14852,#14853,#14854,#14855,#14856,#14857,#14858,
#14859,#14860,#14861,#14862,#14863,#14864,#14865,#14866,#14867,#14868,#14869,
#14870,#14871,#14872,#14873,#14874,#14875,#14876,#14877,#14878,#14879,#14880,
#14881,#14882,#14883,#14884,#14885,#14886,#14887,#14888,#14889,#14890,#14891,
#14892,#14893,#14894,#14895,#14896,#14897,#14898,#14899,#14900,#14901,#14902,
#14903,#14904,#14905,#14906,#14907,#14908,#14909,#14910,#14911,#14912,#14913,
#14914,#14915,#14916,#14917,#14918,#14919,#14920,#14921,#14922,#14923,#14924,
#14925,#14926,#14927,#14928,#14929,#14930,#14931,#14932,#14933,#14934,#14935,
#14936,#14937,#14938,#14939,#14940,#14941,#14942,#14943,#14944,#14945,#14946,
#14947,#14948,#14949,#14950,#14951,#14952,#14953,#14954,#14955,#14956,#14957,
#14958,#14959,#14960,#14961,#14962,#14963,#14964,#14965),.UNSPECIFIED.,
 .F.,.F.,(4,3,3,3,3,3,3,3,3,3,3,3,3,3,3,3,3,3,3,3,3,3,3,3,3,3,3,3,3,3,3,
3,3,3,3,3,3,3,3,3,3,3,3,3,3,3,3,3,3,3,3,3,3,3,3,3,3,3,3,3,3,3,3,3,3,3,3,
3,3,3,4),(19.9668563310701,19.969381922063,20.0646150993086,20.1597169323645,
20.2547169873338,20.3496485630696,20.4445456192546,20.5394347154935,20.6343423969547,
20.7293543630204,20.8244247029744,20.9196489826402,20.9678510181662,21.0630841950999,
21.1581860278414,21.2531860824947,21.348117657913,21.4430147137796,21.5379038096999,
21.6328114908426,21.7278234565917,21.82289379623,21.918118075584,21.9663201142693,
22.0615532910726,22.1566551236806,22.2516551781973,22.3465867534752,22.4414838091989,
22.5363729049742,22.6312805859698,22.7262925515696,22.8213628910571,22.9165871702596,
22.9647892103725,23.0600223873118,23.1551242200579,23.2501242747148,23.345055850135,
23.4399529060026,23.5348420019228,23.6297496830645,23.724761648811,23.8198319884458,
23.9150562677951,23.9632583064756,24.0584914833744,24.1535933160796,24.2485933706953,
24.343524946074,24.4384220018998,24.5333110977782,24.6282187788779,24.7232307445827,
24.8183010841758,24.9135253634839,24.9617274025788,25.0569605794681,25.1520624121635,
25.247062466769,25.3419940421372,25.4368910979524,25.53178019382,25.6266878749087,
25.7216998406021,25.8167701801838,25.9119944594803,25.9601964986819,26.0776664416472,
26.1934396858132,26.2500416368193),.UNSPECIFIED.);
#149=B_SPLINE_CURVE_WITH_KNOTS('',3,(#14967,#14968,#14969,#14970,#14971,
#14972,#14973,#14974,#14975,#14976,#14977,#14978,#14979,#14980,#14981,#14982,
#14983,#14984,#14985,#14986,#14987,#14988,#14989,#14990,#14991,#14992,#14993,
#14994,#14995,#14996,#14997,#14998,#14999,#15000,#15001,#15002,#15003,#15004,
#15005,#15006,#15007,#15008,#15009,#15010,#15011,#15012,#15013,#15014,#15015,
#15016,#15017,#15018,#15019,#15020,#15021,#15022,#15023,#15024,#15025,#15026,
#15027,#15028,#15029,#15030,#15031,#15032,#15033,#15034,#15035,#15036,#15037,
#15038,#15039,#15040,#15041,#15042,#15043,#15044,#15045,#15046,#15047,#15048,
#15049,#15050,#15051,#15052,#15053,#15054,#15055,#15056,#15057,#15058,#15059,
#15060,#15061,#15062,#15063,#15064,#15065,#15066,#15067,#15068,#15069,#15070,
#15071,#15072,#15073,#15074,#15075,#15076,#15077,#15078,#15079,#15080,#15081,
#15082,#15083,#15084,#15085,#15086,#15087,#15088,#15089,#15090,#15091,#15092,
#15093,#15094,#15095,#15096,#15097,#15098,#15099,#15100,#15101,#15102,#15103,
#15104,#15105,#15106,#15107,#15108,#15109,#15110,#15111,#15112,#15113,#15114,
#15115,#15116,#15117,#15118,#15119,#15120,#15121,#15122,#15123,#15124,#15125,
#15126,#15127,#15128,#15129,#15130,#15131,#15132,#15133,#15134,#15135,#15136,
#15137,#15138,#15139,#15140,#15141,#15142,#15143,#15144,#15145,#15146,#15147,
#15148,#15149,#15150,#15151,#15152,#15153,#15154,#15155,#15156,#15157,#15158,
#15159,#15160,#15161,#15162,#15163,#15164,#15165,#15166,#15167,#15168,#15169,
#15170,#15171,#15172,#15173,#15174),.UNSPECIFIED.,.F.,.F.,(4,3,3,3,3,3,
3,3,3,3,3,3,3,3,3,3,3,3,3,3,3,3,3,3,3,3,3,3,3,3,3,3,3,3,3,3,3,3,3,3,3,3,
3,3,3,3,3,3,3,3,3,3,3,3,3,3,3,3,3,3,3,3,3,3,3,3,3,3,3,4),(26.2500416370864,
26.3442956412353,26.4385114134094,26.5327162678039,26.626937501813,26.7212619406864,
26.815644110387,26.910181456667,26.9586655947851,27.0538987716832,27.1490006043877,
27.2440006590025,27.3389322343801,27.4338292902048,27.528718386082,27.6236260671802,
27.7186380328836,27.8137083724751,27.9089326517814,27.9571346908882,28.0523678677858,
28.1474697004896,28.2424697551041,28.3374013304812,28.4322983863053,28.5271874821818,
28.6220951632799,28.7171071289826,28.8121774685736,28.9074017478793,28.9556037869914,
29.0508369638904,29.1459387965958,29.2409388512117,29.3358704265903,29.4307674824158,
29.5256565782939,29.6205642593929,29.7155762250971,29.8106465646894,29.9058708439967,
29.9540728830945,30.0493060599929,30.1444078926975,30.2394079473122,30.3343395226901,
30.4292365785151,30.5241256743925,30.6190333554911,30.7140453211946,30.8091156607864,
30.9043399400928,30.9525419791977,31.0477751560962,31.142876988801,31.2378770434165,
31.3328086187944,31.4277056746193,31.5225947704971,31.617502451596,31.7125144172995,
31.8075847568911,31.9028090361976,31.9510110753008,32.0481125083967,32.1450646576551,
32.2421052293078,32.3388092131387,32.4360180787024,32.5332269442661),
 .UNSPECIFIED.);
#150=B_SPLINE_CURVE_WITH_KNOTS('',3,(#15176,#15177,#15178,#15179,#15180,
#15181,#15182,#15183,#15184,#15185,#15186,#15187,#15188,#15189,#15190,#15191,
#15192,#15193,#15194,#15195,#15196,#15197,#15198,#15199,#15200,#15201,#15202,
#15203,#15204,#15205,#15206,#15207,#15208,#15209,#15210,#15211,#15212,#15213,
#15214,#15215,#15216,#15217,#15218,#15219,#15220,#15221,#15222,#15223,#15224,
#15225,#15226,#15227,#15228,#15229,#15230,#15231,#15232,#15233,#15234,#15235,
#15236,#15237,#15238,#15239,#15240,#15241,#15242,#15243,#15244,#15245,#15246,
#15247,#15248,#15249,#15250,#15251,#15252,#15253,#15254,#15255,#15256,#15257,
#15258,#15259,#15260,#15261,#15262,#15263,#15264,#15265,#15266,#15267,#15268,
#15269,#15270,#15271,#15272,#15273,#15274,#15275,#15276,#15277,#15278,#15279,
#15280,#15281,#15282,#15283,#15284,#15285,#15286,#15287,#15288,#15289,#15290,
#15291,#15292,#15293,#15294,#15295,#15296,#15297,#15298,#15299,#15300,#15301,
#15302,#15303,#15304,#15305,#15306,#15307,#15308,#15309,#15310,#15311,#15312,
#15313,#15314,#15315,#15316,#15317,#15318,#15319,#15320,#15321,#15322,#15323,
#15324,#15325,#15326,#15327,#15328,#15329,#15330,#15331,#15332,#15333,#15334,
#15335,#15336,#15337,#15338,#15339,#15340,#15341,#15342,#15343,#15344,#15345,
#15346,#15347,#15348,#15349,#15350,#15351,#15352,#15353,#15354,#15355,#15356,
#15357,#15358,#15359,#15360,#15361,#15362,#15363,#15364,#15365,#15366,#15367,
#15368,#15369,#15370,#15371,#15372,#15373,#15374,#15375,#15376,#15377,#15378,
#15379,#15380,#15381,#15382,#15383),.UNSPECIFIED.,.F.,.F.,(4,3,3,3,3,3,
3,3,3,3,3,3,3,3,3,3,3,3,3,3,3,3,3,3,3,3,3,3,3,3,3,3,3,3,3,3,3,3,3,3,3,3,
3,3,3,3,3,3,3,3,3,3,3,3,3,3,3,3,3,3,3,3,3,3,3,3,3,3,3,4),(32.5332269444471,
32.6372902511863,32.7414250445488,32.8460277844409,32.949480171404,33.0447133483024,
33.139815181007,33.2348152356221,33.3297468109999,33.4246438668248,33.5195329627023,
33.6144406438008,33.7094526095044,33.804522949096,33.8997472284026,33.9479492675071,
34.0431824444056,34.1382842771103,34.2332843317255,34.3282159071034,34.4231129629284,
34.5180020588059,34.6129097399045,34.7079217056081,34.8029920451999,34.8982163245065,
34.9464183636103,35.0416515405094,35.1367533732147,35.2317534278304,35.326685003209,
35.4215820590346,35.5164711549127,35.611378836012,35.7063908017162,35.8014611413086,
35.8966854206158,35.9448874597135,36.040120636611,36.1352224693148,36.2302225239289,
36.325154099306,36.42005115513,36.5149402510066,36.6098479321044,36.704859897807,
36.7999302373979,36.8951545167037,36.9433565558166,37.0385897327149,37.1336915654195,
37.2286916200344,37.3236231954121,37.4185202512368,37.5134093471141,37.6083170282125,
37.7033289939159,37.7983993335075,37.8936236128138,37.9418256519198,38.0357356109504,
38.133320190983,38.2269898496088,38.320602829707,38.4141870665519,38.5077704591112,
38.6014277414157,38.6951291379142,38.788953707224,38.8164122512114),
 .UNSPECIFIED.);
#151=B_SPLINE_CURVE_WITH_KNOTS('',3,(#15385,#15386,#15387,#15388,#15389,
#15390,#15391,#15392,#15393,#15394,#15395,#15396,#15397,#15398,#15399,#15400,
#15401,#15402,#15403,#15404,#15405,#15406,#15407,#15408,#15409,#15410,#15411,
#15412,#15413,#15414,#15415,#15416,#15417,#15418,#15419,#15420,#15421,#15422,
#15423,#15424,#15425,#15426,#15427,#15428,#15429,#15430,#15431,#15432,#15433,
#15434,#15435,#15436,#15437,#15438,#15439,#15440,#15441,#15442,#15443,#15444,
#15445,#15446,#15447,#15448,#15449,#15450,#15451,#15452,#15453,#15454,#15455,
#15456,#15457,#15458,#15459,#15460,#15461,#15462,#15463,#15464,#15465,#15466,
#15467,#15468,#15469,#15470,#15471,#15472,#15473,#15474,#15475,#15476,#15477,
#15478,#15479,#15480,#15481,#15482,#15483,#15484,#15485,#15486,#15487,#15488,
#15489,#15490,#15491,#15492,#15493,#15494,#15495,#15496,#15497,#15498,#15499,
#15500,#15501,#15502,#15503,#15504,#15505,#15506,#15507,#15508,#15509,#15510,
#15511,#15512,#15513,#15514,#15515,#15516,#15517,#15518,#15519,#15520,#15521,
#15522,#15523,#15524,#15525,#15526,#15527,#15528,#15529,#15530,#15531,#15532,
#15533,#15534,#15535,#15536,#15537,#15538,#15539,#15540,#15541,#15542,#15543,
#15544,#15545,#15546,#15547,#15548,#15549,#15550,#15551,#15552,#15553,#15554,
#15555,#15556,#15557,#15558,#15559,#15560,#15561,#15562,#15563,#15564,#15565,
#15566,#15567,#15568,#15569,#15570,#15571,#15572,#15573,#15574,#15575,#15576,
#15577,#15578,#15579,#15580,#15581,#15582,#15583,#15584,#15585,#15586,#15587,
#15588,#15589,#15590,#15591,#15592),.UNSPECIFIED.,.F.,.F.,(4,3,3,3,3,3,
3,3,3,3,3,3,3,3,3,3,3,3,3,3,3,3,3,3,3,3,3,3,3,3,3,3,3,3,3,3,3,3,3,3,3,3,
3,3,3,3,3,3,3,3,3,3,3,3,3,3,3,3,3,3,3,3,3,3,3,3,3,3,3,4),(38.8164122514458,
38.9402947480229,39.0355279249114,39.1306297576062,39.2256298122114,39.3205613875795,
39.4154584433947,39.5103475392625,39.6052552203517,39.7002671860458,39.7953375256283,
39.8905618049258,39.9387638441261,40.0339970210259,40.1290988537319,40.2240989083482,
40.319030483727,40.4139275395529,40.5088166354311,40.6037243165304,40.6987362822345,
40.7938066218268,40.8890309011337,40.9372329402292,41.0324661171702,41.1275679499177,
41.2225680045755,41.3174995799963,41.412396635864,41.5072857317841,41.6021934129253,
41.697205378671,41.7922757183046,41.8874999976523,41.9357020363324,42.0309352131271,
42.1260370457283,42.22103710024,42.3159686755154,42.4108657312383,42.5057548270144,
42.6006625080123,42.6956744736171,42.7907448131109,42.8859690923218,42.9341711324355,
43.0294043093814,43.1245061421326,43.2195061967932,43.314437772215,43.4093348280827,
43.5042239240018,43.5991316051411,43.6941435708833,43.7892139105126,43.8844381898547,
43.9326402285387,44.0278734057947,44.1229752388588,44.2179752938344,44.3129068695732,
44.407803925759,44.5026930219969,44.5976007034551,44.6926126695148,44.7876830094613,
44.8829072891169,44.9311093246418,45.0810523173759,45.0995975586252),
 .UNSPECIFIED.);
#152=B_SPLINE_CURVE_WITH_KNOTS('',3,(#15594,#15595,#15596,#15597,#15598,
#15599,#15600,#15601,#15602,#15603,#15604,#15605,#15606,#15607,#15608,#15609,
#15610,#15611,#15612,#15613,#15614,#15615,#15616,#15617,#15618,#15619,#15620,
#15621,#15622,#15623,#15624,#15625,#15626,#15627,#15628,#15629,#15630,#15631,
#15632,#15633,#15634,#15635,#15636,#15637,#15638,#15639,#15640,#15641,#15642,
#15643,#15644,#15645,#15646,#15647,#15648,#15649,#15650,#15651,#15652,#15653,
#15654,#15655,#15656,#15657,#15658,#15659,#15660,#15661,#15662,#15663,#15664,
#15665,#15666,#15667,#15668,#15669,#15670,#15671,#15672,#15673,#15674,#15675,
#15676,#15677,#15678,#15679,#15680,#15681,#15682,#15683,#15684,#15685,#15686,
#15687,#15688,#15689,#15690,#15691,#15692,#15693,#15694,#15695,#15696,#15697,
#15698,#15699,#15700,#15701,#15702,#15703,#15704,#15705,#15706,#15707,#15708,
#15709,#15710,#15711,#15712,#15713,#15714,#15715,#15716,#15717,#15718,#15719,
#15720,#15721,#15722,#15723,#15724,#15725,#15726,#15727,#15728,#15729,#15730,
#15731,#15732,#15733,#15734,#15735,#15736,#15737,#15738,#15739,#15740,#15741,
#15742,#15743,#15744,#15745,#15746,#15747,#15748,#15749,#15750,#15751,#15752,
#15753,#15754,#15755,#15756,#15757,#15758,#15759,#15760,#15761,#15762,#15763,
#15764,#15765,#15766,#15767,#15768,#15769,#15770,#15771,#15772,#15773,#15774,
#15775,#15776,#15777,#15778,#15779,#15780,#15781,#15782,#15783,#15784,#15785,
#15786,#15787,#15788,#15789,#15790,#15791,#15792,#15793,#15794,#15795,#15796,
#15797,#15798,#15799,#15800,#15801),.UNSPECIFIED.,.F.,.F.,(4,3,3,3,3,3,
3,3,3,3,3,3,3,3,3,3,3,3,3,3,3,3,3,3,3,3,3,3,3,3,3,3,3,3,3,3,3,3,3,3,3,3,
3,3,3,3,3,3,3,3,3,3,3,3,3,3,3,3,3,3,3,3,3,3,3,3,3,3,3,4),(45.0995975587957,
45.1932779352248,45.2868546323476,45.3803749446052,45.473866884399,45.5673584285438,
45.6609386622286,45.7545628987289,45.848346419118,45.929578420745,46.0248115984109,
46.1199134318747,46.2149134872393,46.3098450633499,46.4047421198968,46.4996312164845,
46.5945388982812,46.68955086466,46.7846212049148,46.8798454848594,46.9280475168481,
47.0232806966308,47.1183825322378,47.213382589769,47.3083141680714,47.4032112268248,
47.4981003256312,47.5930080096552,47.6880199782615,47.7830903207475,47.8783146029061,
47.9265166129513,48.0217497797786,48.1168516024089,48.2118516469599,48.3067832123307,
48.4016802581877,48.4965693441479,48.5914770153927,48.6864889713977,48.7815593013646,
48.8767835712549,48.9249857090544,49.0202188961172,49.1153207389126,49.2103208035327,
49.3052523887474,49.4001494543016,49.4950385597896,49.5899462503684,49.6849582252982,
49.7800285739857,49.8752528620976,49.9234548051576,50.0186880039757,50.1137898587833,
50.2087899356529,50.3037215334149,50.3986186116959,50.4935077300731,50.588415433687,
50.6834274217903,50.7784977837497,50.8737220851538,50.9219239012607,51.0239506924649,
51.1256428471772,51.2271277096782,51.3283182871639,51.3827828656131),
 .UNSPECIFIED.);
#153=B_SPLINE_CURVE_WITH_KNOTS('',3,(#15803,#15804,#15805,#15806,#15807,
#15808,#15809,#15810,#15811,#15812,#15813,#15814,#15815,#15816,#15817,#15818,
#15819,#15820,#15821,#15822,#15823,#15824,#15825,#15826,#15827,#15828,#15829,
#15830,#15831,#15832,#15833,#15834,#15835,#15836,#15837,#15838,#15839,#15840,
#15841,#15842,#15843,#15844,#15845,#15846,#15847,#15848,#15849,#15850,#15851,
#15852,#15853,#15854,#15855,#15856,#15857,#15858,#15859,#15860,#15861,#15862,
#15863,#15864,#15865,#15866,#15867,#15868,#15869,#15870,#15871,#15872,#15873,
#15874,#15875,#15876,#15877,#15878,#15879,#15880,#15881,#15882,#15883,#15884,
#15885,#15886,#15887,#15888,#15889,#15890,#15891,#15892,#15893,#15894,#15895,
#15896,#15897,#15898,#15899,#15900,#15901,#15902,#15903,#15904,#15905,#15906,
#15907,#15908,#15909,#15910,#15911,#15912,#15913,#15914,#15915,#15916,#15917,
#15918,#15919,#15920,#15921,#15922,#15923,#15924,#15925,#15926,#15927,#15928,
#15929,#15930,#15931,#15932,#15933,#15934,#15935,#15936,#15937,#15938,#15939,
#15940,#15941,#15942,#15943,#15944,#15945,#15946,#15947,#15948,#15949,#15950,
#15951,#15952,#15953,#15954,#15955,#15956,#15957,#15958,#15959,#15960,#15961,
#15962,#15963,#15964,#15965,#15966,#15967,#15968,#15969,#15970,#15971,#15972,
#15973,#15974,#15975,#15976,#15977,#15978,#15979,#15980,#15981,#15982,#15983,
#15984,#15985,#15986,#15987,#15988,#15989,#15990,#15991,#15992,#15993,#15994,
#15995,#15996,#15997,#15998,#15999,#16000,#16001,#16002,#16003,#16004,#16005,
#16006,#16007,#16008,#16009,#16010),.UNSPECIFIED.,.F.,.F.,(4,3,3,3,3,3,
3,3,3,3,3,3,3,3,3,3,3,3,3,3,3,3,3,3,3,3,3,3,3,3,3,3,3,3,3,3,3,3,3,3,3,3,
3,3,3,3,3,3,3,3,3,3,3,3,3,3,3,3,3,3,3,3,3,3,3,3,3,3,3,4),(51.3827828658049,
51.4807372785994,51.5787843849556,51.6770268854418,51.7753771076044,51.873937487025,
51.9203929973639,52.0156262962162,52.110728250258,52.2057284254395,52.3006601197524,
52.3955572934587,52.4904465060247,52.5853543024792,52.6803663808299,52.7754368316972,
52.8706612190731,52.918862093467,53.0140954217918,53.109197407746,53.2041976172003,
53.2991293491129,53.3940265624625,53.488915816653,53.583823656652,53.6788357811606,
53.7739062797388,53.8691307167445,53.9173311895702,54.0125634707333,54.107664406289,
54.2026635635679,54.2975942450476,54.3924904094359,54.4873786174258,54.5822854152763,
54.6772965101222,54.7723659846023,54.8675894161599,54.9158002856733,55.0110348389498,
55.1061380430872,55.2011394624195,55.2960723870005,55.3909707819247,55.4858612052065,
55.5807702004123,55.675783452194,55.7708550638512,55.8660805811321,55.9142693817765,
56.0095034236643,56.1046061390741,56.1996070926603,56.2945395871862,56.3894375742971,
56.4843276123638,56.5792362453301,56.674249171574,56.7693204780544,56.8645457244948,
56.9127384778796,57.0068921897677,57.1008392901937,57.1946960848869,57.2884904327465,
57.3828598678059,57.4766387039323,57.5713034384583,57.6659681729844),
 .UNSPECIFIED.);
#154=B_SPLINE_CURVE_WITH_KNOTS('',3,(#16012,#16013,#16014,#16015,#16016,
#16017,#16018,#16019,#16020,#16021,#16022,#16023,#16024,#16025,#16026,#16027,
#16028,#16029,#16030,#16031,#16032,#16033,#16034,#16035,#16036,#16037,#16038,
#16039,#16040,#16041,#16042,#16043,#16044,#16045,#16046,#16047,#16048,#16049,
#16050,#16051,#16052,#16053,#16054,#16055,#16056,#16057,#16058,#16059,#16060,
#16061,#16062,#16063,#16064,#16065,#16066,#16067,#16068,#16069,#16070,#16071,
#16072,#16073,#16074,#16075,#16076,#16077,#16078,#16079,#16080,#16081,#16082,
#16083,#16084,#16085,#16086,#16087,#16088,#16089,#16090,#16091,#16092,#16093,
#16094,#16095,#16096,#16097,#16098,#16099,#16100,#16101,#16102,#16103,#16104,
#16105,#16106,#16107,#16108,#16109,#16110,#16111,#16112,#16113,#16114,#16115,
#16116,#16117,#16118,#16119,#16120,#16121,#16122,#16123,#16124,#16125,#16126,
#16127,#16128,#16129,#16130,#16131,#16132,#16133,#16134,#16135,#16136,#16137,
#16138,#16139,#16140,#16141,#16142,#16143,#16144,#16145,#16146,#16147,#16148,
#16149,#16150,#16151,#16152,#16153,#16154,#16155,#16156,#16157,#16158,#16159,
#16160,#16161,#16162,#16163,#16164,#16165,#16166,#16167,#16168,#16169,#16170,
#16171,#16172,#16173,#16174,#16175,#16176,#16177,#16178,#16179,#16180),
 .UNSPECIFIED.,.F.,.F.,(4,3,3,3,3,3,3,3,3,3,3,3,3,3,3,3,3,3,3,3,3,3,3,3,
3,3,3,3,3,3,3,3,3,3,3,3,3,3,3,3,3,3,3,3,3,3,3,3,3,3,3,3,3,3,3,3,4),(57.6659681732708,
57.7902087726151,57.9112075739828,58.0064556392205,58.1015723229298,58.196587171758,
58.2915333966034,58.3864450068061,58.4813485445348,58.5762705374193,58.671296531744,
58.7663807598672,58.8616185754268,58.9096766700859,59.004912436105,59.1000170253905,
59.1950199978214,59.289954715732,59.3848550519149,59.479747560965,59.5746587831537,
59.6696744600382,59.7647486129024,59.8599768249392,59.9081457661891,60.0033062082597,
60.0983350869559,60.193262068454,60.2881206954997,60.3829449061964,60.4777613484371,
60.5725966558729,60.6675371112889,60.7625363234842,60.8576907662809,60.9066148622922,
61.0020019720403,61.0972575100589,61.1924108347871,61.2874943988881,61.3825425880511,
61.4775817760709,61.5726383213704,61.6677963912266,61.7630114770783,61.8583769974531,
61.9050839583954,61.9992755558128,62.0933384919762,62.1872975266918,62.2811999994194,
62.3750735970995,62.4689459722077,62.5629043553239,62.6569055365934,62.7510620984975,
62.8314472505513),.UNSPECIFIED.);
#155=B_SPLINE_CURVE_WITH_KNOTS('',3,(#16184,#16185,#16186,#16187,#16188,
#16189,#16190,#16191),.UNSPECIFIED.,.F.,.F.,(4,1,1,1,1,4),(-64.9004912467048,
-63.9020221506017,-62.9035530544986,-61.9050839583954,-60.9066148622923,
-60.6416007602447),.UNSPECIFIED.);
#156=B_SPLINE_CURVE_WITH_KNOTS('',3,(#16193,#16194,#16195,#16196,#16197,
#16198,#16199,#16200,#16201,#16202,#16203,#16204,#16205,#16206,#16207,#16208,
#16209,#16210,#16211,#16212,#16213,#16214,#16215,#16216,#16217,#16218,#16219,
#16220,#16221,#16222,#16223,#16224,#16225,#16226,#16227,#16228,#16229,#16230,
#16231,#16232,#16233,#16234,#16235,#16236,#16237,#16238,#16239,#16240,#16241,
#16242,#16243,#16244,#16245,#16246,#16247,#16248,#16249,#16250,#16251,#16252,
#16253,#16254,#16255,#16256,#16257,#16258,#16259,#16260,#16261,#16262,#16263,
#16264,#16265,#16266,#16267,#16268,#16269,#16270,#16271,#16272,#16273,#16274,
#16275,#16276,#16277,#16278,#16279,#16280,#16281,#16282,#16283,#16284,#16285,
#16286,#16287,#16288,#16289,#16290,#16291,#16292,#16293,#16294,#16295,#16296,
#16297,#16298,#16299,#16300,#16301,#16302,#16303,#16304,#16305,#16306,#16307,
#16308,#16309,#16310,#16311,#16312,#16313,#16314,#16315,#16316,#16317,#16318,
#16319,#16320,#16321,#16322,#16323,#16324,#16325,#16326,#16327,#16328,#16329,
#16330,#16331,#16332,#16333,#16334,#16335,#16336,#16337,#16338,#16339,#16340,
#16341,#16342,#16343,#16344,#16345,#16346,#16347,#16348,#16349,#16350,#16351,
#16352,#16353,#16354,#16355,#16356,#16357,#16358,#16359,#16360,#16361,#16362,
#16363,#16364,#16365,#16366,#16367,#16368,#16369,#16370,#16371,#16372,#16373,
#16374,#16375,#16376,#16377,#16378,#16379,#16380,#16381,#16382,#16383,#16384,
#16385,#16386,#16387,#16388,#16389,#16390,#16391,#16392,#16393,#16394,#16395,
#16396,#16397,#16398,#16399,#16400),.UNSPECIFIED.,.F.,.F.,(4,3,3,3,3,3,
3,3,3,3,3,3,3,3,3,3,3,3,3,3,3,3,3,3,3,3,3,3,3,3,3,3,3,3,3,3,3,3,3,3,3,3,
3,3,3,3,3,3,3,3,3,3,3,3,3,3,3,3,3,3,3,3,3,3,3,3,3,3,3,4),(-60.6415981847468,
-60.5476350400387,-60.4537214927512,-60.3598299001311,-60.2659326468451,
-60.1719401382506,-60.0778989118986,-59.9836963724679,-59.9081457661891,
-59.8129086437597,-59.7178029735791,-59.6227991945564,-59.527864080263,
-59.4329636022303,-59.3380712056622,-59.2431603503057,-59.148145423244,
-59.0530722390154,-58.9578453257664,-58.909676670086,-58.8144300356268,
-58.7193144878493,-58.6243004814298,-58.529354660147,-58.4344431811965,
-58.3395395026492,-58.2446170968802,-58.149590280176,-58.0545049956603,
-57.9592657709175,-57.9112075739828,-57.8159821428235,-57.720888162612,
-57.6258960555731,-57.530972535854,-57.4360835997414,-57.341202677585,-57.2463032142147,
-57.1512994829464,-57.0562373995538,-56.9610213295851,-56.9127384778797,
-56.8175043351744,-56.7224015392209,-56.6274005252774,-56.5324680005851,
-56.4375700020421,-56.3426799712632,-56.2477713643077,-56.1527584922739,
-56.0576872561126,-55.9624621043086,-55.9142693817765,-55.8190349740819,
-55.7239318854878,-55.6289305517956,-55.5339976681447,-55.4390992864092,
-55.3442088485995,-55.2492998111501,-55.1542864754041,-55.0592147559437,
-54.9639890949103,-54.9158002856733,-54.8179259631399,-54.720211039569,
-54.6226729319707,-54.525238837996,-54.427905479594,-54.3584128775674),
 .UNSPECIFIED.);
#157=B_SPLINE_CURVE_WITH_KNOTS('',3,(#16402,#16403,#16404,#16405,#16406,
#16407,#16408,#16409,#16410,#16411,#16412,#16413,#16414,#16415,#16416,#16417,
#16418,#16419,#16420,#16421,#16422,#16423,#16424,#16425,#16426,#16427,#16428,
#16429,#16430,#16431,#16432,#16433,#16434,#16435,#16436,#16437,#16438,#16439,
#16440,#16441,#16442,#16443,#16444,#16445,#16446,#16447,#16448,#16449,#16450,
#16451,#16452,#16453,#16454,#16455,#16456,#16457,#16458,#16459,#16460,#16461,
#16462,#16463,#16464,#16465,#16466,#16467,#16468,#16469,#16470,#16471,#16472,
#16473,#16474,#16475,#16476,#16477,#16478,#16479,#16480,#16481,#16482,#16483,
#16484,#16485,#16486,#16487,#16488,#16489,#16490,#16491,#16492,#16493,#16494,
#16495,#16496,#16497,#16498,#16499,#16500,#16501,#16502,#16503,#16504,#16505,
#16506,#16507,#16508,#16509,#16510,#16511,#16512,#16513,#16514,#16515,#16516,
#16517,#16518,#16519,#16520,#16521,#16522,#16523,#16524,#16525,#16526,#16527,
#16528,#16529,#16530,#16531,#16532,#16533,#16534,#16535,#16536,#16537,#16538,
#16539,#16540,#16541,#16542,#16543,#16544,#16545,#16546,#16547,#16548,#16549,
#16550,#16551,#16552,#16553,#16554,#16555,#16556,#16557,#16558,#16559,#16560,
#16561,#16562,#16563,#16564,#16565,#16566,#16567,#16568,#16569,#16570,#16571,
#16572,#16573,#16574,#16575,#16576,#16577,#16578,#16579,#16580,#16581,#16582,
#16583,#16584,#16585,#16586,#16587,#16588,#16589,#16590,#16591,#16592,#16593,
#16594,#16595,#16596,#16597,#16598,#16599,#16600,#16601,#16602,#16603,#16604,
#16605,#16606,#16607,#16608,#16609),.UNSPECIFIED.,.F.,.F.,(4,3,3,3,3,3,
3,3,3,3,3,3,3,3,3,3,3,3,3,3,3,3,3,3,3,3,3,3,3,3,3,3,3,3,3,3,3,3,3,3,3,3,
3,3,3,3,3,3,3,3,3,3,3,3,3,3,3,3,3,3,3,3,3,3,3,3,3,3,3,4),(-54.3584128772902,
-54.2562491996727,-54.1536641317825,-54.0508554030152,-53.9477257033755,
-53.9173311895702,-53.8220978553623,-53.726995864671,-53.6319956516206,
-53.5370639178197,-53.4421667036412,-53.347277449681,-53.2523696109718,
-53.1573574893496,-53.06228699457,-52.9670625627409,-52.918862093467,-52.8236288091345,
-52.7285268666147,-52.633526699971,-52.5385950097338,-52.4436978373347,
-52.3488086233097,-52.2539008226304,-52.1588887358914,-52.0638182742564,
-51.9685938725254,-51.9203929973639,-51.8251599103758,-51.7300581689489,
-51.6350582068426,-51.5401267254171,-51.4452297644054,-51.350340764085,
-51.2554331791706,-51.1604213100182,-51.0653510673298,-50.9701268845282,
-50.9219239012607,-50.826690702328,-50.7315888474202,-50.6365887704656,
-50.5416571726404,-50.4467600943099,-50.3518709758971,-50.2569632722615,
-50.1619512841573,-50.0668809222091,-49.9716566208346,-49.9234548051576,
-49.8282216195079,-49.7331197778338,-49.6381197140452,-49.5431881292274,
-49.4482910638008,-49.3534019581714,-49.2584942671821,-49.1634822914365,
-49.0684119417016,-48.9731876521932,-48.9249857090544,-48.8311534134105,
-48.7366626830585,-48.6430693691703,-48.5495338342124,-48.4560280787456,
-48.3608279517078,-48.2672557543579,-48.1712416624761,-48.0752275705943),
 .UNSPECIFIED.);
#158=B_SPLINE_CURVE_WITH_KNOTS('',3,(#16611,#16612,#16613,#16614,#16615,
#16616,#16617,#16618,#16619,#16620,#16621,#16622,#16623,#16624,#16625,#16626,
#16627,#16628,#16629,#16630,#16631,#16632,#16633,#16634,#16635,#16636,#16637,
#16638,#16639,#16640,#16641,#16642,#16643,#16644,#16645,#16646,#16647,#16648,
#16649,#16650,#16651,#16652,#16653,#16654,#16655,#16656,#16657,#16658,#16659,
#16660,#16661,#16662,#16663,#16664,#16665,#16666,#16667,#16668,#16669,#16670,
#16671,#16672,#16673,#16674,#16675,#16676,#16677,#16678,#16679,#16680,#16681,
#16682,#16683,#16684,#16685,#16686,#16687,#16688,#16689,#16690,#16691,#16692,
#16693,#16694,#16695,#16696,#16697,#16698,#16699,#16700,#16701,#16702,#16703,
#16704,#16705,#16706,#16707,#16708,#16709,#16710,#16711,#16712,#16713,#16714,
#16715,#16716,#16717,#16718,#16719,#16720,#16721,#16722,#16723,#16724,#16725,
#16726,#16727,#16728,#16729,#16730,#16731,#16732,#16733,#16734,#16735,#16736,
#16737,#16738,#16739,#16740,#16741,#16742,#16743,#16744,#16745,#16746,#16747,
#16748,#16749,#16750,#16751,#16752,#16753,#16754,#16755,#16756,#16757,#16758,
#16759,#16760,#16761,#16762,#16763,#16764,#16765,#16766,#16767,#16768,#16769,
#16770,#16771,#16772,#16773,#16774,#16775,#16776,#16777,#16778,#16779,#16780,
#16781,#16782,#16783,#16784,#16785,#16786,#16787,#16788,#16789,#16790,#16791,
#16792,#16793,#16794,#16795,#16796,#16797,#16798,#16799,#16800,#16801,#16802,
#16803,#16804,#16805,#16806,#16807,#16808,#16809,#16810,#16811,#16812,#16813,
#16814,#16815),.UNSPECIFIED.,.F.,.F.,(4,3,3,3,3,3,3,3,3,3,3,3,3,3,3,3,3,
3,3,3,3,3,3,3,3,3,3,3,3,3,3,3,3,3,3,3,3,3,3,3,3,3,3,3,3,3,3,3,3,3,3,3,3,
3,3,3,3,3,3,3,3,3,3,3,3,3,3,3,4),(-48.0752275703877,-47.9265166129513,-47.8312834332093,
-47.7361815976334,-47.6411815401237,-47.5462499618286,-47.4513529030737,
-47.356463804257,-47.2615561202136,-47.166544151575,-47.0714738090493,-46.9762495268394,
-46.9280475168481,-46.832814339316,-46.7377125059585,-46.6427124506726,
-46.5477808745998,-46.4528838180653,-46.3579947214643,-46.2630870396291,
-46.1680750731736,-46.07300473282,-45.9777804527437,-45.929578420745,-45.8343452448031,
-45.7392434130709,-45.6442433594427,-45.549311785069,-45.4544147302587,
-45.3595256354049,-45.2646179553379,-45.1696059906717,-45.0745356521221,
-44.9793113738549,-44.9311093246418,-44.8358761473955,-44.7407743143389,
-44.6457742593688,-44.5508426836322,-44.4559456274466,-44.3610565312069,
-44.2661488497449,-44.1711368836785,-44.0760665437236,-43.980842264057,
-43.9326402285387,-43.837407051605,-43.7423052188635,-43.6473051642101,
-43.5523735887918,-43.4574765329253,-43.3625874370049,-43.2676797558623,
-43.1726677901132,-43.0775974504749,-42.9823731711208,-42.9341711324355,
-42.8389379556324,-42.7438361230246,-42.6488360685081,-42.5539044932305,
-42.459007437507,-42.364118341732,-42.2692106607367,-42.174198695137,-42.0791283556497,
-41.9839040764474,-41.9357020363324,-41.792042263208),.UNSPECIFIED.);
#159=B_SPLINE_CURVE_WITH_KNOTS('',3,(#16817,#16818,#16819,#16820,#16821,
#16822,#16823,#16824,#16825,#16826,#16827,#16828,#16829,#16830,#16831,#16832,
#16833,#16834,#16835,#16836,#16837,#16838,#16839,#16840,#16841,#16842,#16843,
#16844,#16845,#16846,#16847,#16848,#16849,#16850,#16851,#16852,#16853,#16854,
#16855,#16856,#16857,#16858,#16859,#16860,#16861,#16862,#16863,#16864,#16865,
#16866,#16867,#16868,#16869,#16870,#16871,#16872,#16873,#16874,#16875,#16876,
#16877,#16878,#16879,#16880,#16881,#16882,#16883,#16884,#16885,#16886,#16887,
#16888,#16889,#16890,#16891,#16892,#16893,#16894,#16895,#16896,#16897,#16898,
#16899,#16900,#16901,#16902,#16903,#16904,#16905,#16906,#16907,#16908,#16909,
#16910,#16911,#16912,#16913,#16914,#16915,#16916,#16917,#16918,#16919,#16920,
#16921,#16922,#16923,#16924,#16925,#16926,#16927,#16928,#16929,#16930,#16931,
#16932,#16933,#16934,#16935,#16936,#16937,#16938,#16939,#16940,#16941,#16942,
#16943,#16944,#16945,#16946,#16947,#16948,#16949,#16950,#16951,#16952,#16953,
#16954,#16955,#16956,#16957,#16958,#16959,#16960,#16961,#16962,#16963,#16964,
#16965,#16966,#16967,#16968,#16969,#16970,#16971,#16972,#16973,#16974,#16975,
#16976,#16977,#16978,#16979,#16980,#16981,#16982,#16983,#16984,#16985,#16986,
#16987,#16988,#16989,#16990,#16991,#16992,#16993,#16994,#16995,#16996,#16997,
#16998,#16999,#17000,#17001,#17002,#17003,#17004,#17005,#17006,#17007,#17008,
#17009,#17010,#17011,#17012,#17013,#17014,#17015,#17016,#17017,#17018,#17019,
#17020,#17021,#17022,#17023,#17024),.UNSPECIFIED.,.F.,.F.,(4,3,3,3,3,3,
3,3,3,3,3,3,3,3,3,3,3,3,3,3,3,3,3,3,3,3,3,3,3,3,3,3,3,3,3,3,3,3,3,3,3,3,
3,3,3,3,3,3,3,3,3,3,3,3,3,3,3,3,3,3,3,3,3,3,3,3,3,3,3,4),(-41.7920422629959,
-41.6983020718591,-41.6031684304054,-41.5096071386079,-41.4160808478565,
-41.3225615994021,-41.2262294346088,-41.132586215821,-41.0349095780251,
-40.9372329402292,-40.8419997633305,-40.7468979306253,-40.6518978760097,
-40.5569663006309,-40.4620692448051,-40.3671801489268,-40.2722724678267,
-40.177260502122,-40.082190162529,-39.986965883221,-39.9387638441261,-39.8435306672368,
-39.7484288345412,-39.6534287799355,-39.5584972045672,-39.4636001487521,
-39.3687110528847,-39.2738033717959,-39.1787914061024,-39.0837210665206,
-38.9884967872241,-38.9402947480229,-38.8450615711197,-38.7499597384101,
-38.6549596837903,-38.5600281084075,-38.4651310525776,-38.3702419566952,
-38.2753342755915,-38.1803223098829,-38.0852519702858,-37.9900276909743,
-37.9418256519198,-37.8465924750215,-37.7514906423169,-37.6564905877022,
-37.5615590123245,-37.4666619564998,-37.3717728606225,-37.2768651795238,
-37.1818532138203,-37.0867828742286,-36.9915585949221,-36.9433565558166,
-36.8481233789189,-36.7530215462151,-36.6580214916009,-36.5630899162239,
-36.4681928603998,-36.373303764523,-36.2783960834249,-36.1833841177223,
-36.0883137781316,-35.9930894988259,-35.9448874597135,-35.8414187106333,
-35.7383353835895,-35.6355021233564,-35.5330254003549,-35.5088569563256),
 .UNSPECIFIED.);
#160=B_SPLINE_CURVE_WITH_KNOTS('',3,(#17026,#17027,#17028,#17029,#17030,
#17031,#17032,#17033,#17034,#17035,#17036,#17037,#17038,#17039,#17040,#17041,
#17042,#17043,#17044,#17045,#17046,#17047,#17048,#17049,#17050,#17051,#17052,
#17053,#17054,#17055,#17056,#17057,#17058,#17059,#17060,#17061,#17062,#17063,
#17064,#17065,#17066,#17067,#17068,#17069,#17070,#17071,#17072,#17073,#17074,
#17075,#17076,#17077,#17078,#17079,#17080,#17081,#17082,#17083,#17084,#17085,
#17086,#17087,#17088,#17089,#17090,#17091,#17092,#17093,#17094,#17095,#17096,
#17097,#17098,#17099,#17100,#17101,#17102,#17103,#17104,#17105,#17106,#17107,
#17108,#17109,#17110,#17111,#17112,#17113,#17114,#17115,#17116,#17117,#17118,
#17119,#17120,#17121,#17122,#17123,#17124,#17125,#17126,#17127,#17128,#17129,
#17130,#17131,#17132,#17133,#17134,#17135,#17136,#17137,#17138,#17139,#17140,
#17141,#17142,#17143,#17144,#17145,#17146,#17147,#17148,#17149,#17150,#17151,
#17152,#17153,#17154,#17155,#17156,#17157,#17158,#17159,#17160,#17161,#17162,
#17163,#17164,#17165,#17166,#17167,#17168,#17169,#17170,#17171,#17172,#17173,
#17174,#17175,#17176,#17177,#17178,#17179,#17180,#17181,#17182,#17183,#17184,
#17185,#17186,#17187,#17188,#17189,#17190,#17191,#17192,#17193,#17194,#17195,
#17196,#17197,#17198,#17199,#17200,#17201,#17202,#17203,#17204,#17205,#17206,
#17207,#17208,#17209,#17210,#17211,#17212,#17213,#17214,#17215,#17216,#17217,
#17218,#17219,#17220,#17221,#17222,#17223,#17224,#17225,#17226,#17227,#17228,
#17229,#17230,#17231,#17232,#17233),.UNSPECIFIED.,.F.,.F.,(4,3,3,3,3,3,
3,3,3,3,3,3,3,3,3,3,3,3,3,3,3,3,3,3,3,3,3,3,3,3,3,3,3,3,3,3,3,3,3,3,3,3,
3,3,3,3,3,3,3,3,3,3,3,3,3,3,3,3,3,3,3,3,3,3,3,3,3,3,3,4),(-35.5088569560286,
-35.4116942923171,-35.3144674214492,-35.2170727180144,-35.119590030636,
-35.0219006533429,-34.9464183636103,-34.8511851867119,-34.7560833540071,
-34.6610832993923,-34.5661517240144,-34.4712546681895,-34.3763655723121,
-34.2814578912133,-34.1864459255097,-34.0913755859181,-33.9961513066115,
-33.9479492675072,-33.8527160906088,-33.757614257904,-33.6626142032893,
-33.5676826279114,-33.4727855720865,-33.3778964762091,-33.2829887951106,
-33.1879768294071,-33.0929064898154,-32.9976822105088,-32.949480171404,
-32.8542469945053,-32.7591451618005,-32.6641451071851,-32.5692135318069,
-32.4743164759818,-32.3794273801041,-32.2845196990056,-32.1895077333018,
-32.09443739371,-31.9992131144032,-31.9510110753009,-31.8557778984026,-31.7606760656978,
-31.6656760110824,-31.5707444357045,-31.4758473798796,-31.3809582840021,
-31.2860506029035,-31.1910386372,-31.0959682976082,-31.0007440183016,-30.9525419791977,
-30.8573088022992,-30.7622069695944,-30.6672069149792,-30.5722753396014,
-30.4773782837763,-30.3824891878987,-30.2875815068003,-30.1925695410967,
-30.0974992015048,-30.0022749221982,-29.9540728830946,-29.8597759658973,
-29.7655993400692,-29.6715152517421,-29.5774960483942,-29.4834917361403,
-29.3894992479983,-29.2954458217341,-29.2256716488489),.UNSPECIFIED.);
#161=B_SPLINE_CURVE_WITH_KNOTS('',3,(#17235,#17236,#17237,#17238,#17239,
#17240,#17241,#17242,#17243,#17244,#17245,#17246,#17247,#17248,#17249,#17250,
#17251,#17252,#17253,#17254,#17255,#17256,#17257,#17258,#17259,#17260,#17261,
#17262,#17263,#17264,#17265,#17266,#17267,#17268,#17269,#17270,#17271,#17272,
#17273,#17274,#17275,#17276,#17277,#17278,#17279,#17280,#17281,#17282,#17283,
#17284,#17285,#17286,#17287,#17288,#17289,#17290,#17291,#17292,#17293,#17294,
#17295,#17296,#17297,#17298,#17299,#17300,#17301,#17302,#17303,#17304,#17305,
#17306,#17307,#17308,#17309,#17310,#17311,#17312,#17313,#17314,#17315,#17316,
#17317,#17318,#17319,#17320,#17321,#17322,#17323,#17324,#17325,#17326,#17327,
#17328,#17329,#17330,#17331,#17332,#17333,#17334,#17335,#17336,#17337,#17338,
#17339,#17340,#17341,#17342,#17343,#17344,#17345,#17346,#17347,#17348,#17349,
#17350,#17351,#17352,#17353,#17354,#17355,#17356,#17357,#17358,#17359,#17360,
#17361,#17362,#17363,#17364,#17365,#17366,#17367,#17368,#17369,#17370,#17371,
#17372,#17373,#17374,#17375,#17376,#17377,#17378,#17379,#17380,#17381,#17382,
#17383,#17384,#17385,#17386,#17387,#17388,#17389,#17390,#17391,#17392,#17393,
#17394,#17395,#17396,#17397,#17398,#17399,#17400,#17401,#17402,#17403,#17404,
#17405,#17406,#17407,#17408,#17409,#17410,#17411,#17412,#17413,#17414,#17415,
#17416,#17417,#17418,#17419,#17420,#17421,#17422,#17423,#17424,#17425,#17426,
#17427,#17428,#17429,#17430,#17431,#17432,#17433,#17434,#17435,#17436,#17437,
#17438,#17439,#17440,#17441,#17442,#17443,#17444,#17445),.UNSPECIFIED.,
 .F.,.F.,(4,3,3,3,3,3,3,3,3,3,3,3,3,3,3,3,3,3,3,3,3,3,3,3,3,3,3,3,3,3,3,
3,3,3,3,3,3,3,3,3,3,3,3,3,3,3,3,3,3,3,3,3,3,3,3,3,3,3,3,3,3,3,3,3,3,3,3,
3,3,3,4),(-29.2256716486763,-29.1072434664186,-28.986625190017,-28.9556037869914,
-28.8603706100939,-28.76526877739,-28.6702687227759,-28.5753371473988,-28.4804400915747,
-28.3855509956981,-28.2906433146002,-28.1956313488974,-28.1005610093064,
-28.0053367300007,-27.9571346908882,-27.86190151399,-27.7667996812855,-27.6717996266707,
-27.576868051293,-27.4819709954682,-27.387081899591,-27.2921742184927,-27.1971622527894,
-27.1020919131979,-27.0068676338916,-26.9586655947851,-26.8634324178817,
-26.768330585172,-26.6733305305519,-26.578398955169,-26.483501899339,-26.3886128034566,
-26.293705122353,-26.1986931566446,-26.1036228170479,-26.0083985377366,
-25.9601964986819,-25.8649633217936,-25.769861489099,-25.674861434494,-25.579929859126,
-25.485032803311,-25.3901437074434,-25.2952360263545,-25.2002240606605,
-25.1051537210782,-25.0099294417809,-24.9617274025788,-24.8664942256789,
-24.7713923929728,-24.6763923383566,-24.5814607629776,-24.4865637071516,
-24.3916746112732,-24.2967669301737,-24.2017549644695,-24.1066846248772,
-24.0114603455702,-23.9632583064756,-23.8680251295345,-23.7729232967871,
-23.6779232421291,-23.5829916667083,-23.4880946108405,-23.3932055149203,
-23.298297833779,-23.2032858680333,-23.1082155283996,-23.0129912490518,
-22.9647892103725,-22.9424863416694),.UNSPECIFIED.);
#162=B_SPLINE_CURVE_WITH_KNOTS('',3,(#17447,#17448,#17449,#17450,#17451,
#17452,#17453,#17454,#17455,#17456,#17457,#17458,#17459,#17460,#17461,#17462,
#17463,#17464,#17465,#17466,#17467,#17468,#17469,#17470,#17471,#17472,#17473,
#17474,#17475,#17476,#17477,#17478,#17479,#17480,#17481,#17482,#17483,#17484,
#17485,#17486,#17487,#17488,#17489,#17490,#17491,#17492,#17493,#17494,#17495,
#17496,#17497,#17498,#17499,#17500,#17501,#17502,#17503,#17504,#17505,#17506,
#17507,#17508,#17509,#17510,#17511,#17512,#17513,#17514,#17515,#17516,#17517,
#17518,#17519,#17520,#17521,#17522,#17523,#17524,#17525,#17526,#17527,#17528,
#17529,#17530,#17531,#17532,#17533,#17534,#17535,#17536,#17537,#17538,#17539,
#17540,#17541,#17542,#17543,#17544,#17545,#17546,#17547,#17548,#17549,#17550,
#17551,#17552,#17553,#17554,#17555,#17556,#17557,#17558,#17559,#17560,#17561,
#17562,#17563,#17564,#17565,#17566,#17567,#17568,#17569,#17570,#17571,#17572,
#17573,#17574,#17575,#17576,#17577,#17578,#17579,#17580,#17581,#17582,#17583,
#17584,#17585,#17586,#17587,#17588,#17589,#17590,#17591,#17592,#17593,#17594,
#17595,#17596,#17597,#17598,#17599,#17600,#17601,#17602,#17603,#17604,#17605,
#17606,#17607,#17608,#17609,#17610,#17611,#17612,#17613,#17614,#17615,#17616,
#17617,#17618,#17619,#17620,#17621,#17622,#17623,#17624,#17625,#17626,#17627,
#17628,#17629,#17630,#17631,#17632,#17633,#17634,#17635,#17636,#17637,#17638,
#17639,#17640,#17641,#17642,#17643,#17644,#17645,#17646,#17647,#17648,#17649,
#17650,#17651,#17652,#17653,#17654),.UNSPECIFIED.,.F.,.F.,(4,3,3,3,3,3,
3,3,3,3,3,3,3,3,3,3,3,3,3,3,3,3,3,3,3,3,3,3,3,3,3,3,3,3,3,3,3,3,3,3,3,3,
3,3,3,3,3,3,3,3,3,3,3,3,3,3,3,3,3,3,3,3,3,3,3,3,3,3,3,4),(-22.942486341331,
-22.8476150237653,-22.7528740368907,-22.654554796563,-22.5599818052167,
-22.4654400589883,-22.3709025735227,-22.2763423756061,-22.1816765680522,
-22.086947869278,-21.9920723020764,-21.9663201142693,-21.8710869373234,
-21.7759851045722,-21.6809850499115,-21.5860534744897,-21.491156418622,
-21.3962673227029,-21.3013596415636,-21.2063476758215,-21.1112773361922,
-21.01605305685,-20.9678510181662,-20.8726178409093,-20.7775160078446,-20.6825159528683,
-20.5875843771288,-20.4926873209421,-20.3977982247034,-20.3028905432446,
-20.2078785771841,-20.1128082372368,-20.0175839575806,-19.969381922063,
-19.8741487462001,-19.7790469145306,-19.6840468609492,-19.5891152865979,
-19.494218231795,-19.3993291369339,-19.3044214568442,-19.2094094921331,
-19.1143391535259,-19.0191148751815,-18.9709128259599,-18.8756796482935,
-18.7805778148294,-18.6855777594645,-18.5906461833534,-18.4957491268059,
-18.4008600302176,-18.3059523484206,-18.2109403820415,-18.115870041786,
-18.0206457618408,-17.9724437298567,-17.877210550068,-17.7821087144555,
-17.6871086569185,-17.5921770786102,-17.4972800198508,-17.4023909210385,
-17.3074832370082,-17.2124712683962,-17.1174009259047,-17.0221766437404,
-16.9739746337536,-16.8599445077596,-16.7472092989469,-16.6593010346695),
 .UNSPECIFIED.);
#163=B_SPLINE_CURVE_WITH_KNOTS('',3,(#17656,#17657,#17658,#17659,#17660,
#17661,#17662,#17663,#17664,#17665,#17666,#17667,#17668,#17669,#17670,#17671,
#17672,#17673,#17674,#17675,#17676,#17677,#17678,#17679,#17680,#17681,#17682,
#17683,#17684,#17685,#17686,#17687,#17688,#17689,#17690,#17691,#17692,#17693,
#17694,#17695,#17696,#17697,#17698,#17699,#17700,#17701,#17702,#17703,#17704,
#17705,#17706,#17707,#17708,#17709,#17710,#17711,#17712,#17713,#17714,#17715,
#17716,#17717,#17718,#17719,#17720,#17721,#17722,#17723,#17724,#17725,#17726,
#17727,#17728,#17729,#17730,#17731,#17732,#17733,#17734,#17735,#17736,#17737,
#17738,#17739,#17740,#17741,#17742,#17743,#17744,#17745,#17746,#17747,#17748,
#17749,#17750,#17751,#17752,#17753,#17754,#17755,#17756,#17757,#17758,#17759,
#17760,#17761,#17762,#17763,#17764,#17765,#17766,#17767,#17768,#17769,#17770,
#17771,#17772,#17773,#17774,#17775,#17776,#17777,#17778,#17779,#17780,#17781,
#17782,#17783,#17784,#17785,#17786,#17787,#17788,#17789,#17790,#17791,#17792,
#17793,#17794,#17795,#17796,#17797,#17798,#17799,#17800,#17801,#17802,#17803,
#17804,#17805,#17806,#17807,#17808,#17809,#17810,#17811,#17812,#17813,#17814,
#17815,#17816,#17817,#17818,#17819,#17820,#17821,#17822,#17823,#17824,#17825,
#17826,#17827,#17828,#17829,#17830,#17831,#17832,#17833,#17834,#17835,#17836,
#17837,#17838,#17839,#17840,#17841,#17842,#17843,#17844,#17845,#17846,#17847,
#17848,#17849,#17850,#17851,#17852,#17853,#17854,#17855,#17856,#17857,#17858,
#17859,#17860,#17861,#17862,#17863,#17864,#17865,#17866),.UNSPECIFIED.,
 .F.,.F.,(4,3,3,3,3,3,3,3,3,3,3,3,3,3,3,3,3,3,3,3,3,3,3,3,3,3,3,3,3,3,3,
3,3,3,3,3,3,3,3,3,3,3,3,3,3,3,3,3,3,3,3,3,3,3,3,3,3,3,3,3,3,3,3,3,3,3,3,
3,3,3,4),(-16.6593010344898,-16.564737636787,-16.4701999869256,-16.3756611684414,
-16.281094271255,-16.1864152516017,-16.0916687801366,-15.9967719690251,
-15.9755055376504,-15.8802723505797,-15.7851705077762,-15.6901704431488,
-15.5952388579267,-15.5003417923652,-15.4054526868703,-15.3105449962849,
-15.2155330213483,-15.1204626726541,-15.0252383845358,-14.9770364415473,
-14.8818032426871,-14.7867013878369,-14.691701310925,-14.5967697131203,
-14.5018726347967,-14.406983516377,-14.3120758127208,-14.2170638245753,
-14.121993462574,-14.0267691611285,-13.9785673454441,-13.8833342646743,
-13.7882325281889,-13.6932325697527,-13.5983010900969,-13.5034041296754,
-13.4085151287669,-13.3136075420861,-13.2185956693933,-13.123525422151,
-13.028301233267,-12.980098249341,-12.8848649504053,-12.7897629962807,-12.6947628210174,
-12.5998311266244,-12.5049339528391,-12.4100447401951,-12.3151369436636,
-12.2201248652386,-12.1250544142982,-12.0298300268517,-11.9816291532378,
-11.8863958246192,-11.7912938383692,-11.6962936286177,-11.6013618964074,
-11.5064646827596,-11.411575428271,-11.3166675879739,-11.2216554631697,
-11.1265849642967,-11.0313605270005,-10.9831600571347,-10.88673590317,-10.7904530193315,
-10.6942866233368,-10.5982246406379,-10.5022232640172,-10.4062551289695,
-10.3761157273101),.UNSPECIFIED.);
#164=B_SPLINE_CURVE_WITH_KNOTS('',3,(#17868,#17869,#17870,#17871,#17872,
#17873,#17874,#17875,#17876,#17877,#17878,#17879,#17880,#17881,#17882,#17883,
#17884,#17885,#17886,#17887,#17888,#17889,#17890,#17891,#17892,#17893,#17894,
#17895,#17896,#17897,#17898,#17899,#17900,#17901,#17902,#17903,#17904,#17905,
#17906,#17907,#17908,#17909,#17910,#17911,#17912,#17913,#17914,#17915,#17916,
#17917,#17918,#17919,#17920,#17921,#17922,#17923,#17924,#17925,#17926,#17927,
#17928,#17929,#17930,#17931,#17932,#17933,#17934,#17935,#17936,#17937,#17938,
#17939,#17940,#17941,#17942,#17943,#17944,#17945,#17946,#17947,#17948,#17949,
#17950,#17951,#17952,#17953,#17954,#17955,#17956,#17957,#17958,#17959,#17960,
#17961,#17962,#17963,#17964,#17965,#17966,#17967,#17968,#17969,#17970,#17971,
#17972,#17973,#17974,#17975,#17976,#17977,#17978,#17979,#17980,#17981,#17982,
#17983,#17984,#17985,#17986,#17987,#17988,#17989,#17990,#17991,#17992,#17993,
#17994,#17995,#17996,#17997,#17998,#17999,#18000,#18001,#18002,#18003,#18004,
#18005,#18006,#18007,#18008,#18009,#18010,#18011,#18012,#18013,#18014,#18015,
#18016,#18017,#18018,#18019,#18020,#18021,#18022,#18023,#18024,#18025,#18026,
#18027,#18028,#18029,#18030,#18031,#18032,#18033,#18034,#18035,#18036,#18037,
#18038,#18039,#18040,#18041,#18042,#18043,#18044,#18045,#18046,#18047,#18048,
#18049,#18050,#18051,#18052,#18053,#18054,#18055,#18056,#18057,#18058,#18059,
#18060,#18061,#18062,#18063,#18064,#18065,#18066,#18067,#18068,#18069,#18070,
#18071,#18072,#18073,#18074,#18075),.UNSPECIFIED.,.F.,.F.,(4,3,3,3,3,3,
3,3,3,3,3,3,3,3,3,3,3,3,3,3,3,3,3,3,3,3,3,3,3,3,3,3,3,3,3,3,3,3,3,3,3,3,
3,3,3,3,3,3,3,3,3,3,3,3,3,3,3,3,3,3,3,3,3,3,3,3,3,3,3,4),(-10.3761157271004,
-10.2705941373572,-10.1646889495115,-10.0582504347146,-9.98469096103152,
-9.88945640702594,-9.79435320216464,-9.69935178211476,-9.60441885682833,
-9.50952046120628,-9.41463003723521,-9.31972104134926,-9.22470778890569,
-9.12963617659603,-9.03441065868313,-8.98622186492837,-8.89098782101992,
-8.79588510357613,-8.70088414794559,-8.60595165136803,-8.51105366220213,
-8.41616362207912,-8.32125498705802,-8.22624205877446,-8.13117075025981,
-8.03594550181371,-7.98775276882521,-7.89252776793133,-7.79743412964125,
-7.70244227657632,-7.60751887932103,-7.51262998407767,-7.41774902126599,
-7.32284943571592,-7.22784545952439,-7.13278306108336,-7.03756657027433,
-6.98928367272206,-6.8940356024099,-6.79891891365831,-6.70390405982608,
-6.6089578300529,-6.51404621497145,-6.41914267241841,-6.32422067476947,
-6.22919467579913,-6.13411044309066,-6.03887262308352,-5.99081457661891,
-5.89557879637505,-5.80047419276722,-5.70547120593688,-5.61053647357262,
-5.51563612290772,-5.42074359936495,-5.32583236269098,-5.2308166714205,
-5.13574250420529,-5.04051427801215,-4.99234548051576,-4.89835863124272,
-4.80450220502569,-4.71075270953591,-4.6170611967346,-4.52339979495569,
-4.4297406695336,-4.33600307487336,-4.24222301883573,-4.14830479318644,
-4.09293042036874),.UNSPECIFIED.);
#165=B_SPLINE_CURVE_WITH_KNOTS('',3,(#18077,#18078,#18079,#18080,#18081,
#18082,#18083,#18084,#18085,#18086,#18087,#18088,#18089,#18090,#18091,#18092,
#18093,#18094,#18095,#18096,#18097,#18098,#18099,#18100,#18101,#18102,#18103,
#18104,#18105,#18106,#18107,#18108,#18109,#18110,#18111,#18112,#18113,#18114,
#18115,#18116,#18117,#18118,#18119,#18120,#18121,#18122,#18123,#18124,#18125,
#18126,#18127,#18128,#18129,#18130,#18131,#18132,#18133,#18134,#18135,#18136,
#18137,#18138,#18139,#18140,#18141,#18142,#18143),.UNSPECIFIED.,.F.,.F.,
(4,3,3,3,3,3,3,3,3,3,3,3,3,3,3,3,3,3,3,3,3,3,4),(-4.09293042013064,-3.99387638441261,
-3.89848924053276,-3.80323366876535,-3.70808031071437,-3.61299671406167,
-3.51794849283965,-3.4229092732933,-3.32785269704006,-3.23269459728435,
-3.13747948209115,-3.04211393352018,-2.99540728830946,-2.90121559909012,
-2.80715256457177,-2.7131934050502,-2.61929079818114,-2.52541705715098,
-2.43154452959619,-2.3375858729544,-2.24358441504212,-2.14942728251797,
-2.06864179208665),.UNSPECIFIED.);
#166=B_SPLINE_CURVE_WITH_KNOTS('',3,(#18144,#18145,#18146,#18147),
 .UNSPECIFIED.,.F.,.F.,(4,4),(-0.0553882262895087,0.),.UNSPECIFIED.);
#167=B_SPLINE_CURVE_WITH_KNOTS('',3,(#18150,#18151,#18152,#18153,#18154,
#18155,#18156,#18157,#18158,#18159,#18160,#18161,#18162,#18163,#18164,#18165,
#18166,#18167,#18168,#18169,#18170,#18171,#18172,#18173,#18174,#18175,#18176,
#18177,#18178,#18179,#18180,#18181,#18182,#18183,#18184,#18185,#18186,#18187,
#18188,#18189,#18190,#18191,#18192,#18193,#18194,#18195,#18196,#18197,#18198,
#18199,#18200,#18201,#18202,#18203,#18204,#18205,#18206,#18207,#18208,#18209,
#18210,#18211,#18212,#18213,#18214,#18215,#18216,#18217,#18218,#18219,#18220,
#18221,#18222,#18223,#18224,#18225,#18226,#18227,#18228,#18229,#18230,#18231,
#18232,#18233,#18234,#18235,#18236,#18237,#18238,#18239,#18240,#18241,#18242,
#18243,#18244,#18245,#18246,#18247,#18248,#18249,#18250,#18251,#18252,#18253,
#18254,#18255,#18256,#18257,#18258,#18259,#18260,#18261,#18262,#18263,#18264,
#18265),.UNSPECIFIED.,.F.,.F.,(4,2,2,2,2,2,2,2,2,2,2,2,2,2,2,2,2,2,2,2,
2,2,2,2,2,2,2,2,2,2,2,2,2,2,2,2,2,2,2,2,2,2,2,2,2,2,2,2,2,2,2,2,2,2,2,2,
2,4),(0.00393879945399954,0.0559409183588363,0.0876972450261331,0.0976998745863839,
0.104613482977544,0.11166922140705,0.122434269394492,0.179131978558203,
0.210354110329382,0.216991056490599,0.221067292598832,0.225123889707987,
0.231759555487665,0.261970513582465,0.302284660286109,0.325250128468266,
0.334362352316371,0.341123207111329,0.348441239547103,0.360557058247711,
0.406262420026052,0.434559681824057,0.450020364199544,0.45554426629461,
0.459375550971286,0.463708309240328,0.471808681292075,0.502901677971822,
0.532030064578008,0.561159612056953,0.570874880434037,0.577678874304539,
0.583863827512892,0.593949037105209,0.625063658570325,0.661425587696632,
0.686059983943537,0.69235077777511,0.696301740721866,0.700359261123135,
0.707095866720147,0.743137023178607,0.777207886595307,0.800425351770403,
0.809544959571145,0.81628096716921,0.823541975926377,0.835486602649266,
0.883868277417384,0.910317304618082,0.925173636210761,0.930612516942996,
0.934428206452051,0.938813273964349,0.946886601823189,0.978921547363476,
1.00811846899774,1.00824602608924),.UNSPECIFIED.);
#168=B_SPLINE_CURVE_WITH_KNOTS('',3,(#18269,#18270,#18271,#18272,#18273,
#18274,#18275,#18276,#18277,#18278,#18279,#18280,#18281,#18282,#18283,#18284,
#18285,#18286,#18287,#18288,#18289,#18290,#18291,#18292,#18293,#18294,#18295,
#18296,#18297,#18298,#18299),.UNSPECIFIED.,.F.,.F.,(4,3,3,3,3,3,3,3,3,3,
4),(72.2566310328722,72.358764204796,72.4649147790848,72.5667140368636,
72.6684219268066,72.7700668437146,72.8716771107077,72.973313692877,73.0749655043999,
73.1767014162145,73.207968799106),.UNSPECIFIED.);
#169=B_SPLINE_CURVE_WITH_KNOTS('',3,(#18300,#18301,#18302,#18303,#18304,
#18305,#18306,#18307,#18308,#18309,#18310,#18311,#18312,#18313,#18314,#18315,
#18316,#18317,#18318,#18319,#18320,#18321,#18322,#18323,#18324,#18325,#18326,
#18327,#18328,#18329,#18330,#18331,#18332,#18333,#18334,#18335,#18336,#18337,
#18338,#18339,#18340,#18341,#18342,#18343,#18344,#18345,#18346,#18347,#18348,
#18349,#18350,#18351,#18352,#18353,#18354,#18355,#18356,#18357,#18358,#18359,
#18360,#18361,#18362,#18363,#18364,#18365,#18366),.UNSPECIFIED.,.F.,.F.,
(4,3,3,3,3,3,3,3,3,3,3,3,3,3,3,3,3,3,3,3,3,3,4),(70.2101735890481,70.2125615107965,
70.3130249063546,70.413345018932,70.5135515181276,70.6136960857837,70.7138100121525,
70.813924548465,70.9141425502769,71.0144104356228,71.1148647428971,71.2110306068997,
71.3108636815101,71.4105510300929,71.5104196142066,71.6099303183161,71.7094110548427,
71.8088939006647,71.9090453512492,72.0086912716984,72.1090954873506,72.2094997030028,
72.2566310325651),.UNSPECIFIED.);
#170=B_SPLINE_CURVE_WITH_KNOTS('',3,(#18639,#18640,#18641,#18642,#18643,
#18644,#18645,#18646,#18647,#18648,#18649,#18650,#18651,#18652,#18653,#18654,
#18655,#18656,#18657,#18658,#18659,#18660,#18661,#18662,#18663,#18664,#18665,
#18666,#18667,#18668,#18669,#18670,#18671,#18672,#18673,#18674,#18675,#18676,
#18677,#18678,#18679,#18680,#18681,#18682,#18683,#18684,#18685,#18686,#18687,
#18688,#18689,#18690,#18691,#18692,#18693,#18694,#18695,#18696,#18697,#18698,
#18699,#18700,#18701,#18702,#18703,#18704,#18705,#18706,#18707,#18708,#18709,
#18710,#18711,#18712,#18713,#18714,#18715,#18716,#18717,#18718,#18719,#18720,
#18721,#18722,#18723,#18724,#18725,#18726,#18727,#18728,#18729,#18730,#18731,
#18732),.UNSPECIFIED.,.F.,.F.,(4,3,3,3,3,3,3,3,3,3,3,3,3,3,3,3,3,3,3,3,
3,3,3,3,3,3,3,3,3,3,3,4),(0.,0.0211515250929699,0.0503479224047965,0.0799219030506932,
0.107557403668628,0.112306557576265,0.116555306404556,0.145320497988993,
0.173988624024303,0.202002260365531,0.214552337294273,0.219717600821093,
0.223840641427237,0.251416480277754,0.27821193354047,0.301838152182752,
0.317677816946291,0.324502722029292,0.329013266588695,0.3558249978195,0.382923040397653,
0.405945422486999,0.417986286650722,0.424997553960968,0.429588563398635,
0.455730667603274,0.480731501813387,0.487617912295433,0.494575057586814,
0.519602150133133,0.544372461559281,0.555272788399386),.UNSPECIFIED.);
#171=B_SPLINE_CURVE_WITH_KNOTS('',3,(#18733,#18734,#18735,#18736,#18737,
#18738,#18739,#18740,#18741,#18742,#18743,#18744,#18745,#18746,#18747,#18748,
#18749,#18750,#18751,#18752,#18753,#18754,#18755,#18756,#18757,#18758,#18759,
#18760,#18761,#18762,#18763,#18764,#18765,#18766,#18767,#18768,#18769,#18770,
#18771,#18772,#18773,#18774,#18775,#18776,#18777,#18778,#18779,#18780,#18781,
#18782,#18783,#18784,#18785,#18786,#18787,#18788,#18789,#18790,#18791,#18792,
#18793,#18794,#18795,#18796,#18797,#18798,#18799,#18800,#18801,#18802,#18803,
#18804,#18805,#18806,#18807,#18808,#18809,#18810,#18811,#18812,#18813,#18814,
#18815,#18816,#18817,#18818,#18819,#18820),.UNSPECIFIED.,.F.,.F.,(4,3,3,
3,3,3,3,3,3,3,3,3,3,3,3,3,3,3,3,3,3,3,3,3,3,3,3,3,3,4),(-0.555272788399294,
-0.537998135235996,-0.513195393070161,-0.498873792586909,-0.492711473426493,
-0.487860772154604,-0.462111258555471,-0.439632717483603,-0.428896962458095,
-0.424839679808983,-0.398150918614796,-0.371100690967241,-0.344106017964823,
-0.328877992852833,-0.32454079642153,-0.296627170519809,-0.282566212897678,
-0.255355425971256,-0.228144639044835,-0.22107377310443,-0.216711755873243,
-0.188903627081518,-0.160211248623033,-0.131518870164547,-0.114266101543064,
-0.109583468965517,-0.0801051988652096,-0.0505616879768782,-0.0216028909587886,
0.),.UNSPECIFIED.);
#172=B_SPLINE_CURVE_WITH_KNOTS('',3,(#18822,#18823,#18824,#18825,#18826,
#18827,#18828,#18829,#18830,#18831,#18832,#18833,#18834,#18835,#18836,#18837,
#18838,#18839,#18840,#18841,#18842,#18843,#18844,#18845,#18846,#18847,#18848,
#18849,#18850,#18851,#18852,#18853,#18854,#18855,#18856,#18857,#18858,#18859,
#18860,#18861,#18862,#18863,#18864,#18865,#18866,#18867,#18868,#18869,#18870,
#18871,#18872,#18873,#18874,#18875,#18876,#18877,#18878,#18879,#18880,#18881,
#18882,#18883,#18884,#18885,#18886,#18887,#18888,#18889,#18890,#18891,#18892,
#18893,#18894,#18895,#18896,#18897,#18898,#18899,#18900,#18901,#18902,#18903,
#18904,#18905,#18906,#18907,#18908,#18909,#18910,#18911,#18912,#18913,#18914,
#18915),.UNSPECIFIED.,.F.,.F.,(4,3,3,3,3,3,3,3,3,3,3,3,3,3,3,3,3,3,3,3,
3,3,3,3,3,3,3,3,3,3,3,4),(-0.547176240833745,-0.531693267680898,-0.502322832918406,
-0.486713217316651,-0.479140335200163,-0.472082504350801,-0.44303092644762,
-0.419220841452745,-0.408408989901447,-0.402036527603242,-0.397475090495561,
-0.369198891406047,-0.341216278386301,-0.314050980020528,-0.297439627272632,
-0.29142916710721,-0.264617850724684,-0.252568983290324,-0.224809796970208,
-0.197050610650091,-0.192202487211981,-0.188184385718677,-0.161573441667812,
-0.135063262774347,-0.108787981383092,-0.0997862447992211,-0.0945269665459779,
-0.0902272799954171,-0.064692601081796,-0.039564031532061,-0.0152229077075751,
0.),.UNSPECIFIED.);
#173=B_SPLINE_CURVE_WITH_KNOTS('',3,(#19189,#19190,#19191,#19192,#19193,
#19194,#19195,#19196,#19197,#19198,#19199,#19200,#19201,#19202,#19203,#19204,
#19205,#19206,#19207,#19208,#19209,#19210,#19211,#19212,#19213,#19214,#19215,
#19216,#19217,#19218,#19219,#19220,#19221,#19222,#19223,#19224,#19225,#19226,
#19227,#19228,#19229,#19230,#19231,#19232,#19233,#19234,#19235,#19236,#19237,
#19238,#19239,#19240,#19241,#19242,#19243,#19244,#19245,#19246,#19247,#19248,
#19249,#19250,#19251,#19252,#19253,#19254,#19255,#19256,#19257,#19258,#19259,
#19260,#19261,#19262,#19263,#19264,#19265,#19266,#19267,#19268,#19269,#19270,
#19271,#19272,#19273,#19274,#19275,#19276,#19277,#19278,#19279),
 .UNSPECIFIED.,.F.,.F.,(4,3,3,3,3,3,3,3,3,3,3,3,3,3,3,3,3,3,3,3,3,3,3,3,
3,3,3,3,3,3,4),(0.,0.0172144967118733,0.041750612664055,0.0670931170711941,
0.0923753317934749,0.0966923746148899,0.122587060977129,0.149199398849806,
0.175811736722484,0.187831472308839,0.191843178428869,0.196232750464077,
0.223664672674057,0.251007710322057,0.271753036768803,0.289315058119197,
0.293959260700982,0.29839462330624,0.326041543022183,0.353688462738127,
0.37857057719275,0.391580430417787,0.398055686999867,0.403828921411263,
0.433238481825865,0.462648042240467,0.472327168294413,0.47934658435098,
0.508876613490308,0.538109240394632,0.55274537837511),.UNSPECIFIED.);
#174=B_SPLINE_CURVE_WITH_KNOTS('',3,(#19280,#19281,#19282,#19283),
 .UNSPECIFIED.,.F.,.F.,(4,4),(0.,0.0136660632777819),.UNSPECIFIED.);
#179=SHAPE_REPRESENTATION_RELATIONSHIP('SRR','None',#19479,#187);
#187=ADVANCED_BREP_SHAPE_REPRESENTATION('',(#203),#19439);
#195=STYLED_ITEM('',(#19525),#203);
#203=MANIFOLD_SOLID_BREP('Body1',#2022);
#214=FACE_BOUND('',#439,.T.);
#215=FACE_BOUND('',#445,.T.);
#247=PLANE('',#2213);
#248=PLANE('',#2214);
#249=PLANE('',#2218);
#250=PLANE('',#2219);
#325=FACE_OUTER_BOUND('',#428,.T.);
#326=FACE_OUTER_BOUND('',#429,.T.);
#327=FACE_OUTER_BOUND('',#430,.T.);
#328=FACE_OUTER_BOUND('',#431,.T.);
#329=FACE_OUTER_BOUND('',#432,.T.);
#330=FACE_OUTER_BOUND('',#433,.T.);
#331=FACE_OUTER_BOUND('',#434,.T.);
#332=FACE_OUTER_BOUND('',#435,.T.);
#333=FACE_OUTER_BOUND('',#436,.T.);
#334=FACE_OUTER_BOUND('',#437,.T.);
#335=FACE_OUTER_BOUND('',#438,.T.);
#336=FACE_OUTER_BOUND('',#440,.T.);
#337=FACE_OUTER_BOUND('',#441,.T.);
#338=FACE_OUTER_BOUND('',#442,.T.);
#339=FACE_OUTER_BOUND('',#443,.T.);
#340=FACE_OUTER_BOUND('',#444,.T.);
#341=FACE_OUTER_BOUND('',#446,.T.);
#342=FACE_OUTER_BOUND('',#447,.T.);
#343=FACE_OUTER_BOUND('',#448,.T.);
#428=EDGE_LOOP('',(#1609,#1610,#1611,#1612));
#429=EDGE_LOOP('',(#1613,#1614,#1615,#1616,#1617));
#430=EDGE_LOOP('',(#1618,#1619,#1620,#1621,#1622));
#431=EDGE_LOOP('',(#1623,#1624,#1625,#1626,#1627,#1628));
#432=EDGE_LOOP('',(#1629,#1630,#1631,#1632,#1633));
#433=EDGE_LOOP('',(#1634,#1635,#1636,#1637,#1638));
#434=EDGE_LOOP('',(#1639,#1640,#1641,#1642,#1643));
#435=EDGE_LOOP('',(#1644,#1645,#1646,#1647,#1648));
#436=EDGE_LOOP('',(#1649,#1650,#1651,#1652,#1653,#1654));
#437=EDGE_LOOP('',(#1655,#1656,#1657,#1658,#1659,#1660));
#438=EDGE_LOOP('',(#1661));
#439=EDGE_LOOP('',(#1662,#1663,#1664,#1665,#1666,#1667,#1668,#1669,#1670,
#1671,#1672,#1673,#1674,#1675,#1676,#1677,#1678,#1679,#1680,#1681,#1682,
#1683,#1684,#1685,#1686));
#440=EDGE_LOOP('',(#1687,#1688,#1689,#1690,#1691));
#441=EDGE_LOOP('',(#1692,#1693,#1694,#1695,#1696,#1697,#1698,#1699,#1700,
#1701,#1702,#1703,#1704,#1705,#1706,#1707,#1708,#1709,#1710,#1711,#1712,
#1713,#1714,#1715,#1716,#1717,#1718,#1719,#1720,#1721,#1722));
#442=EDGE_LOOP('',(#1723,#1724,#1725,#1726));
#443=EDGE_LOOP('',(#1727,#1728,#1729,#1730,#1731,#1732,#1733,#1734,#1735,
#1736,#1737,#1738,#1739,#1740,#1741,#1742,#1743,#1744,#1745,#1746,#1747,
#1748,#1749,#1750,#1751,#1752,#1753,#1754,#1755,#1756,#1757,#1758));
#444=EDGE_LOOP('',(#1759));
#445=EDGE_LOOP('',(#1760));
#446=EDGE_LOOP('',(#1761,#1762,#1763,#1764));
#447=EDGE_LOOP('',(#1765));
#448=EDGE_LOOP('',(#1766,#1767,#1768,#1769,#1770));
#547=LINE('',#10942,#674);
#548=LINE('',#11114,#675);
#549=LINE('',#11481,#676);
#550=LINE('',#11844,#677);
#551=LINE('',#12104,#678);
#552=LINE('',#12425,#679);
#553=LINE('',#12784,#680);
#554=LINE('',#13149,#681);
#555=LINE('',#13404,#682);
#556=LINE('',#13736,#683);
#557=LINE('',#19290,#684);
#674=VECTOR('',#2499,2.37175);
#675=VECTOR('',#2504,2.37175);
#676=VECTOR('',#2507,2.37175);
#677=VECTOR('',#2510,2.37175);
#678=VECTOR('',#2513,2.37175);
#679=VECTOR('',#2516,2.37175);
#680=VECTOR('',#2519,2.37175);
#681=VECTOR('',#2522,2.37175);
#682=VECTOR('',#2525,2.37175);
#683=VECTOR('',#2528,2.37175);
#684=VECTOR('',#2551,4.);
#759=CIRCLE('',#2197,2.37175);
#760=CIRCLE('',#2208,2.942);
#761=CIRCLE('',#2209,2.942);
#762=CIRCLE('',#2210,2.942);
#763=CIRCLE('',#2212,2.37175);
#764=CIRCLE('',#2215,4.);
#765=CIRCLE('',#2217,4.);
#890=VERTEX_POINT('',#10940);
#891=VERTEX_POINT('',#10941);
#892=VERTEX_POINT('',#10943);
#893=VERTEX_POINT('',#11047);
#894=VERTEX_POINT('',#11112);
#895=VERTEX_POINT('',#11113);
#896=VERTEX_POINT('',#11115);
#897=VERTEX_POINT('',#11479);
#898=VERTEX_POINT('',#11480);
#899=VERTEX_POINT('',#11654);
#900=VERTEX_POINT('',#11842);
#901=VERTEX_POINT('',#11843);
#902=VERTEX_POINT('',#11845);
#903=VERTEX_POINT('',#12028);
#904=VERTEX_POINT('',#12102);
#905=VERTEX_POINT('',#12103);
#906=VERTEX_POINT('',#12281);
#907=VERTEX_POINT('',#12423);
#908=VERTEX_POINT('',#12424);
#909=VERTEX_POINT('',#12426);
#910=VERTEX_POINT('',#12782);
#911=VERTEX_POINT('',#12783);
#912=VERTEX_POINT('',#12965);
#913=VERTEX_POINT('',#13147);
#914=VERTEX_POINT('',#13148);
#915=VERTEX_POINT('',#13150);
#916=VERTEX_POINT('',#13402);
#917=VERTEX_POINT('',#13403);
#918=VERTEX_POINT('',#13405);
#919=VERTEX_POINT('',#13542);
#920=VERTEX_POINT('',#13734);
#921=VERTEX_POINT('',#13735);
#922=VERTEX_POINT('',#13737);
#923=VERTEX_POINT('',#13929);
#924=VERTEX_POINT('',#14116);
#925=VERTEX_POINT('',#14118);
#926=VERTEX_POINT('',#14119);
#927=VERTEX_POINT('',#14121);
#928=VERTEX_POINT('',#14127);
#929=VERTEX_POINT('',#14336);
#930=VERTEX_POINT('',#14545);
#931=VERTEX_POINT('',#14754);
#932=VERTEX_POINT('',#14966);
#933=VERTEX_POINT('',#15175);
#934=VERTEX_POINT('',#15384);
#935=VERTEX_POINT('',#15593);
#936=VERTEX_POINT('',#15802);
#937=VERTEX_POINT('',#16011);
#938=VERTEX_POINT('',#16181);
#939=VERTEX_POINT('',#16183);
#940=VERTEX_POINT('',#16192);
#941=VERTEX_POINT('',#16401);
#942=VERTEX_POINT('',#16610);
#943=VERTEX_POINT('',#16816);
#944=VERTEX_POINT('',#17025);
#945=VERTEX_POINT('',#17234);
#946=VERTEX_POINT('',#17446);
#947=VERTEX_POINT('',#17655);
#948=VERTEX_POINT('',#17867);
#949=VERTEX_POINT('',#18076);
#950=VERTEX_POINT('',#18149);
#951=VERTEX_POINT('',#18266);
#952=VERTEX_POINT('',#18268);
#953=VERTEX_POINT('',#19188);
#954=VERTEX_POINT('',#19285);
#955=VERTEX_POINT('',#19288);
#1153=EDGE_CURVE('',#890,#891,#547,.T.);
#1154=EDGE_CURVE('',#892,#890,#112,.T.);
#1155=EDGE_CURVE('',#893,#892,#759,.T.);
#1156=EDGE_CURVE('',#893,#891,#113,.T.);
#1157=EDGE_CURVE('',#894,#895,#548,.T.);
#1158=EDGE_CURVE('',#896,#894,#114,.F.);
#1159=EDGE_CURVE('',#890,#896,#115,.T.);
#1160=EDGE_CURVE('',#891,#895,#116,.T.);
#1161=EDGE_CURVE('',#897,#898,#549,.T.);
#1162=EDGE_CURVE('',#894,#897,#117,.F.);
#1163=EDGE_CURVE('',#895,#899,#118,.T.);
#1164=EDGE_CURVE('',#899,#898,#119,.T.);
#1165=EDGE_CURVE('',#900,#901,#550,.T.);
#1166=EDGE_CURVE('',#902,#900,#120,.F.);
#1167=EDGE_CURVE('',#897,#902,#121,.F.);
#1168=EDGE_CURVE('',#898,#903,#122,.T.);
#1169=EDGE_CURVE('',#903,#901,#123,.T.);
#1170=EDGE_CURVE('',#904,#905,#551,.T.);
#1171=EDGE_CURVE('',#900,#904,#124,.F.);
#1172=EDGE_CURVE('',#901,#906,#125,.T.);
#1173=EDGE_CURVE('',#906,#905,#126,.T.);
#1174=EDGE_CURVE('',#907,#908,#552,.T.);
#1175=EDGE_CURVE('',#909,#907,#127,.F.);
#1176=EDGE_CURVE('',#904,#909,#128,.F.);
#1177=EDGE_CURVE('',#905,#908,#129,.T.);
#1178=EDGE_CURVE('',#910,#911,#553,.T.);
#1179=EDGE_CURVE('',#907,#910,#130,.F.);
#1180=EDGE_CURVE('',#908,#912,#131,.T.);
#1181=EDGE_CURVE('',#912,#911,#132,.T.);
#1182=EDGE_CURVE('',#913,#914,#554,.T.);
#1183=EDGE_CURVE('',#915,#913,#133,.T.);
#1184=EDGE_CURVE('',#910,#915,#134,.F.);
#1185=EDGE_CURVE('',#911,#914,#135,.T.);
#1186=EDGE_CURVE('',#916,#917,#555,.T.);
#1187=EDGE_CURVE('',#918,#916,#136,.T.);
#1188=EDGE_CURVE('',#913,#918,#137,.T.);
#1189=EDGE_CURVE('',#914,#919,#138,.T.);
#1190=EDGE_CURVE('',#919,#917,#139,.T.);
#1191=EDGE_CURVE('',#920,#921,#556,.T.);
#1192=EDGE_CURVE('',#922,#920,#140,.T.);
#1193=EDGE_CURVE('',#916,#922,#141,.T.);
#1194=EDGE_CURVE('',#917,#923,#142,.T.);
#1195=EDGE_CURVE('',#923,#921,#143,.F.);
#1196=EDGE_CURVE('',#924,#924,#760,.F.);
#1197=EDGE_CURVE('',#925,#926,#761,.T.);
#1198=EDGE_CURVE('',#926,#927,#144,.T.);
#1199=EDGE_CURVE('',#927,#928,#145,.T.);
#1200=EDGE_CURVE('',#928,#929,#146,.T.);
#1201=EDGE_CURVE('',#929,#930,#147,.T.);
#1202=EDGE_CURVE('',#930,#931,#148,.T.);
#1203=EDGE_CURVE('',#931,#932,#149,.T.);
#1204=EDGE_CURVE('',#932,#933,#150,.T.);
#1205=EDGE_CURVE('',#933,#934,#151,.T.);
#1206=EDGE_CURVE('',#934,#935,#152,.T.);
#1207=EDGE_CURVE('',#935,#936,#153,.T.);
#1208=EDGE_CURVE('',#936,#937,#154,.T.);
#1209=EDGE_CURVE('',#938,#937,#762,.T.);
#1210=EDGE_CURVE('',#938,#939,#155,.T.);
#1211=EDGE_CURVE('',#939,#940,#156,.T.);
#1212=EDGE_CURVE('',#940,#941,#157,.T.);
#1213=EDGE_CURVE('',#941,#942,#158,.T.);
#1214=EDGE_CURVE('',#942,#943,#159,.T.);
#1215=EDGE_CURVE('',#943,#944,#160,.T.);
#1216=EDGE_CURVE('',#944,#945,#161,.T.);
#1217=EDGE_CURVE('',#945,#946,#162,.T.);
#1218=EDGE_CURVE('',#946,#947,#163,.T.);
#1219=EDGE_CURVE('',#947,#948,#164,.T.);
#1220=EDGE_CURVE('',#948,#949,#165,.T.);
#1221=EDGE_CURVE('',#949,#925,#166,.T.);
#1222=EDGE_CURVE('',#921,#950,#167,.F.);
#1223=EDGE_CURVE('',#951,#950,#763,.T.);
#1224=EDGE_CURVE('',#952,#951,#168,.T.);
#1225=EDGE_CURVE('',#920,#952,#169,.T.);
#1226=EDGE_CURVE('',#937,#951,#170,.T.);
#1227=EDGE_CURVE('',#892,#926,#171,.T.);
#1228=EDGE_CURVE('',#925,#893,#172,.T.);
#1229=EDGE_CURVE('',#953,#938,#173,.T.);
#1230=EDGE_CURVE('',#950,#953,#174,.T.);
#1231=EDGE_CURVE('',#954,#954,#764,.T.);
#1232=EDGE_CURVE('',#955,#955,#765,.T.);
#1233=EDGE_CURVE('',#955,#954,#557,.T.);
#1609=ORIENTED_EDGE('',*,*,#1153,.F.);
#1610=ORIENTED_EDGE('',*,*,#1154,.F.);
#1611=ORIENTED_EDGE('',*,*,#1155,.F.);
#1612=ORIENTED_EDGE('',*,*,#1156,.T.);
#1613=ORIENTED_EDGE('',*,*,#1157,.F.);
#1614=ORIENTED_EDGE('',*,*,#1158,.F.);
#1615=ORIENTED_EDGE('',*,*,#1159,.F.);
#1616=ORIENTED_EDGE('',*,*,#1153,.T.);
#1617=ORIENTED_EDGE('',*,*,#1160,.T.);
#1618=ORIENTED_EDGE('',*,*,#1161,.F.);
#1619=ORIENTED_EDGE('',*,*,#1162,.F.);
#1620=ORIENTED_EDGE('',*,*,#1157,.T.);
#1621=ORIENTED_EDGE('',*,*,#1163,.T.);
#1622=ORIENTED_EDGE('',*,*,#1164,.T.);
#1623=ORIENTED_EDGE('',*,*,#1165,.F.);
#1624=ORIENTED_EDGE('',*,*,#1166,.F.);
#1625=ORIENTED_EDGE('',*,*,#1167,.F.);
#1626=ORIENTED_EDGE('',*,*,#1161,.T.);
#1627=ORIENTED_EDGE('',*,*,#1168,.T.);
#1628=ORIENTED_EDGE('',*,*,#1169,.T.);
#1629=ORIENTED_EDGE('',*,*,#1170,.F.);
#1630=ORIENTED_EDGE('',*,*,#1171,.F.);
#1631=ORIENTED_EDGE('',*,*,#1165,.T.);
#1632=ORIENTED_EDGE('',*,*,#1172,.T.);
#1633=ORIENTED_EDGE('',*,*,#1173,.T.);
#1634=ORIENTED_EDGE('',*,*,#1174,.F.);
#1635=ORIENTED_EDGE('',*,*,#1175,.F.);
#1636=ORIENTED_EDGE('',*,*,#1176,.F.);
#1637=ORIENTED_EDGE('',*,*,#1170,.T.);
#1638=ORIENTED_EDGE('',*,*,#1177,.T.);
#1639=ORIENTED_EDGE('',*,*,#1178,.F.);
#1640=ORIENTED_EDGE('',*,*,#1179,.F.);
#1641=ORIENTED_EDGE('',*,*,#1174,.T.);
#1642=ORIENTED_EDGE('',*,*,#1180,.T.);
#1643=ORIENTED_EDGE('',*,*,#1181,.T.);
#1644=ORIENTED_EDGE('',*,*,#1182,.F.);
#1645=ORIENTED_EDGE('',*,*,#1183,.F.);
#1646=ORIENTED_EDGE('',*,*,#1184,.F.);
#1647=ORIENTED_EDGE('',*,*,#1178,.T.);
#1648=ORIENTED_EDGE('',*,*,#1185,.T.);
#1649=ORIENTED_EDGE('',*,*,#1186,.F.);
#1650=ORIENTED_EDGE('',*,*,#1187,.F.);
#1651=ORIENTED_EDGE('',*,*,#1188,.F.);
#1652=ORIENTED_EDGE('',*,*,#1182,.T.);
#1653=ORIENTED_EDGE('',*,*,#1189,.T.);
#1654=ORIENTED_EDGE('',*,*,#1190,.T.);
#1655=ORIENTED_EDGE('',*,*,#1191,.F.);
#1656=ORIENTED_EDGE('',*,*,#1192,.F.);
#1657=ORIENTED_EDGE('',*,*,#1193,.F.);
#1658=ORIENTED_EDGE('',*,*,#1186,.T.);
#1659=ORIENTED_EDGE('',*,*,#1194,.T.);
#1660=ORIENTED_EDGE('',*,*,#1195,.T.);
#1661=ORIENTED_EDGE('',*,*,#1196,.F.);
#1662=ORIENTED_EDGE('',*,*,#1197,.T.);
#1663=ORIENTED_EDGE('',*,*,#1198,.T.);
#1664=ORIENTED_EDGE('',*,*,#1199,.T.);
#1665=ORIENTED_EDGE('',*,*,#1200,.T.);
#1666=ORIENTED_EDGE('',*,*,#1201,.T.);
#1667=ORIENTED_EDGE('',*,*,#1202,.T.);
#1668=ORIENTED_EDGE('',*,*,#1203,.T.);
#1669=ORIENTED_EDGE('',*,*,#1204,.T.);
#1670=ORIENTED_EDGE('',*,*,#1205,.T.);
#1671=ORIENTED_EDGE('',*,*,#1206,.T.);
#1672=ORIENTED_EDGE('',*,*,#1207,.T.);
#1673=ORIENTED_EDGE('',*,*,#1208,.T.);
#1674=ORIENTED_EDGE('',*,*,#1209,.F.);
#1675=ORIENTED_EDGE('',*,*,#1210,.T.);
#1676=ORIENTED_EDGE('',*,*,#1211,.T.);
#1677=ORIENTED_EDGE('',*,*,#1212,.T.);
#1678=ORIENTED_EDGE('',*,*,#1213,.T.);
#1679=ORIENTED_EDGE('',*,*,#1214,.T.);
#1680=ORIENTED_EDGE('',*,*,#1215,.T.);
#1681=ORIENTED_EDGE('',*,*,#1216,.T.);
#1682=ORIENTED_EDGE('',*,*,#1217,.T.);
#1683=ORIENTED_EDGE('',*,*,#1218,.T.);
#1684=ORIENTED_EDGE('',*,*,#1219,.T.);
#1685=ORIENTED_EDGE('',*,*,#1220,.T.);
#1686=ORIENTED_EDGE('',*,*,#1221,.T.);
#1687=ORIENTED_EDGE('',*,*,#1191,.T.);
#1688=ORIENTED_EDGE('',*,*,#1222,.T.);
#1689=ORIENTED_EDGE('',*,*,#1223,.F.);
#1690=ORIENTED_EDGE('',*,*,#1224,.F.);
#1691=ORIENTED_EDGE('',*,*,#1225,.F.);
#1692=ORIENTED_EDGE('',*,*,#1226,.F.);
#1693=ORIENTED_EDGE('',*,*,#1208,.F.);
#1694=ORIENTED_EDGE('',*,*,#1207,.F.);
#1695=ORIENTED_EDGE('',*,*,#1206,.F.);
#1696=ORIENTED_EDGE('',*,*,#1205,.F.);
#1697=ORIENTED_EDGE('',*,*,#1204,.F.);
#1698=ORIENTED_EDGE('',*,*,#1203,.F.);
#1699=ORIENTED_EDGE('',*,*,#1202,.F.);
#1700=ORIENTED_EDGE('',*,*,#1201,.F.);
#1701=ORIENTED_EDGE('',*,*,#1200,.F.);
#1702=ORIENTED_EDGE('',*,*,#1199,.F.);
#1703=ORIENTED_EDGE('',*,*,#1198,.F.);
#1704=ORIENTED_EDGE('',*,*,#1227,.F.);
#1705=ORIENTED_EDGE('',*,*,#1154,.T.);
#1706=ORIENTED_EDGE('',*,*,#1159,.T.);
#1707=ORIENTED_EDGE('',*,*,#1158,.T.);
#1708=ORIENTED_EDGE('',*,*,#1162,.T.);
#1709=ORIENTED_EDGE('',*,*,#1167,.T.);
#1710=ORIENTED_EDGE('',*,*,#1166,.T.);
#1711=ORIENTED_EDGE('',*,*,#1171,.T.);
#1712=ORIENTED_EDGE('',*,*,#1176,.T.);
#1713=ORIENTED_EDGE('',*,*,#1175,.T.);
#1714=ORIENTED_EDGE('',*,*,#1179,.T.);
#1715=ORIENTED_EDGE('',*,*,#1184,.T.);
#1716=ORIENTED_EDGE('',*,*,#1183,.T.);
#1717=ORIENTED_EDGE('',*,*,#1188,.T.);
#1718=ORIENTED_EDGE('',*,*,#1187,.T.);
#1719=ORIENTED_EDGE('',*,*,#1193,.T.);
#1720=ORIENTED_EDGE('',*,*,#1192,.T.);
#1721=ORIENTED_EDGE('',*,*,#1225,.T.);
#1722=ORIENTED_EDGE('',*,*,#1224,.T.);
#1723=ORIENTED_EDGE('',*,*,#1197,.F.);
#1724=ORIENTED_EDGE('',*,*,#1228,.T.);
#1725=ORIENTED_EDGE('',*,*,#1155,.T.);
#1726=ORIENTED_EDGE('',*,*,#1227,.T.);
#1727=ORIENTED_EDGE('',*,*,#1229,.F.);
#1728=ORIENTED_EDGE('',*,*,#1230,.F.);
#1729=ORIENTED_EDGE('',*,*,#1222,.F.);
#1730=ORIENTED_EDGE('',*,*,#1195,.F.);
#1731=ORIENTED_EDGE('',*,*,#1194,.F.);
#1732=ORIENTED_EDGE('',*,*,#1190,.F.);
#1733=ORIENTED_EDGE('',*,*,#1189,.F.);
#1734=ORIENTED_EDGE('',*,*,#1185,.F.);
#1735=ORIENTED_EDGE('',*,*,#1181,.F.);
#1736=ORIENTED_EDGE('',*,*,#1180,.F.);
#1737=ORIENTED_EDGE('',*,*,#1177,.F.);
#1738=ORIENTED_EDGE('',*,*,#1173,.F.);
#1739=ORIENTED_EDGE('',*,*,#1172,.F.);
#1740=ORIENTED_EDGE('',*,*,#1169,.F.);
#1741=ORIENTED_EDGE('',*,*,#1168,.F.);
#1742=ORIENTED_EDGE('',*,*,#1164,.F.);
#1743=ORIENTED_EDGE('',*,*,#1163,.F.);
#1744=ORIENTED_EDGE('',*,*,#1160,.F.);
#1745=ORIENTED_EDGE('',*,*,#1156,.F.);
#1746=ORIENTED_EDGE('',*,*,#1228,.F.);
#1747=ORIENTED_EDGE('',*,*,#1221,.F.);
#1748=ORIENTED_EDGE('',*,*,#1220,.F.);
#1749=ORIENTED_EDGE('',*,*,#1219,.F.);
#1750=ORIENTED_EDGE('',*,*,#1218,.F.);
#1751=ORIENTED_EDGE('',*,*,#1217,.F.);
#1752=ORIENTED_EDGE('',*,*,#1216,.F.);
#1753=ORIENTED_EDGE('',*,*,#1215,.F.);
#1754=ORIENTED_EDGE('',*,*,#1214,.F.);
#1755=ORIENTED_EDGE('',*,*,#1213,.F.);
#1756=ORIENTED_EDGE('',*,*,#1212,.F.);
#1757=ORIENTED_EDGE('',*,*,#1211,.F.);
#1758=ORIENTED_EDGE('',*,*,#1210,.F.);
#1759=ORIENTED_EDGE('',*,*,#1231,.F.);
#1760=ORIENTED_EDGE('',*,*,#1196,.T.);
#1761=ORIENTED_EDGE('',*,*,#1232,.F.);
#1762=ORIENTED_EDGE('',*,*,#1233,.T.);
#1763=ORIENTED_EDGE('',*,*,#1231,.T.);
#1764=ORIENTED_EDGE('',*,*,#1233,.F.);
#1765=ORIENTED_EDGE('',*,*,#1232,.T.);
#1766=ORIENTED_EDGE('',*,*,#1229,.T.);
#1767=ORIENTED_EDGE('',*,*,#1209,.T.);
#1768=ORIENTED_EDGE('',*,*,#1226,.T.);
#1769=ORIENTED_EDGE('',*,*,#1223,.T.);
#1770=ORIENTED_EDGE('',*,*,#1230,.T.);
#1906=CYLINDRICAL_SURFACE('',#2196,2.37175);
#1907=CYLINDRICAL_SURFACE('',#2198,2.37175);
#1908=CYLINDRICAL_SURFACE('',#2199,2.37175);
#1909=CYLINDRICAL_SURFACE('',#2200,2.37175);
#1910=CYLINDRICAL_SURFACE('',#2201,2.37175);
#1911=CYLINDRICAL_SURFACE('',#2202,2.37175);
#1912=CYLINDRICAL_SURFACE('',#2203,2.37175);
#1913=CYLINDRICAL_SURFACE('',#2204,2.37175);
#1914=CYLINDRICAL_SURFACE('',#2205,2.37175);
#1915=CYLINDRICAL_SURFACE('',#2206,2.37175);
#1916=CYLINDRICAL_SURFACE('',#2207,2.942);
#1917=CYLINDRICAL_SURFACE('',#2211,2.37175);
#1918=CYLINDRICAL_SURFACE('',#2216,4.);
#1974=ADVANCED_FACE('',(#325),#1906,.T.);
#1975=ADVANCED_FACE('',(#326),#1907,.T.);
#1976=ADVANCED_FACE('',(#327),#1908,.T.);
#1977=ADVANCED_FACE('',(#328),#1909,.T.);
#1978=ADVANCED_FACE('',(#329),#1910,.T.);
#1979=ADVANCED_FACE('',(#330),#1911,.T.);
#1980=ADVANCED_FACE('',(#331),#1912,.T.);
#1981=ADVANCED_FACE('',(#332),#1913,.T.);
#1982=ADVANCED_FACE('',(#333),#1914,.T.);
#1983=ADVANCED_FACE('',(#334),#1915,.T.);
#1984=ADVANCED_FACE('',(#335,#214),#1916,.T.);
#1985=ADVANCED_FACE('',(#336),#1917,.T.);
#1986=ADVANCED_FACE('',(#337),#47,.F.);
#1987=ADVANCED_FACE('',(#338),#247,.T.);
#1988=ADVANCED_FACE('',(#339),#48,.F.);
#1989=ADVANCED_FACE('',(#340,#215),#248,.F.);
#1990=ADVANCED_FACE('',(#341),#1918,.T.);
#1991=ADVANCED_FACE('',(#342),#249,.T.);
#1992=ADVANCED_FACE('',(#343),#250,.F.);
#2022=CLOSED_SHELL('',(#1974,#1975,#1976,#1977,#1978,#1979,#1980,#1981,
#1982,#1983,#1984,#1985,#1986,#1987,#1988,#1989,#1990,#1991,#1992));
#2195=AXIS2_PLACEMENT_3D('',#10938,#2495,#2496);
#2196=AXIS2_PLACEMENT_3D('',#10939,#2497,#2498);
#2197=AXIS2_PLACEMENT_3D('',#11048,#2500,#2501);
#2198=AXIS2_PLACEMENT_3D('',#11111,#2502,#2503);
#2199=AXIS2_PLACEMENT_3D('',#11478,#2505,#2506);
#2200=AXIS2_PLACEMENT_3D('',#11841,#2508,#2509);
#2201=AXIS2_PLACEMENT_3D('',#12101,#2511,#2512);
#2202=AXIS2_PLACEMENT_3D('',#12422,#2514,#2515);
#2203=AXIS2_PLACEMENT_3D('',#12781,#2517,#2518);
#2204=AXIS2_PLACEMENT_3D('',#13146,#2520,#2521);
#2205=AXIS2_PLACEMENT_3D('',#13401,#2523,#2524);
#2206=AXIS2_PLACEMENT_3D('',#13733,#2526,#2527);
#2207=AXIS2_PLACEMENT_3D('',#14115,#2529,#2530);
#2208=AXIS2_PLACEMENT_3D('',#14117,#2531,#2532);
#2209=AXIS2_PLACEMENT_3D('',#14120,#2533,#2534);
#2210=AXIS2_PLACEMENT_3D('',#16182,#2535,#2536);
#2211=AXIS2_PLACEMENT_3D('',#18148,#2537,#2538);
#2212=AXIS2_PLACEMENT_3D('',#18267,#2539,#2540);
#2213=AXIS2_PLACEMENT_3D('',#18821,#2541,#2542);
#2214=AXIS2_PLACEMENT_3D('',#19284,#2543,#2544);
#2215=AXIS2_PLACEMENT_3D('',#19286,#2545,#2546);
#2216=AXIS2_PLACEMENT_3D('',#19287,#2547,#2548);
#2217=AXIS2_PLACEMENT_3D('',#19289,#2549,#2550);
#2218=AXIS2_PLACEMENT_3D('',#19291,#2552,#2553);
#2219=AXIS2_PLACEMENT_3D('',#19292,#2554,#2555);
#2495=DIRECTION('axis',(0.,0.,1.));
#2496=DIRECTION('refdir',(1.,0.,0.));
#2497=DIRECTION('center_axis',(0.,0.,1.));
#2498=DIRECTION('ref_axis',(-0.457964771069041,-0.888970341721073,0.));
#2499=DIRECTION('',(0.,0.,-1.));
#2500=DIRECTION('center_axis',(0.,0.,-1.));
#2501=DIRECTION('ref_axis',(1.,5.97970744629653E-14,0.));
#2502=DIRECTION('center_axis',(0.,0.,1.));
#2503=DIRECTION('ref_axis',(-0.457964771069041,-0.888970341721073,0.));
#2504=DIRECTION('',(0.,0.,-1.));
#2505=DIRECTION('center_axis',(0.,0.,1.));
#2506=DIRECTION('ref_axis',(-0.457964771069041,-0.888970341721073,0.));
#2507=DIRECTION('',(0.,0.,-1.));
#2508=DIRECTION('center_axis',(0.,0.,1.));
#2509=DIRECTION('ref_axis',(-0.457964771069041,-0.888970341721073,0.));
#2510=DIRECTION('',(0.,0.,-1.));
#2511=DIRECTION('center_axis',(0.,0.,1.));
#2512=DIRECTION('ref_axis',(-0.457964771069041,-0.888970341721073,0.));
#2513=DIRECTION('',(0.,0.,-1.));
#2514=DIRECTION('center_axis',(0.,0.,1.));
#2515=DIRECTION('ref_axis',(-0.457964771069041,-0.888970341721073,0.));
#2516=DIRECTION('',(0.,0.,-1.));
#2517=DIRECTION('center_axis',(0.,0.,1.));
#2518=DIRECTION('ref_axis',(-0.457964771069041,-0.888970341721073,0.));
#2519=DIRECTION('',(0.,0.,-1.));
#2520=DIRECTION('center_axis',(0.,0.,1.));
#2521=DIRECTION('ref_axis',(-0.457964771069041,-0.888970341721073,0.));
#2522=DIRECTION('',(0.,0.,-1.));
#2523=DIRECTION('center_axis',(0.,0.,1.));
#2524=DIRECTION('ref_axis',(-0.457964771069041,-0.888970341721073,0.));
#2525=DIRECTION('',(0.,0.,-1.));
#2526=DIRECTION('center_axis',(0.,0.,1.));
#2527=DIRECTION('ref_axis',(-0.457964771069041,-0.888970341721073,0.));
#2528=DIRECTION('',(0.,0.,-1.));
#2529=DIRECTION('center_axis',(0.,0.,1.));
#2530=DIRECTION('ref_axis',(1.,0.,0.));
#2531=DIRECTION('center_axis',(0.,0.,1.));
#2532=DIRECTION('ref_axis',(1.,0.,0.));
#2533=DIRECTION('center_axis',(0.,0.,-1.));
#2534=DIRECTION('ref_axis',(1.,0.,0.));
#2535=DIRECTION('center_axis',(0.,0.,1.));
#2536=DIRECTION('ref_axis',(1.,0.,0.));
#2537=DIRECTION('center_axis',(0.,0.,1.));
#2538=DIRECTION('ref_axis',(-0.457964771069041,-0.888970341721073,0.));
#2539=DIRECTION('center_axis',(0.,0.,1.));
#2540=DIRECTION('ref_axis',(1.,5.97970744629653E-14,0.));
#2541=DIRECTION('center_axis',(0.,0.,1.));
#2542=DIRECTION('ref_axis',(1.,0.,0.));
#2543=DIRECTION('center_axis',(0.,0.,-1.));
#2544=DIRECTION('ref_axis',(1.,0.,0.));
#2545=DIRECTION('center_axis',(0.,0.,-1.));
#2546=DIRECTION('ref_axis',(1.,0.,0.));
#2547=DIRECTION('center_axis',(0.,0.,-1.));
#2548=DIRECTION('ref_axis',(1.,0.,0.));
#2549=DIRECTION('center_axis',(0.,0.,-1.));
#2550=DIRECTION('ref_axis',(1.,0.,0.));
#2551=DIRECTION('',(0.,0.,1.));
#2552=DIRECTION('center_axis',(0.,0.,-1.));
#2553=DIRECTION('ref_axis',(1.,0.,0.));
#2554=DIRECTION('center_axis',(0.,0.,-1.));
#2555=DIRECTION('ref_axis',(1.,0.,0.));
#10938=CARTESIAN_POINT('',(0.,0.,0.));
#10939=CARTESIAN_POINT('Origin',(-33.7561270252576,0.,302.151410108095));
#10940=CARTESIAN_POINT('',(-32.6699490794746,2.10841540797695,304.52294196412));
#10941=CARTESIAN_POINT('',(-32.6699490795102,2.1084154079953,304.328189117937));
#10942=CARTESIAN_POINT('',(-32.6699490794746,2.10841540797695,302.151410108095));
#10943=CARTESIAN_POINT('',(-35.133102683896,-1.9310971228857,304.000068852074));
#10944=CARTESIAN_POINT('Ctrl Pts',(-35.133102683896,-1.9310971228857,304.000068852074));
#10945=CARTESIAN_POINT('Ctrl Pts',(-35.0694875830777,-1.9764580963502,304.005341754287));
#10946=CARTESIAN_POINT('Ctrl Pts',(-35.003498681129,-2.0187646946572,304.0106146565));
#10947=CARTESIAN_POINT('Ctrl Pts',(-34.9354651692809,-2.05775596331338,
304.015887558713));
#10948=CARTESIAN_POINT('Ctrl Pts',(-34.8647099473273,-2.09830709455844,
304.021371405662));
#10949=CARTESIAN_POINT('Ctrl Pts',(-34.7917434392969,-2.13527166672132,
304.026855252612));
#10950=CARTESIAN_POINT('Ctrl Pts',(-34.7169726735715,-2.16840349165374,
304.032339099561));
#10951=CARTESIAN_POINT('Ctrl Pts',(-34.6452583963628,-2.20018094978974,
304.037598777144));
#10952=CARTESIAN_POINT('Ctrl Pts',(-34.5718849778249,-2.22843266779446,
304.042858454727));
#10953=CARTESIAN_POINT('Ctrl Pts',(-34.4972378823615,-2.25298751882534,
304.048118132309));
#10954=CARTESIAN_POINT('Ctrl Pts',(-34.4226319693529,-2.27752882305931,
304.053374908152));
#10955=CARTESIAN_POINT('Ctrl Pts',(-34.3467542284446,-2.29837715672903,
304.058631683995));
#10956=CARTESIAN_POINT('Ctrl Pts',(-34.2700087638124,-2.31541003307836,
304.063888459838));
#10957=CARTESIAN_POINT('Ctrl Pts',(-34.1932804682484,-2.33243909892737,
304.069144059664));
#10958=CARTESIAN_POINT('Ctrl Pts',(-34.1156853028774,-2.34565429840249,
304.07439965949));
#10959=CARTESIAN_POINT('Ctrl Pts',(-34.0376395453986,-2.35498381385177,
304.079655259316));
#10960=CARTESIAN_POINT('Ctrl Pts',(-33.9595856504682,-2.36431430204428,
304.084911407119));
#10961=CARTESIAN_POINT('Ctrl Pts',(-33.8810815471019,-2.36975824789373,
304.090167554921));
#10962=CARTESIAN_POINT('Ctrl Pts',(-33.8025490068216,-2.37129565051001,
304.095423702723));
#10963=CARTESIAN_POINT('Ctrl Pts',(-33.723934956216,-2.3728346488239,304.100685305974));
#10964=CARTESIAN_POINT('Ctrl Pts',(-33.6452928903964,-2.37045900619068,
304.105946909226));
#10965=CARTESIAN_POINT('Ctrl Pts',(-33.5670440657278,-2.3642008579889,304.111208512478));
#10966=CARTESIAN_POINT('Ctrl Pts',(-33.4887470148127,-2.35793885277075,
304.116473358556));
#10967=CARTESIAN_POINT('Ctrl Pts',(-33.4108441623262,-2.34778964589175,
304.121738204635));
#10968=CARTESIAN_POINT('Ctrl Pts',(-33.3337485462396,-2.33383685868624,
304.127003050713));
#10969=CARTESIAN_POINT('Ctrl Pts',(-33.2565304255633,-2.31986190056416,
304.132276262608));
#10970=CARTESIAN_POINT('Ctrl Pts',(-33.1801225653048,-2.30207141758808,
304.137549474504));
#10971=CARTESIAN_POINT('Ctrl Pts',(-33.1049239604095,-2.28059918241509,
304.142822686399));
#10972=CARTESIAN_POINT('Ctrl Pts',(-33.0826909043258,-2.27425074803247,
304.144381752767));
#10973=CARTESIAN_POINT('Ctrl Pts',(-33.0605634223953,-2.26758079988008,
304.145940819135));
#10974=CARTESIAN_POINT('Ctrl Pts',(-33.0385514704231,-2.26059359142769,
304.147499885503));
#10975=CARTESIAN_POINT('Ctrl Pts',(-32.9631613635555,-2.23666266551085,
304.152839629122));
#10976=CARTESIAN_POINT('Ctrl Pts',(-32.8888314869022,-2.20891240408737,
304.158179372741));
#10977=CARTESIAN_POINT('Ctrl Pts',(-32.8159756387904,-2.17745572469886,
304.163519116361));
#10978=CARTESIAN_POINT('Ctrl Pts',(-32.7432229658767,-2.14604359285473,
304.168851298074));
#10979=CARTESIAN_POINT('Ctrl Pts',(-32.6719406011688,-2.11093565139043,
304.174183479787));
#10980=CARTESIAN_POINT('Ctrl Pts',(-32.6025265181288,-2.07229436433442,
304.1795156615));
#10981=CARTESIAN_POINT('Ctrl Pts',(-32.5331907392874,-2.03369666749643,
304.184841828119));
#10982=CARTESIAN_POINT('Ctrl Pts',(-32.4657194599147,-1.99157377244779,
304.190167994738));
#10983=CARTESIAN_POINT('Ctrl Pts',(-32.4004886439478,-1.94613530917556,
304.195494161357));
#10984=CARTESIAN_POINT('Ctrl Pts',(-32.3352980304424,-1.90072485012248,
304.200817045402));
#10985=CARTESIAN_POINT('Ctrl Pts',(-32.2723455217536,-1.85200314549746,
304.206139929447));
#10986=CARTESIAN_POINT('Ctrl Pts',(-32.2119794855934,-1.80022399668736,
304.211462813492));
#10987=CARTESIAN_POINT('Ctrl Pts',(-32.1516320067756,-1.74846076549336,
304.216784061209));
#10988=CARTESIAN_POINT('Ctrl Pts',(-32.0938697758154,-1.69364226066575,
304.222105308927));
#10989=CARTESIAN_POINT('Ctrl Pts',(-32.0390081820352,-1.63606263350478,
304.227426556645));
#10990=CARTESIAN_POINT('Ctrl Pts',(-31.9841465073673,-1.57848292144862,
304.232747812208));
#10991=CARTESIAN_POINT('Ctrl Pts',(-31.9321857996217,-1.51814241821111,
304.238069067771));
#10992=CARTESIAN_POINT('Ctrl Pts',(-31.8834036289627,-1.45537113598888,
304.243390323335));
#10993=CARTESIAN_POINT('Ctrl Pts',(-31.8345721355805,-1.39253638691941,
304.248716959118));
#10994=CARTESIAN_POINT('Ctrl Pts',(-31.7889258863432,-1.32726631919432,
304.254043594902));
#10995=CARTESIAN_POINT('Ctrl Pts',(-31.7467008958156,-1.25992249476528,
304.259370230685));
#10996=CARTESIAN_POINT('Ctrl Pts',(-31.7044552699207,-1.19254575938631,
304.264699469597));
#10997=CARTESIAN_POINT('Ctrl Pts',(-31.6656344619511,-1.1230936566465,304.270028708509));
#10998=CARTESIAN_POINT('Ctrl Pts',(-31.6304287304042,-1.0519528609959,304.275357947421));
#10999=CARTESIAN_POINT('Ctrl Pts',(-31.5951589238931,-0.980682588020334,
304.280696885629));
#11000=CARTESIAN_POINT('Ctrl Pts',(-31.5635175276295,-0.907717910366174,
304.286035823837));
#11001=CARTESIAN_POINT('Ctrl Pts',(-31.5356467269886,-0.833465840631194,
304.291374762044));
#11002=CARTESIAN_POINT('Ctrl Pts',(-31.5094819150593,-0.763758785387225,
304.296386900587));
#11003=CARTESIAN_POINT('Ctrl Pts',(-31.4866398483132,-0.692917589734796,
304.301399039129));
#11004=CARTESIAN_POINT('Ctrl Pts',(-31.4671973727891,-0.62128826526054,
304.306411177672));
#11005=CARTESIAN_POINT('Ctrl Pts',(-31.4465296698883,-0.545144998659011,
304.311739171536));
#11006=CARTESIAN_POINT('Ctrl Pts',(-31.4296258778281,-0.467823027100496,
304.3170671654));
#11007=CARTESIAN_POINT('Ctrl Pts',(-31.4166165369438,-0.389729056614872,
304.322395159264));
#11008=CARTESIAN_POINT('Ctrl Pts',(-31.4036261558074,-0.311748899887667,
304.327715388137));
#11009=CARTESIAN_POINT('Ctrl Pts',(-31.3945190316741,-0.232999437688756,
304.33303561701));
#11010=CARTESIAN_POINT('Ctrl Pts',(-31.3893755614233,-0.153901172634812,
304.338355845883));
#11011=CARTESIAN_POINT('Ctrl Pts',(-31.3842381475483,-0.0748960448578465,
304.343669810248));
#11012=CARTESIAN_POINT('Ctrl Pts',(-31.383055143537,0.00445660346383708,
304.348983774614));
#11013=CARTESIAN_POINT('Ctrl Pts',(-31.3858554128096,0.0837290016837932,
304.35429773898));
#11014=CARTESIAN_POINT('Ctrl Pts',(-31.3886538752934,0.162950251796037,
304.359608274672));
#11015=CARTESIAN_POINT('Ctrl Pts',(-31.3954304936321,0.242090886526085,
304.364918810363));
#11016=CARTESIAN_POINT('Ctrl Pts',(-31.4061620604436,0.320722195438071,
304.370229346055));
#11017=CARTESIAN_POINT('Ctrl Pts',(-31.4168900604234,0.399327369802875,
304.375538116693));
#11018=CARTESIAN_POINT('Ctrl Pts',(-31.4315703353571,0.477423089519046,
304.380846887332));
#11019=CARTESIAN_POINT('Ctrl Pts',(-31.4501278790099,0.554586332327998,
304.38615565797));
#11020=CARTESIAN_POINT('Ctrl Pts',(-31.4686850603757,0.631748068728147,
304.391464324969));
#11021=CARTESIAN_POINT('Ctrl Pts',(-31.4911192489282,0.70797690809233,304.396772991968));
#11022=CARTESIAN_POINT('Ctrl Pts',(-31.5173047749994,0.782862053141504,
304.402081658966));
#11023=CARTESIAN_POINT('Ctrl Pts',(-31.543516409334,0.857821862380335,304.407395618968));
#11024=CARTESIAN_POINT('Ctrl Pts',(-31.5734866975547,0.931434856612447,
304.41270957897));
#11025=CARTESIAN_POINT('Ctrl Pts',(-31.6070409009699,1.0033079750975,304.418023538972));
#11026=CARTESIAN_POINT('Ctrl Pts',(-31.6406111111443,1.0752153800676,304.423340033956));
#11027=CARTESIAN_POINT('Ctrl Pts',(-31.677768422223,1.14538084027812,304.428656528939));
#11028=CARTESIAN_POINT('Ctrl Pts',(-31.7182921612011,1.21343608374556,304.433973023922));
#11029=CARTESIAN_POINT('Ctrl Pts',(-31.7588901001272,1.28161593801295,304.439299253537));
#11030=CARTESIAN_POINT('Ctrl Pts',(-31.8028665231676,1.34767746266607,304.444625483151));
#11031=CARTESIAN_POINT('Ctrl Pts',(-31.8499575801153,1.41128172556225,304.449951712766));
#11032=CARTESIAN_POINT('Ctrl Pts',(-31.8952569913421,1.47246607451222,304.455075298457));
#11033=CARTESIAN_POINT('Ctrl Pts',(-31.9434380280056,1.53137651453439,304.460198884149));
#11034=CARTESIAN_POINT('Ctrl Pts',(-31.9942333057017,1.58774323600805,304.465322469841));
#11035=CARTESIAN_POINT('Ctrl Pts',(-32.0470827982975,1.64638948747656,304.470653258772));
#11036=CARTESIAN_POINT('Ctrl Pts',(-32.1029637711113,1.70250526679375,304.475984047703));
#11037=CARTESIAN_POINT('Ctrl Pts',(-32.1616044026078,1.75576070931038,304.481314836634));
#11038=CARTESIAN_POINT('Ctrl Pts',(-32.2201707660216,1.8089487040607,304.486638874146));
#11039=CARTESIAN_POINT('Ctrl Pts',(-32.2814895103399,1.85928323676079,304.491962911658));
#11040=CARTESIAN_POINT('Ctrl Pts',(-32.3452499759995,1.90646899119202,304.49728694917));
#11041=CARTESIAN_POINT('Ctrl Pts',(-32.408939174419,1.95360200450137,304.502605035824));
#11042=CARTESIAN_POINT('Ctrl Pts',(-32.4750642973849,1.9975929542515,304.507923122478));
#11043=CARTESIAN_POINT('Ctrl Pts',(-32.5432806701215,2.03818590450751,304.513241209133));
#11044=CARTESIAN_POINT('Ctrl Pts',(-32.5847586402436,2.06286785563367,304.516474794129));
#11045=CARTESIAN_POINT('Ctrl Pts',(-32.6270090988392,2.08629431182957,304.519708379124));
#11046=CARTESIAN_POINT('Ctrl Pts',(-32.6699490794746,2.10841540797695,304.52294196412));
#11047=CARTESIAN_POINT('',(-32.3791022351265,-1.93106208855757,304.));
#11048=CARTESIAN_POINT('Origin',(-33.7561270252576,0.,304.));
#11049=CARTESIAN_POINT('Ctrl Pts',(-32.3791022351265,-1.93106208855758,
304.));
#11050=CARTESIAN_POINT('Ctrl Pts',(-32.372383794194,-1.92627122255186,304.000553722788));
#11051=CARTESIAN_POINT('Ctrl Pts',(-32.365690294893,-1.92144525176054,304.001105480632));
#11052=CARTESIAN_POINT('Ctrl Pts',(-32.351055489904,-1.91077712792039,304.002312345817));
#11053=CARTESIAN_POINT('Ctrl Pts',(-32.3431251147181,-1.90492017144399,
304.002966647622));
#11054=CARTESIAN_POINT('Ctrl Pts',(-32.3123044268341,-1.88185926415591,
304.005511672187));
#11055=CARTESIAN_POINT('Ctrl Pts',(-32.2896890562164,-1.86429016234149,
304.007383786941));
#11056=CARTESIAN_POINT('Ctrl Pts',(-32.1433176031211,-1.74626715523718,
304.019567842445));
#11057=CARTESIAN_POINT('Ctrl Pts',(-32.029629893516,-1.6339581815929,304.02937038556));
#11058=CARTESIAN_POINT('Ctrl Pts',(-31.8625511884864,-1.43183153393863,
304.045807677244));
#11059=CARTESIAN_POINT('Ctrl Pts',(-31.8022683225534,-1.34840805993611,
304.052310383391));
#11060=CARTESIAN_POINT('Ctrl Pts',(-31.7294611830989,-1.23247143628013,
304.061207693097));
#11061=CARTESIAN_POINT('Ctrl Pts',(-31.7119560853931,-1.2032145583658,304.063441326482));
#11062=CARTESIAN_POINT('Ctrl Pts',(-31.6828615830205,-1.15211935922127,
304.067329597822));
#11063=CARTESIAN_POINT('Ctrl Pts',(-31.6709715775492,-1.13045800411972,
304.068974179702));
#11064=CARTESIAN_POINT('Ctrl Pts',(-31.6470762526234,-1.08526520511566,
304.07240012123));
#11065=CARTESIAN_POINT('Ctrl Pts',(-31.6351213442428,-1.06171113614403,
304.074182843954));
#11066=CARTESIAN_POINT('Ctrl Pts',(-31.6046373686383,-0.999079775851659,
304.078918926595));
#11067=CARTESIAN_POINT('Ctrl Pts',(-31.5867801472149,-0.959688416450391,
304.081893480809));
#11068=CARTESIAN_POINT('Ctrl Pts',(-31.5011751545305,-0.756235746958286,
304.097252202384));
#11069=CARTESIAN_POINT('Ctrl Pts',(-31.4509327899566,-0.585455956005303,
304.110186955138));
#11070=CARTESIAN_POINT('Ctrl Pts',(-31.4040698176274,-0.318920429501764,
304.130075262116));
#11071=CARTESIAN_POINT('Ctrl Pts',(-31.3933547949862,-0.2262574943469,304.136923917303));
#11072=CARTESIAN_POINT('Ctrl Pts',(-31.3852061838439,-0.0813934329749035,
304.147360545508));
#11073=CARTESIAN_POINT('Ctrl Pts',(-31.3839927149568,-0.0295001198401178,
304.151044748579));
#11074=CARTESIAN_POINT('Ctrl Pts',(-31.3846576241952,0.0409130542434561,
304.155937841315));
#11075=CARTESIAN_POINT('Ctrl Pts',(-31.3850493654905,0.0594288202409265,
304.157214556448));
#11076=CARTESIAN_POINT('Ctrl Pts',(-31.3860773174482,0.0906934458287153,
304.159351557626));
#11077=CARTESIAN_POINT('Ctrl Pts',(-31.3865996294996,0.103445005545772,
304.160217859862));
#11078=CARTESIAN_POINT('Ctrl Pts',(-31.3879186001374,0.130335865156393,
304.162032829539));
#11079=CARTESIAN_POINT('Ctrl Pts',(-31.3887389998056,0.144473339197381,
304.162980170615));
#11080=CARTESIAN_POINT('Ctrl Pts',(-31.3914324490789,0.184661013930785,
304.165655857413));
#11081=CARTESIAN_POINT('Ctrl Pts',(-31.3936092732913,0.210689678850066,
304.167368196035));
#11082=CARTESIAN_POINT('Ctrl Pts',(-31.408759857812,0.36175558652666,304.177214760618));
#11083=CARTESIAN_POINT('Ctrl Pts',(-31.4312295616042,0.485653295681868,
304.184932480841));
#11084=CARTESIAN_POINT('Ctrl Pts',(-31.4907951271127,0.710565841075942,
304.199207257352));
#11085=CARTESIAN_POINT('Ctrl Pts',(-31.5251293607131,0.811960750388482,
304.205748774764));
#11086=CARTESIAN_POINT('Ctrl Pts',(-31.5918300990257,0.972356665312212,
304.216653188886));
#11087=CARTESIAN_POINT('Ctrl Pts',(-31.6200661485106,1.03290917980854,304.220905457598));
#11088=CARTESIAN_POINT('Ctrl Pts',(-31.6638603280129,1.11732731735751,304.227085539766));
#11089=CARTESIAN_POINT('Ctrl Pts',(-31.6773519155927,1.14223211051689,304.228941083339));
#11090=CARTESIAN_POINT('Ctrl Pts',(-31.7018742494461,1.18562505501877,304.232235225492));
#11091=CARTESIAN_POINT('Ctrl Pts',(-31.7127169367836,1.2042160913737,304.233666799671));
#11092=CARTESIAN_POINT('Ctrl Pts',(-31.7360493754349,1.24299958800252,304.23669771837));
#11093=CARTESIAN_POINT('Ctrl Pts',(-31.7485922774706,1.26315709619378,304.238298959829));
#11094=CARTESIAN_POINT('Ctrl Pts',(-31.7832034831385,1.31696232430415,304.242645578171));
#11095=CARTESIAN_POINT('Ctrl Pts',(-31.8058280346489,1.3502409247028,304.245412136589));
#11096=CARTESIAN_POINT('Ctrl Pts',(-31.9430749518018,1.54146795382015,304.261785416916));
#11097=CARTESIAN_POINT('Ctrl Pts',(-32.0759767677403,1.68533294663214,304.276143635163));
#11098=CARTESIAN_POINT('Ctrl Pts',(-32.2812087133711,1.85882772557642,304.295885295031));
#11099=CARTESIAN_POINT('Ctrl Pts',(-32.3396540123282,1.90374107562473,304.30127104078));
#11100=CARTESIAN_POINT('Ctrl Pts',(-32.4363786513325,1.9711463092728,304.309717051742));
#11101=CARTESIAN_POINT('Ctrl Pts',(-32.4733619057364,1.99541169177774,304.312844363311));
#11102=CARTESIAN_POINT('Ctrl Pts',(-32.5253632199481,2.02748689632691,304.317080377009));
#11103=CARTESIAN_POINT('Ctrl Pts',(-32.539816164388,2.03619021541879,304.318241011223));
#11104=CARTESIAN_POINT('Ctrl Pts',(-32.5649011618963,2.05093355995385,304.320225156927));
#11105=CARTESIAN_POINT('Ctrl Pts',(-32.5754883891497,2.05704641372135,304.321053285514));
#11106=CARTESIAN_POINT('Ctrl Pts',(-32.5987250625579,2.07022429727514,304.322851050667));
#11107=CARTESIAN_POINT('Ctrl Pts',(-32.6113925350712,2.07725562192876,304.323818552738));
#11108=CARTESIAN_POINT('Ctrl Pts',(-32.6393100146382,2.09241880908629,304.325925222684));
#11109=CARTESIAN_POINT('Ctrl Pts',(-32.6545859334898,2.10050088113243,304.327061439715));
#11110=CARTESIAN_POINT('Ctrl Pts',(-32.6699490795102,2.1084154079953,304.328189117937));
#11111=CARTESIAN_POINT('Origin',(-33.7561270252576,0.,302.151410108095));
#11112=CARTESIAN_POINT('',(-32.6699490731211,2.10841540470388,305.524079281032));
#11113=CARTESIAN_POINT('',(-32.6699493942465,2.1084155701358,305.324530114841));
#11114=CARTESIAN_POINT('',(-32.6699490794746,2.10841540797695,302.151410108095));
#11115=CARTESIAN_POINT('',(-36.1278767663821,0.00110814072209554,304.848589891855));
#11116=CARTESIAN_POINT('Ctrl Pts',(-32.6699490731214,2.10841540470401,305.524079281032));
#11117=CARTESIAN_POINT('Ctrl Pts',(-32.6181216565324,2.08171582876206,305.520434275554));
#11118=CARTESIAN_POINT('Ctrl Pts',(-32.5672521921668,2.05309167355925,305.516743827637));
#11119=CARTESIAN_POINT('Ctrl Pts',(-32.4854943209372,2.00302137170522,305.510578700104));
#11120=CARTESIAN_POINT('Ctrl Pts',(-32.454010028249,1.98269845406367,305.508144832193));
#11121=CARTESIAN_POINT('Ctrl Pts',(-32.4034285920564,1.94832394525082,305.504127258202));
#11122=CARTESIAN_POINT('Ctrl Pts',(-32.3840367160886,1.93471635174277,305.502560304462));
#11123=CARTESIAN_POINT('Ctrl Pts',(-32.3465602066406,1.90757164974185,305.499477388479));
#11124=CARTESIAN_POINT('Ctrl Pts',(-32.3284586877127,1.8940621087477,305.497962606613));
#11125=CARTESIAN_POINT('Ctrl Pts',(-32.2855166339777,1.86104821955232,305.494305251938));
#11126=CARTESIAN_POINT('Ctrl Pts',(-32.2608679295274,1.84130265490888,305.492153274022));
#11127=CARTESIAN_POINT('Ctrl Pts',(-32.1688030044336,1.76448352823755,305.48390821089));
#11128=CARTESIAN_POINT('Ctrl Pts',(-32.1042062859053,1.70415792351539,305.477685449562));
#11129=CARTESIAN_POINT('Ctrl Pts',(-31.9102167026194,1.50158038130959,305.457568101374));
#11130=CARTESIAN_POINT('Ctrl Pts',(-31.7946758074913,1.34715674638086,305.443270458497));
#11131=CARTESIAN_POINT('Ctrl Pts',(-31.6798467494391,1.14705896648543,305.426868389652));
#11132=CARTESIAN_POINT('Ctrl Pts',(-31.6614765686871,1.1131594325377,305.424158539114));
#11133=CARTESIAN_POINT('Ctrl Pts',(-31.6370000137217,1.06523778711765,305.420437545151));
#11134=CARTESIAN_POINT('Ctrl Pts',(-31.6301912445061,1.05158353027739,305.41938949495));
#11135=CARTESIAN_POINT('Ctrl Pts',(-31.617966898918,1.02646483382323,305.417484921128));
#11136=CARTESIAN_POINT('Ctrl Pts',(-31.6125106258224,1.01502095753611,305.416626059093));
#11137=CARTESIAN_POINT('Ctrl Pts',(-31.6009915845908,0.99035390809909,305.414794249643));
#11138=CARTESIAN_POINT('Ctrl Pts',(-31.5949583155752,0.977117939095003,
305.413823026405));
#11139=CARTESIAN_POINT('Ctrl Pts',(-31.5778821625025,0.93872370948763,305.41103701726));
#11140=CARTESIAN_POINT('Ctrl Pts',(-31.5671537626555,0.91342711756605,305.409239861761));
#11141=CARTESIAN_POINT('Ctrl Pts',(-31.5171338724186,0.789538453185028,
305.400596970975));
#11142=CARTESIAN_POINT('Ctrl Pts',(-31.4840466025184,0.688561335344408,
305.394032332415));
#11143=CARTESIAN_POINT('Ctrl Pts',(-31.4137832117428,0.41284580156758,305.376556719394));
#11144=CARTESIAN_POINT('Ctrl Pts',(-31.3893771465728,0.235594430216639,
305.365743369847));
#11145=CARTESIAN_POINT('Ctrl Pts',(-31.3841509149287,0.0192899891988883,
305.351837760297));
#11146=CARTESIAN_POINT('Ctrl Pts',(-31.3841464266578,-0.0187229822491736,
305.349370046344));
#11147=CARTESIAN_POINT('Ctrl Pts',(-31.3856243381822,-0.0805064373339045,
305.345311372373));
#11148=CARTESIAN_POINT('Ctrl Pts',(-31.3865513222008,-0.104284197700153,
305.343737860391));
#11149=CARTESIAN_POINT('Ctrl Pts',(-31.3890521442885,-0.150539455882248,
305.340652496818));
#11150=CARTESIAN_POINT('Ctrl Pts',(-31.3905888490534,-0.173016461854979,
305.339141977042));
#11151=CARTESIAN_POINT('Ctrl Pts',(-31.3950198481144,-0.226598106673857,
305.33551274049));
#11152=CARTESIAN_POINT('Ctrl Pts',(-31.3982088666395,-0.257673433709,305.333384988067));
#11153=CARTESIAN_POINT('Ctrl Pts',(-31.4123690306273,-0.373148004602919,
305.325388757618));
#11154=CARTESIAN_POINT('Ctrl Pts',(-31.4272654415711,-0.456992025248043,
305.319400793902));
#11155=CARTESIAN_POINT('Ctrl Pts',(-31.4858069850722,-0.70743619402694,
305.300981347359));
#11156=CARTESIAN_POINT('Ctrl Pts',(-31.5431018911505,-0.870248190707576,
305.288238017824));
#11157=CARTESIAN_POINT('Ctrl Pts',(-31.642056148665,-1.07662778785411,305.27176955701));
#11158=CARTESIAN_POINT('Ctrl Pts',(-31.6684422114981,-1.1269411178138,305.267732675978));
#11159=CARTESIAN_POINT('Ctrl Pts',(-31.7062482664399,-1.19313566260966,
305.262435535179));
#11160=CARTESIAN_POINT('Ctrl Pts',(-31.7160925243171,-1.20989046296971,
305.261096035152));
#11161=CARTESIAN_POINT('Ctrl Pts',(-31.7327447513185,-1.23745111211543,
305.258897141823));
#11162=CARTESIAN_POINT('Ctrl Pts',(-31.7394359244163,-1.24832612573336,
305.25803069155));
#11163=CARTESIAN_POINT('Ctrl Pts',(-31.7536136304817,-1.27095727132005,
305.256230867488));
#11164=CARTESIAN_POINT('Ctrl Pts',(-31.7611164867596,-1.28270232624646,
305.255298556012));
#11165=CARTESIAN_POINT('Ctrl Pts',(-31.7820880874436,-1.31490231416333,
305.252745417354));
#11166=CARTESIAN_POINT('Ctrl Pts',(-31.7957711945606,-1.3352164455795,305.251137935039));
#11167=CARTESIAN_POINT('Ctrl Pts',(-31.8277389507178,-1.38112511928629,
305.247503579465));
#11168=CARTESIAN_POINT('Ctrl Pts',(-31.846223205704,-1.4065755412505,305.245487661209));
#11169=CARTESIAN_POINT('Ctrl Pts',(-31.9114730003668,-1.4927571065043,305.238629039777));
#11170=CARTESIAN_POINT('Ctrl Pts',(-31.9606747638233,-1.55158787637714,
305.23388967039));
#11171=CARTESIAN_POINT('Ctrl Pts',(-32.1364737003043,-1.74220667171159,
305.217954213384));
#11172=CARTESIAN_POINT('Ctrl Pts',(-32.2753877912973,-1.86171046637986,
305.206896218619));
#11173=CARTESIAN_POINT('Ctrl Pts',(-32.4576412969985,-1.98507806684135,
305.192743224935));
#11174=CARTESIAN_POINT('Ctrl Pts',(-32.4891405869647,-2.00532920800316,
305.190311002364));
#11175=CARTESIAN_POINT('Ctrl Pts',(-32.5413247513177,-2.03715842597403,
305.186295403946));
#11176=CARTESIAN_POINT('Ctrl Pts',(-32.5617277762762,-2.04918749331368,
305.184728746464));
#11177=CARTESIAN_POINT('Ctrl Pts',(-32.6019362513427,-2.07208880768021,
305.181645882816));
#11178=CARTESIAN_POINT('Ctrl Pts',(-32.6217237007363,-2.08298761531809,
305.180130849391));
#11179=CARTESIAN_POINT('Ctrl Pts',(-32.6695564107046,-2.10844987059365,
305.176471969222));
#11180=CARTESIAN_POINT('Ctrl Pts',(-32.697742294909,-2.12273836150287,305.174318698113));
#11181=CARTESIAN_POINT('Ctrl Pts',(-32.805925583813,-2.17489028993111,305.166060163608));
#11182=CARTESIAN_POINT('Ctrl Pts',(-32.8877261450782,-2.20882483112531,
305.159824665474));
#11183=CARTESIAN_POINT('Ctrl Pts',(-33.1537677640361,-2.30212562174332,
305.139602004255));
#11184=CARTESIAN_POINT('Ctrl Pts',(-33.3434431248135,-2.3435666723399,305.125205540751));
#11185=CARTESIAN_POINT('Ctrl Pts',(-33.5730667055112,-2.3649672452909,305.108824015106));
#11186=CARTESIAN_POINT('Ctrl Pts',(-33.6101746946479,-2.36754713408198,
305.10621142543));
#11187=CARTESIAN_POINT('Ctrl Pts',(-33.6625234416,-2.36995100138893,305.102588141953));
#11188=CARTESIAN_POINT('Ctrl Pts',(-33.6777234198243,-2.37050253852458,
305.101543482546));
#11189=CARTESIAN_POINT('Ctrl Pts',(-33.7055934205733,-2.37124544078164,
305.099642857348));
#11190=CARTESIAN_POINT('Ctrl Pts',(-33.7182615593693,-2.37148156710566,
305.098784597087));
#11191=CARTESIAN_POINT('Ctrl Pts',(-33.7455149831232,-2.37177109754041,
305.096950865752));
#11192=CARTESIAN_POINT('Ctrl Pts',(-33.760099723317,-2.37179151700474,305.095977163844));
#11193=CARTESIAN_POINT('Ctrl Pts',(-33.8023392391489,-2.37146101419212,
305.093176851555));
#11194=CARTESIAN_POINT('Ctrl Pts',(-33.8299898477957,-2.37076092330193,
305.091368141484));
#11195=CARTESIAN_POINT('Ctrl Pts',(-33.8946318827031,-2.36799210594985,
305.087183606622));
#11196=CARTESIAN_POINT('Ctrl Pts',(-33.931600224627,-2.36554003461956,305.084824153858));
#11197=CARTESIAN_POINT('Ctrl Pts',(-34.0711930949718,-2.35299022398947,
305.075991871651));
#11198=CARTESIAN_POINT('Ctrl Pts',(-34.1731832714032,-2.3370700185528,305.069693111292));
#11199=CARTESIAN_POINT('Ctrl Pts',(-34.4099525970118,-2.28411246821819,
305.05482454512));
#11200=CARTESIAN_POINT('Ctrl Pts',(-34.5431206747547,-2.2417165620999,305.046254938475));
#11201=CARTESIAN_POINT('Ctrl Pts',(-34.7089579750039,-2.17231100895509,
305.034728193582));
#11202=CARTESIAN_POINT('Ctrl Pts',(-34.7457266360603,-2.15580941662165,
305.032116895528));
#11203=CARTESIAN_POINT('Ctrl Pts',(-34.8039228525743,-2.12788867601317,
305.027883030112));
#11204=CARTESIAN_POINT('Ctrl Pts',(-34.8256273284665,-2.1170629044455,305.026280962068));
#11205=CARTESIAN_POINT('Ctrl Pts',(-34.8670028425869,-2.09562695551453,
305.023180228047));
#11206=CARTESIAN_POINT('Ctrl Pts',(-34.8866974921257,-2.08506781148047,
305.021683494114));
#11207=CARTESIAN_POINT('Ctrl Pts',(-34.9324881557618,-2.05967797867248,
305.018152936988));
#11208=CARTESIAN_POINT('Ctrl Pts',(-34.9584571323438,-2.04462736319817,
305.016111381013));
#11209=CARTESIAN_POINT('Ctrl Pts',(-35.048137862753,-1.99035253807139,305.008918871316));
#11210=CARTESIAN_POINT('Ctrl Pts',(-35.1102679548164,-1.94861373796396,
305.003678229668));
#11211=CARTESIAN_POINT('Ctrl Pts',(-35.273642641933,-1.82726854838893,304.989180911537));
#11212=CARTESIAN_POINT('Ctrl Pts',(-35.3705423976899,-1.74224616564757,
304.979764130925));
#11213=CARTESIAN_POINT('Ctrl Pts',(-35.5293607819236,-1.578216152808,304.9631006366));
#11214=CARTESIAN_POINT('Ctrl Pts',(-35.5940909633752,-1.50233693668429,
304.955864831576));
#11215=CARTESIAN_POINT('Ctrl Pts',(-35.6697542502341,-1.40140323059667,
304.947005728748));
#11216=CARTESIAN_POINT('Ctrl Pts',(-35.6852920996744,-1.37993566236092,
304.945162494972));
#11217=CARTESIAN_POINT('Ctrl Pts',(-35.7087735485585,-1.34632090606661,
304.942344465875));
#11218=CARTESIAN_POINT('Ctrl Pts',(-35.7169704430909,-1.33435435531888,
304.941354319121));
#11219=CARTESIAN_POINT('Ctrl Pts',(-35.732129446701,-1.3117825270777,304.939512094049));
#11220=CARTESIAN_POINT('Ctrl Pts',(-35.7391166861297,-1.30119598071789,
304.938658508707));
#11221=CARTESIAN_POINT('Ctrl Pts',(-35.7559077787892,-1.2753059491114,304.936595346927));
#11222=CARTESIAN_POINT('Ctrl Pts',(-35.7656212467673,-1.25994497923001,
304.935391565351));
#11223=CARTESIAN_POINT('Ctrl Pts',(-35.8015282977124,-1.20168946429857,
304.930896210252));
#11224=CARTESIAN_POINT('Ctrl Pts',(-35.8265346278844,-1.15807473979308,
304.927671513271));
#11225=CARTESIAN_POINT('Ctrl Pts',(-35.8926687857399,-1.03372682251686,
304.918771002815));
#11226=CARTESIAN_POINT('Ctrl Pts',(-35.9305866432221,-0.951382823163796,
304.913209131072));
#11227=CARTESIAN_POINT('Ctrl Pts',(-35.9833939359804,-0.816934037775414,
304.904355158999));
#11228=CARTESIAN_POINT('Ctrl Pts',(-36.0013710684059,-0.766145041210571,
304.901060175691));
#11229=CARTESIAN_POINT('Ctrl Pts',(-36.0524976455148,-0.604388754233415,
304.890619029732));
#11230=CARTESIAN_POINT('Ctrl Pts',(-36.0792572764916,-0.491594399928589,
304.883406527555));
#11231=CARTESIAN_POINT('Ctrl Pts',(-36.1030786734283,-0.34375945544675,
304.87373898335));
#11232=CARTESIAN_POINT('Ctrl Pts',(-36.1077623370245,-0.310102840630191,
304.871524785634));
#11233=CARTESIAN_POINT('Ctrl Pts',(-36.1141341230659,-0.255791724389269,
304.867924540332));
#11234=CARTESIAN_POINT('Ctrl Pts',(-36.1162775011514,-0.235194737764522,
304.866552931835));
#11235=CARTESIAN_POINT('Ctrl Pts',(-36.1200461649209,-0.193709186586245,
304.863776436969));
#11236=CARTESIAN_POINT('Ctrl Pts',(-36.1216649101111,-0.172821914907311,
304.862371474394));
#11237=CARTESIAN_POINT('Ctrl Pts',(-36.1245600991057,-0.127714479985215,
304.859321057913));
#11238=CARTESIAN_POINT('Ctrl Pts',(-36.1257421368948,-0.103490869569307,
304.857672795567));
#11239=CARTESIAN_POINT('Ctrl Pts',(-36.1274492786462,-0.052431689755752,
304.854176069068));
#11240=CARTESIAN_POINT('Ctrl Pts',(-36.1278907109207,-0.0255970923137018,
304.852325268517));
#11241=CARTESIAN_POINT('Ctrl Pts',(-36.1278767020865,0.00123812836145487,
304.850461017329));
#11242=CARTESIAN_POINT('Ctrl Pts',(-32.6699490794746,2.10841540797695,304.52294196412));
#11243=CARTESIAN_POINT('Ctrl Pts',(-32.7405091890633,2.14476537705674,304.528255476336));
#11244=CARTESIAN_POINT('Ctrl Pts',(-32.812932257405,2.17758811148641,304.533568988553));
#11245=CARTESIAN_POINT('Ctrl Pts',(-32.8868298076994,2.2066989849197,304.538882500769));
#11246=CARTESIAN_POINT('Ctrl Pts',(-32.9607171270794,2.23580582803188,304.544195277344));
#11247=CARTESIAN_POINT('Ctrl Pts',(-33.0360780865893,2.26120165971117,304.549508053919));
#11248=CARTESIAN_POINT('Ctrl Pts',(-33.1125046495563,2.28275016153689,304.554820830494));
#11249=CARTESIAN_POINT('Ctrl Pts',(-33.188944438043,2.30430239230347,304.560134526438));
#11250=CARTESIAN_POINT('Ctrl Pts',(-33.2664497444773,2.32200584587864,304.565448222382));
#11251=CARTESIAN_POINT('Ctrl Pts',(-33.3445992591608,2.33577459533907,304.570761918326));
#11252=CARTESIAN_POINT('Ctrl Pts',(-33.4228355339393,2.34955863060153,304.576081513434));
#11253=CARTESIAN_POINT('Ctrl Pts',(-33.501716981682,2.35939916406787,304.581401108542));
#11254=CARTESIAN_POINT('Ctrl Pts',(-33.5808147186556,2.36526185815733,304.58672070365));
#11255=CARTESIAN_POINT('Ctrl Pts',(-33.6599636679274,2.3711283480828,304.592043742961));
#11256=CARTESIAN_POINT('Ctrl Pts',(-33.7393287168723,2.37301186233046,304.597366782272));
#11257=CARTESIAN_POINT('Ctrl Pts',(-33.8184810139544,2.37093020618356,304.602689821583));
#11258=CARTESIAN_POINT('Ctrl Pts',(-33.8977626590998,2.3688451482631,304.608021559628));
#11259=CARTESIAN_POINT('Ctrl Pts',(-33.9768303922003,2.36278202619957,304.613353297674));
#11260=CARTESIAN_POINT('Ctrl Pts',(-34.055261151041,2.35281041252622,304.61868503572));
#11261=CARTESIAN_POINT('Ctrl Pts',(-34.082468715122,2.34935126815456,304.62053461115));
#11262=CARTESIAN_POINT('Ctrl Pts',(-34.1095997281322,2.34542222903315,304.62238418658));
#11263=CARTESIAN_POINT('Ctrl Pts',(-34.1366369059784,2.34102761478241,304.624233762011));
#11264=CARTESIAN_POINT('Ctrl Pts',(-34.2145896209335,2.32835720539376,304.629566397951));
#11265=CARTESIAN_POINT('Ctrl Pts',(-34.292056016926,2.3117650491669,304.634899033892));
#11266=CARTESIAN_POINT('Ctrl Pts',(-34.3686111942889,2.29130120350557,304.640231669832));
#11267=CARTESIAN_POINT('Ctrl Pts',(-34.4450558691736,2.2708668960902,304.645556608456));
#11268=CARTESIAN_POINT('Ctrl Pts',(-34.5205914884406,2.24657211742218,304.650881547079));
#11269=CARTESIAN_POINT('Ctrl Pts',(-34.5948014173447,2.21851827275714,304.656206485702));
#11270=CARTESIAN_POINT('Ctrl Pts',(-34.6689251554939,2.19049701109124,304.661525239702));
#11271=CARTESIAN_POINT('Ctrl Pts',(-34.7417258269051,2.15872552444736,304.666843993702));
#11272=CARTESIAN_POINT('Ctrl Pts',(-34.8128015615324,2.12335512500579,304.672162747702));
#11273=CARTESIAN_POINT('Ctrl Pts',(-34.8838320994485,2.08800721742789,304.677478119532));
#11274=CARTESIAN_POINT('Ctrl Pts',(-34.9531394592419,2.04906514768656,304.682793491362));
#11275=CARTESIAN_POINT('Ctrl Pts',(-35.0203425103695,2.00672800092669,304.688108863192));
#11276=CARTESIAN_POINT('Ctrl Pts',(-35.0875237492067,1.96440459565812,304.693422509796));
#11277=CARTESIAN_POINT('Ctrl Pts',(-35.1526016393793,1.91868855117903,304.698736156401));
#11278=CARTESIAN_POINT('Ctrl Pts',(-35.2152216968624,1.86982373548807,304.704049803005));
#11279=CARTESIAN_POINT('Ctrl Pts',(-35.2778409241516,1.82095956762904,304.709363379163));
#11280=CARTESIAN_POINT('Ctrl Pts',(-35.3380020148532,1.76894700092991,304.714676955321));
#11281=CARTESIAN_POINT('Ctrl Pts',(-35.3953825992675,1.7140709511503,304.719990531479));
#11282=CARTESIAN_POINT('Ctrl Pts',(-35.4528205361549,1.65914005220532,304.72530941861));
#11283=CARTESIAN_POINT('Ctrl Pts',(-35.5074720755336,1.60134027751406,304.730628305741));
#11284=CARTESIAN_POINT('Ctrl Pts',(-35.5590513093841,1.54099386377976,304.735947192872));
#11285=CARTESIAN_POINT('Ctrl Pts',(-35.6106552997318,1.48061848556279,304.74126863291));
#11286=CARTESIAN_POINT('Ctrl Pts',(-35.6591837602601,1.41769440490141,304.746590072949));
#11287=CARTESIAN_POINT('Ctrl Pts',(-35.7043923572474,1.35257541699771,304.751911512987));
#11288=CARTESIAN_POINT('Ctrl Pts',(-35.7496834151574,1.28733765142383,304.757242659384));
#11289=CARTESIAN_POINT('Ctrl Pts',(-35.7916422609772,1.21989737755875,304.762573805781));
#11290=CARTESIAN_POINT('Ctrl Pts',(-35.8300691345773,1.15063555902402,304.767904952178));
#11291=CARTESIAN_POINT('Ctrl Pts',(-35.8666859914183,1.08463617223471,304.772984986179));
#11292=CARTESIAN_POINT('Ctrl Pts',(-35.9000959840596,1.01698330734997,304.778065020179));
#11293=CARTESIAN_POINT('Ctrl Pts',(-35.930167366497,0.948022498237167,304.78314505418));
#11294=CARTESIAN_POINT('Ctrl Pts',(-35.9649442239047,0.868270919464904,
304.78901999586));
#11295=CARTESIAN_POINT('Ctrl Pts',(-35.9953692123839,0.7865113186969,304.79489493754));
#11296=CARTESIAN_POINT('Ctrl Pts',(-36.0212299042613,0.703211923981057,
304.800769879221));
#11297=CARTESIAN_POINT('Ctrl Pts',(-36.0470153730772,0.620154828872908,
304.806627731988));
#11298=CARTESIAN_POINT('Ctrl Pts',(-36.0682628988544,0.535567149082814,
304.812485584756));
#11299=CARTESIAN_POINT('Ctrl Pts',(-36.0848080894652,0.44993617736413,304.818343437524));
#11300=CARTESIAN_POINT('Ctrl Pts',(-36.1012716601613,0.364727636112995,
304.824172392622));
#11301=CARTESIAN_POINT('Ctrl Pts',(-36.1130790496947,0.278486353953334,
304.830001347721));
#11302=CARTESIAN_POINT('Ctrl Pts',(-36.1201162049507,0.191711295426038,
304.83583030282));
#11303=CARTESIAN_POINT('Ctrl Pts',(-36.1252509851141,0.128394396338522,
304.840083499165));
#11304=CARTESIAN_POINT('Ctrl Pts',(-36.1278470108903,0.0647937164408854,
304.84433669551));
#11305=CARTESIAN_POINT('Ctrl Pts',(-36.1278767663821,0.00110814072209554,
304.848589891855));
#11306=CARTESIAN_POINT('Ctrl Pts',(-32.6699490795102,2.1084154079953,304.328189117937));
#11307=CARTESIAN_POINT('Ctrl Pts',(-32.6782653702109,2.11269965459836,304.328799546289));
#11308=CARTESIAN_POINT('Ctrl Pts',(-32.6866072203208,2.11693480692552,304.329407472493));
#11309=CARTESIAN_POINT('Ctrl Pts',(-32.7878987226301,2.16760885279292,304.336739064943));
#11310=CARTESIAN_POINT('Ctrl Pts',(-32.8837883696344,2.20794568566654,304.343172787889));
#11311=CARTESIAN_POINT('Ctrl Pts',(-33.0768027562493,2.27459241156353,304.355714762328));
#11312=CARTESIAN_POINT('Ctrl Pts',(-33.1735598338358,2.30127513138037,304.361814774846));
#11313=CARTESIAN_POINT('Ctrl Pts',(-33.3646674478112,2.34114797902569,304.373905913891));
#11314=CARTESIAN_POINT('Ctrl Pts',(-33.4586918873183,2.35494030258137,304.379874473848));
#11315=CARTESIAN_POINT('Ctrl Pts',(-33.5855386775497,2.36582876944276,304.388111412626));
#11316=CARTESIAN_POINT('Ctrl Pts',(-33.6178462020658,2.36793673875129,304.390224760418));
#11317=CARTESIAN_POINT('Ctrl Pts',(-33.673001948259,2.3704029012557,304.393864174224));
#11318=CARTESIAN_POINT('Ctrl Pts',(-33.6958312191092,2.37109342852079,304.395379710148));
#11319=CARTESIAN_POINT('Ctrl Pts',(-33.7395502163077,2.37178403759726,304.398301118135));
#11320=CARTESIAN_POINT('Ctrl Pts',(-33.7604370354269,2.37183803984174,304.399705162552));
#11321=CARTESIAN_POINT('Ctrl Pts',(-33.815716729144,2.37125079020861,304.40344444518));
#11322=CARTESIAN_POINT('Ctrl Pts',(-33.8500985046813,2.37013720905983,304.405794065494));
#11323=CARTESIAN_POINT('Ctrl Pts',(-34.009584074951,2.36149613499397,304.416809794515));
#11324=CARTESIAN_POINT('Ctrl Pts',(-34.1339728372413,2.34480884998278,304.425750364261));
#11325=CARTESIAN_POINT('Ctrl Pts',(-34.3498712971519,2.29821687594208,304.441764539349));
#11326=CARTESIAN_POINT('Ctrl Pts',(-34.4419926339326,2.27242630110686,304.44875944352));
#11327=CARTESIAN_POINT('Ctrl Pts',(-34.6050449406822,2.21595622508672,304.461249137615));
#11328=CARTESIAN_POINT('Ctrl Pts',(-34.6765214481488,2.18723569282459,304.466762553553));
#11329=CARTESIAN_POINT('Ctrl Pts',(-34.7653883985863,2.1463975767723,304.473567401631));
#11330=CARTESIAN_POINT('Ctrl Pts',(-34.7841821124664,2.13745968116715,304.47500346471));
#11331=CARTESIAN_POINT('Ctrl Pts',(-34.8147838799986,2.12240910270798,304.477333941864));
#11332=CARTESIAN_POINT('Ctrl Pts',(-34.8266621392933,2.11644261226328,304.478236558375));
#11333=CARTESIAN_POINT('Ctrl Pts',(-34.8492344342421,2.10486580639192,304.479947140955));
#11334=CARTESIAN_POINT('Ctrl Pts',(-34.8599368787003,2.09927313469282,304.480756200937));
#11335=CARTESIAN_POINT('Ctrl Pts',(-34.8896707540121,2.08344512872126,304.482999673416));
#11336=CARTESIAN_POINT('Ctrl Pts',(-34.9086062511183,2.07303080166268,304.484423452954));
#11337=CARTESIAN_POINT('Ctrl Pts',(-35.0022685373012,2.01983739798276,304.491454615318));
#11338=CARTESIAN_POINT('Ctrl Pts',(-35.0747768219675,1.97326574074742,304.496862236112));
#11339=CARTESIAN_POINT('Ctrl Pts',(-35.262442986556,1.83775374427855,304.511199676449));
#11340=CARTESIAN_POINT('Ctrl Pts',(-35.3722143693567,1.74200713903659,304.519978661525));
#11341=CARTESIAN_POINT('Ctrl Pts',(-35.5273075093886,1.57937256221924,304.534004445851));
#11342=CARTESIAN_POINT('Ctrl Pts',(-35.5791617448385,1.51922365397991,304.539032010844));
#11343=CARTESIAN_POINT('Ctrl Pts',(-35.6467404985982,1.43238258076507,304.546170138496));
#11344=CARTESIAN_POINT('Ctrl Pts',(-35.6651085303727,1.40780987150087,304.548177175332));
#11345=CARTESIAN_POINT('Ctrl Pts',(-35.69613791137,1.36457465464386,304.551691179659));
#11346=CARTESIAN_POINT('Ctrl Pts',(-35.7090195187109,1.34607469175883,304.55318945473));
#11347=CARTESIAN_POINT('Ctrl Pts',(-35.7351778839948,1.30734130836825,304.556317085283));
#11348=CARTESIAN_POINT('Ctrl Pts',(-35.7484125244415,1.28708275278554,304.557947795987));
#11349=CARTESIAN_POINT('Ctrl Pts',(-35.7824705642847,1.23316514691137,304.562276423632));
#11350=CARTESIAN_POINT('Ctrl Pts',(-35.8027646302404,1.19918247371485,304.564993207242));
#11351=CARTESIAN_POINT('Ctrl Pts',(-35.9180435264787,0.994689985837558,
304.581284146611));
#11352=CARTESIAN_POINT('Ctrl Pts',(-35.9925213376725,0.813513936862788,
304.595574591462));
#11353=CARTESIAN_POINT('Ctrl Pts',(-36.0694956912709,0.531886809244084,
304.616846955885));
#11354=CARTESIAN_POINT('Ctrl Pts',(-36.0892866419849,0.436976204739904,
304.623848480326));
#11355=CARTESIAN_POINT('Ctrl Pts',(-36.106351258462,0.319559778493578,304.632124203974));
#11356=CARTESIAN_POINT('Ctrl Pts',(-36.1091867409673,0.297963852824,304.633630371095));
#11357=CARTESIAN_POINT('Ctrl Pts',(-36.1132862741035,0.263017176194256,
304.636038731036));
#11358=CARTESIAN_POINT('Ctrl Pts',(-36.1147352406086,0.249689944196646,
304.63695040773));
#11359=CARTESIAN_POINT('Ctrl Pts',(-36.1173987716898,0.223094788382456,
304.638755264668));
#11360=CARTESIAN_POINT('Ctrl Pts',(-36.1186146846707,0.209827597193498,
304.639648440372));
#11361=CARTESIAN_POINT('Ctrl Pts',(-36.1215173211892,0.174922339337079,
304.6419811052));
#11362=CARTESIAN_POINT('Ctrl Pts',(-36.1230190001543,0.153269499035327,
304.643410757257));
#11363=CARTESIAN_POINT('Ctrl Pts',(-36.1292740403634,0.0407106423377964,
304.650766703633));
#11364=CARTESIAN_POINT('Ctrl Pts',(-36.1290887556011,-0.0504029442347439,
304.656465858657));
#11365=CARTESIAN_POINT('Ctrl Pts',(-36.1152207116063,-0.282784969798882,
304.670847441797));
#11366=CARTESIAN_POINT('Ctrl Pts',(-36.0941094233503,-0.423236087679238,
304.679408260687));
#11367=CARTESIAN_POINT('Ctrl Pts',(-36.0420461705075,-0.637114207728523,
304.693141830167));
#11368=CARTESIAN_POINT('Ctrl Pts',(-36.0197471952671,-0.712293986752316,
304.698105324059));
#11369=CARTESIAN_POINT('Ctrl Pts',(-35.9836997356749,-0.814886906975633,
304.70515745996));
#11370=CARTESIAN_POINT('Ctrl Pts',(-35.9730804372024,-0.84334944200655,
304.707144348249));
#11371=CARTESIAN_POINT('Ctrl Pts',(-35.953717891521,-0.892351010473146,
304.710622477106));
#11372=CARTESIAN_POINT('Ctrl Pts',(-35.9452257807146,-0.912985499309556,
304.712105111559));
#11373=CARTESIAN_POINT('Ctrl Pts',(-35.9270259661663,-0.95549381598129,
304.715198536749));
#11374=CARTESIAN_POINT('Ctrl Pts',(-35.9172758425538,-0.977346591571641,
304.716810649339));
#11375=CARTESIAN_POINT('Ctrl Pts',(-35.8907519089747,-1.03445583109363,
304.721083360992));
#11376=CARTESIAN_POINT('Ctrl Pts',(-35.8734359034383,-1.06945082096291,
304.723762454098));
#11377=CARTESIAN_POINT('Ctrl Pts',(-35.7760425886514,-1.25463366573736,
304.738277710424));
#11378=CARTESIAN_POINT('Ctrl Pts',(-35.6808490184593,-1.39627745376366,
304.750647367382));
#11379=CARTESIAN_POINT('Ctrl Pts',(-35.5174280069754,-1.59060825631539,
304.769206123132));
#11380=CARTESIAN_POINT('Ctrl Pts',(-35.4601495707921,-1.65182453819164,
304.775322501833));
#11381=CARTESIAN_POINT('Ctrl Pts',(-35.365148622022,-1.74314400070019,304.784754506057));
#11382=CARTESIAN_POINT('Ctrl Pts',(-35.3295433634664,-1.7753487714525,304.788147926515));
#11383=CARTESIAN_POINT('Ctrl Pts',(-35.2793972033692,-1.81801104926626,
304.792710540428));
#11384=CARTESIAN_POINT('Ctrl Pts',(-35.2656813164995,-1.82941578158022,
304.79393723571));
#11385=CARTESIAN_POINT('Ctrl Pts',(-35.242056355216,-1.84861324599437,304.796012314442));
#11386=CARTESIAN_POINT('Ctrl Pts',(-35.2322117540529,-1.85648345259635,
304.796865975599));
#11387=CARTESIAN_POINT('Ctrl Pts',(-35.2108176840076,-1.87330902322722,
304.798697060663));
#11388=CARTESIAN_POINT('Ctrl Pts',(-35.1992475669361,-1.88223663214954,
304.799672625231));
#11389=CARTESIAN_POINT('Ctrl Pts',(-35.1660479879882,-1.90736762676136,
304.802432724611));
#11390=CARTESIAN_POINT('Ctrl Pts',(-35.1442223623002,-1.92330961392877,
304.804200509387));
#11391=CARTESIAN_POINT('Ctrl Pts',(-35.0332510231948,-2.0014925185186,304.81298351766));
#11392=CARTESIAN_POINT('Ctrl Pts',(-34.9401636307845,-2.05793111903594,
304.81970156455));
#11393=CARTESIAN_POINT('Ctrl Pts',(-34.687689332789,-2.18818119480047,304.837143681335));
#11394=CARTESIAN_POINT('Ctrl Pts',(-34.5234376639537,-2.25103824517571,
304.847783709351));
#11395=CARTESIAN_POINT('Ctrl Pts',(-34.3165794975337,-2.30490077680979,
304.861515704527));
#11396=CARTESIAN_POINT('Ctrl Pts',(-34.279166141357,-2.31367767379314,304.864009581738));
#11397=CARTESIAN_POINT('Ctrl Pts',(-34.2181698420588,-2.32643190467913,
304.868101127832));
#11398=CARTESIAN_POINT('Ctrl Pts',(-34.1947101383066,-2.33096841556767,
304.86968083311));
#11399=CARTESIAN_POINT('Ctrl Pts',(-34.1490178393951,-2.33908996220453,
304.872771351299));
#11400=CARTESIAN_POINT('Ctrl Pts',(-34.1267947776484,-2.34271432315199,
304.874280728407));
#11401=CARTESIAN_POINT('Ctrl Pts',(-34.0738119598627,-2.35058256274346,
304.877895701483));
#11402=CARTESIAN_POINT('Ctrl Pts',(-34.0430145325771,-2.35453976404966,
304.880010104894));
#11403=CARTESIAN_POINT('Ctrl Pts',(-33.92933447257,-2.36688327460594,304.887866950756));
#11404=CARTESIAN_POINT('Ctrl Pts',(-33.8461125575706,-2.37150523017019,
304.893723152976));
#11405=CARTESIAN_POINT('Ctrl Pts',(-33.5997387028622,-2.37220130939454,
304.911349754175));
#11406=CARTESIAN_POINT('Ctrl Pts',(-33.4370407070916,-2.35583818044118,
304.923395833102));
#11407=CARTESIAN_POINT('Ctrl Pts',(-33.2130306411181,-2.30966540822406,
304.939917123234));
#11408=CARTESIAN_POINT('Ctrl Pts',(-33.1493041784252,-2.29374706224781,
304.944603642607));
#11409=CARTESIAN_POINT('Ctrl Pts',(-33.0668620024144,-2.26947637416521,
304.950583508467));
#11410=CARTESIAN_POINT('Ctrl Pts',(-33.0474822819601,-2.2634999408469,304.951983013864));
#11411=CARTESIAN_POINT('Ctrl Pts',(-33.0169692056857,-2.2536598129924,304.954174142535));
#11412=CARTESIAN_POINT('Ctrl Pts',(-33.0057843972445,-2.24996061983072,
304.954974665781));
#11413=CARTESIAN_POINT('Ctrl Pts',(-32.9819992704595,-2.24189698191096,
304.956670663574));
#11414=CARTESIAN_POINT('Ctrl Pts',(-32.969407203646,-2.23750928501221,304.957564693609));
#11415=CARTESIAN_POINT('Ctrl Pts',(-32.9365109384593,-2.22573455791831,
304.959891866302));
#11416=CARTESIAN_POINT('Ctrl Pts',(-32.916268961524,-2.21817568436677,304.961315355593));
#11417=CARTESIAN_POINT('Ctrl Pts',(-32.808597695364,-2.17628317470362,304.968856047782));
#11418=CARTESIAN_POINT('Ctrl Pts',(-32.723153164064,-2.13705154587898,304.974731095106));
#11419=CARTESIAN_POINT('Ctrl Pts',(-32.4636178993085,-1.99867148540465,
304.992892552078));
#11420=CARTESIAN_POINT('Ctrl Pts',(-32.299630193214,-1.88251978712095,305.004913331659));
#11421=CARTESIAN_POINT('Ctrl Pts',(-32.1238352068006,-1.72113390130632,
305.020243514319));
#11422=CARTESIAN_POINT('Ctrl Pts',(-32.0961303474466,-1.69442888492212,
305.022740644329));
#11423=CARTESIAN_POINT('Ctrl Pts',(-32.0522926497168,-1.65006590312639,
305.026835639484));
#11424=CARTESIAN_POINT('Ctrl Pts',(-32.0357551809641,-1.63281649643271,
305.028415464109));
#11425=CARTESIAN_POINT('Ctrl Pts',(-32.0041593565324,-1.59884754969592,
305.031504857571));
#11426=CARTESIAN_POINT('Ctrl Pts',(-31.9890726985927,-1.58215774991069,
305.033012971713));
#11427=CARTESIAN_POINT('Ctrl Pts',(-31.953775998309,-1.54197569274489,305.036622484181));
#11428=CARTESIAN_POINT('Ctrl Pts',(-31.933784918249,-1.51829751615685,305.038732638446));
#11429=CARTESIAN_POINT('Ctrl Pts',(-31.8621103250249,-1.4299481424619,305.046549360928));
#11430=CARTESIAN_POINT('Ctrl Pts',(-31.8133637656336,-1.36298169787433,
305.052368260065));
#11431=CARTESIAN_POINT('Ctrl Pts',(-31.6808390316945,-1.15932954321583,
305.069749601049));
#11432=CARTESIAN_POINT('Ctrl Pts',(-31.6072905546142,-1.01654331702153,
305.08157710485));
#11433=CARTESIAN_POINT('Ctrl Pts',(-31.5233622624702,-0.80296940239596,
305.09818044733));
#11434=CARTESIAN_POINT('Ctrl Pts',(-31.5008572958237,-0.737399886432819,
305.103135582619));
#11435=CARTESIAN_POINT('Ctrl Pts',(-31.4754326355699,-0.651194797441105,
305.109393110757));
#11436=CARTESIAN_POINT('Ctrl Pts',(-31.4698679923482,-0.631380448433861,
305.110814094916));
#11437=CARTESIAN_POINT('Ctrl Pts',(-31.4615135451354,-0.600072342127738,
305.113029528886));
#11438=CARTESIAN_POINT('Ctrl Pts',(-31.4585507307447,-0.588626388530102,
305.113833241256));
#11439=CARTESIAN_POINT('Ctrl Pts',(-31.4524527635835,-0.564320948919424,
305.115526047765));
#11440=CARTESIAN_POINT('Ctrl Pts',(-31.4493394143139,-0.551456410201613,
305.116413804899));
#11441=CARTESIAN_POINT('Ctrl Pts',(-31.4415242031187,-0.517938668691449,
305.118707071989));
#11442=CARTESIAN_POINT('Ctrl Pts',(-31.4369908902023,-0.497246773233944,
305.120103415336));
#11443=CARTESIAN_POINT('Ctrl Pts',(-31.4155611911165,-0.392755688942494,
305.127070252656));
#11444=CARTESIAN_POINT('Ctrl Pts',(-31.402925106527,-0.308138556682372,
305.132440566156));
#11445=CARTESIAN_POINT('Ctrl Pts',(-31.3774455707182,-0.0383664983175095,
305.149221959223));
#11446=CARTESIAN_POINT('Ctrl Pts',(-31.3817245529169,0.147682064217546,
305.160345323115));
#11447=CARTESIAN_POINT('Ctrl Pts',(-31.4148545678939,0.38250795782754,305.175390393175));
#11448=CARTESIAN_POINT('Ctrl Pts',(-31.4237447799637,0.433429934434157,
305.178710369656));
#11449=CARTESIAN_POINT('Ctrl Pts',(-31.4397470918975,0.510193066831521,
305.183826441513));
#11450=CARTESIAN_POINT('Ctrl Pts',(-31.4456456356672,0.536272890233299,
305.185584278798));
#11451=CARTESIAN_POINT('Ctrl Pts',(-31.4572069649306,0.58365238906946,305.188816687164));
#11452=CARTESIAN_POINT('Ctrl Pts',(-31.4627281982615,0.604983734482728,
305.190286538057));
#11453=CARTESIAN_POINT('Ctrl Pts',(-31.4754843913659,0.651581025985171,
305.193530857604));
#11454=CARTESIAN_POINT('Ctrl Pts',(-31.4828436418333,0.676809588065451,
305.195309214568));
#11455=CARTESIAN_POINT('Ctrl Pts',(-31.5056773284675,0.750508331398769,
305.200570982667));
#11456=CARTESIAN_POINT('Ctrl Pts',(-31.5222931237489,0.798606291818543,
305.204090964883));
#11457=CARTESIAN_POINT('Ctrl Pts',(-31.5649753820951,0.910374560957247,
305.212479071801));
#11458=CARTESIAN_POINT('Ctrl Pts',(-31.5922898892316,0.973516730120223,
305.217382473062));
#11459=CARTESIAN_POINT('Ctrl Pts',(-31.661963929818,1.11710852273795,305.228896027504));
#11460=CARTESIAN_POINT('Ctrl Pts',(-31.7062826271992,1.19648953636735,305.235541049883));
#11461=CARTESIAN_POINT('Ctrl Pts',(-31.8104008333537,1.36014086664721,305.249702610231));
#11462=CARTESIAN_POINT('Ctrl Pts',(-31.8713805152212,1.44345694112722,305.257201538312));
#11463=CARTESIAN_POINT('Ctrl Pts',(-31.9546956097464,1.54296872142631,305.266318056573));
#11464=CARTESIAN_POINT('Ctrl Pts',(-31.9721393401096,1.56310450938407,305.268171349892));
#11465=CARTESIAN_POINT('Ctrl Pts',(-31.9996158306984,1.59376207571798,305.271000981311));
#11466=CARTESIAN_POINT('Ctrl Pts',(-32.0094116937441,1.60449204085024,305.271992878348));
#11467=CARTESIAN_POINT('Ctrl Pts',(-32.0279391648847,1.62441543461217,305.273836412733));
#11468=CARTESIAN_POINT('Ctrl Pts',(-32.036646388413,1.63362943530695,305.274689588707));
#11469=CARTESIAN_POINT('Ctrl Pts',(-32.0579744418754,1.65583936331158,305.276748532716));
#11470=CARTESIAN_POINT('Ctrl Pts',(-32.070670983612,1.66876126982694,305.277948572669));
#11471=CARTESIAN_POINT('Ctrl Pts',(-32.1187828322008,1.71661776585652,305.282406991744));
#11472=CARTESIAN_POINT('Ctrl Pts',(-32.1551486507734,1.7505832150299,305.285599973393));
#11473=CARTESIAN_POINT('Ctrl Pts',(-32.2594639823441,1.84204097850255,305.294371113383));
#11474=CARTESIAN_POINT('Ctrl Pts',(-32.3296216069873,1.89689206971494,305.299839352546));
#11475=CARTESIAN_POINT('Ctrl Pts',(-32.4882142663704,2.00709720902461,305.311679881417));
#11476=CARTESIAN_POINT('Ctrl Pts',(-32.5774941016077,2.06078602681652,305.318033273464));
#11477=CARTESIAN_POINT('Ctrl Pts',(-32.6699493942465,2.1084155701358,305.324530114841));
#11478=CARTESIAN_POINT('Origin',(-33.7561270252576,0.,302.151410108095));
#11479=CARTESIAN_POINT('',(-32.669949078383,2.10841540741462,306.520649966606));
#11480=CARTESIAN_POINT('',(-32.6699490794746,2.10841540797695,306.325637667994));
#11481=CARTESIAN_POINT('',(-32.6699490794746,2.10841540797695,302.151410108095));
#11482=CARTESIAN_POINT('Ctrl Pts',(-32.669949078383,2.10841540741463,306.520649966606));
#11483=CARTESIAN_POINT('Ctrl Pts',(-32.5859421857569,2.06513815102808,306.514515728316));
#11484=CARTESIAN_POINT('Ctrl Pts',(-32.5045827081745,2.0168715384183,306.508627603963));
#11485=CARTESIAN_POINT('Ctrl Pts',(-32.3148472989697,1.88839381620105,306.494506776106));
#11486=CARTESIAN_POINT('Ctrl Pts',(-32.2100159536117,1.80356823753118,306.486354837066));
#11487=CARTESIAN_POINT('Ctrl Pts',(-32.0577711477892,1.65729893463586,306.473166477512));
#11488=CARTESIAN_POINT('Ctrl Pts',(-32.0051979229085,1.60165476444168,306.46831540019));
#11489=CARTESIAN_POINT('Ctrl Pts',(-31.9357357856755,1.52062077854595,306.461390413495));
#11490=CARTESIAN_POINT('Ctrl Pts',(-31.9165040328186,1.49729720699368,306.459412475234));
#11491=CARTESIAN_POINT('Ctrl Pts',(-31.8838222108656,1.45608151120502,306.455939009056));
#11492=CARTESIAN_POINT('Ctrl Pts',(-31.8701696527893,1.43835441249426,306.454451825248));
#11493=CARTESIAN_POINT('Ctrl Pts',(-31.8423003634598,1.40108862068816,306.451337805631));
#11494=CARTESIAN_POINT('Ctrl Pts',(-31.828127392355,1.38152059509149,306.449709489951));
#11495=CARTESIAN_POINT('Ctrl Pts',(-31.7913812743704,1.32911983763755,306.445365087293));
#11496=CARTESIAN_POINT('Ctrl Pts',(-31.7693331422192,1.29593022202604,306.442629595394));
#11497=CARTESIAN_POINT('Ctrl Pts',(-31.6628690667612,1.12656021743971,306.428742083711));
#11498=CARTESIAN_POINT('Ctrl Pts',(-31.5915825217937,0.982648453125285,
306.417129796858));
#11499=CARTESIAN_POINT('Ctrl Pts',(-31.5041518157228,0.749468535102951,
306.398939522738));
#11500=CARTESIAN_POINT('Ctrl Pts',(-31.4776521538253,0.664566837404724,
306.392444829981));
#11501=CARTESIAN_POINT('Ctrl Pts',(-31.4438573478665,0.530167777379962,
306.382518418221));
#11502=CARTESIAN_POINT('Ctrl Pts',(-31.4332530967946,0.481587413090841,
306.379001225183));
#11503=CARTESIAN_POINT('Ctrl Pts',(-31.4208787636503,0.414899514617037,
306.374299549399));
#11504=CARTESIAN_POINT('Ctrl Pts',(-31.4177785956699,0.397055063656548,
306.373053721082));
#11505=CARTESIAN_POINT('Ctrl Pts',(-31.4128559983261,0.366660216980718,
306.37095443548));
#11506=CARTESIAN_POINT('Ctrl Pts',(-31.4109293093348,0.354127836868415,
306.370095456937));
#11507=CARTESIAN_POINT('Ctrl Pts',(-31.4070088490947,0.327190017686873,
306.368263792683));
#11508=CARTESIAN_POINT('Ctrl Pts',(-31.4050469147632,0.312780841765095,
306.367292825615));
#11509=CARTESIAN_POINT('Ctrl Pts',(-31.399862068979,0.271891595838558,306.364560059864));
#11510=CARTESIAN_POINT('Ctrl Pts',(-31.3969530595573,0.245373041082243,
306.362814491902));
#11511=CARTESIAN_POINT('Ctrl Pts',(-31.3849179393402,0.115476789763453,
306.354369901795));
#11512=CARTESIAN_POINT('Ctrl Pts',(-31.3821352098135,0.0116152235876252,
306.347941672039));
#11513=CARTESIAN_POINT('Ctrl Pts',(-31.3900120649434,-0.191066256825405,
306.335476703579));
#11514=CARTESIAN_POINT('Ctrl Pts',(-31.4000526275048,-0.289688486745452,
306.329446993958));
#11515=CARTESIAN_POINT('Ctrl Pts',(-31.4266668977316,-0.450441557810462,
306.31935132944));
#11516=CARTESIAN_POINT('Ctrl Pts',(-31.4396484641922,-0.513038324383106,
306.315352856988));
#11517=CARTESIAN_POINT('Ctrl Pts',(-31.4668583446621,-0.62191852468309,
306.308209808261));
#11518=CARTESIAN_POINT('Ctrl Pts',(-31.4800053625378,-0.668433549038073,
306.305096555846));
#11519=CARTESIAN_POINT('Ctrl Pts',(-31.50234046248,-0.739128291225599,306.300250648081));
#11520=CARTESIAN_POINT('Ctrl Pts',(-31.5105187371391,-0.763614975167525,
306.298550766854));
#11521=CARTESIAN_POINT('Ctrl Pts',(-31.5264254856782,-0.808774368515765,
306.295373301665));
#11522=CARTESIAN_POINT('Ctrl Pts',(-31.5340460137308,-0.829482282058013,
306.293899449051));
#11523=CARTESIAN_POINT('Ctrl Pts',(-31.5517420555133,-0.875574512768605,
306.290579590689));
#11524=CARTESIAN_POINT('Ctrl Pts',(-31.5619691863605,-0.900896826129921,
306.288728641907));
#11525=CARTESIAN_POINT('Ctrl Pts',(-31.589682078915,-0.966240930140267,
306.283879195033));
#11526=CARTESIAN_POINT('Ctrl Pts',(-31.6078394096627,-1.00596477487028,
306.28085854264));
#11527=CARTESIAN_POINT('Ctrl Pts',(-31.7181771697776,-1.23072794960111,
306.263339490632));
#11528=CARTESIAN_POINT('Ctrl Pts',(-31.8331349176203,-1.4035688354149,306.248063092413));
#11529=CARTESIAN_POINT('Ctrl Pts',(-32.0013349112842,-1.59634644848115,
306.229536840458));
#11530=CARTESIAN_POINT('Ctrl Pts',(-32.0348189527007,-1.63239591537284,
306.226002855252));
#11531=CARTESIAN_POINT('Ctrl Pts',(-32.0932396475318,-1.69149442552852,
306.220122446263));
#11532=CARTESIAN_POINT('Ctrl Pts',(-32.117593537376,-1.71509653322599,306.217748884753));
#11533=CARTESIAN_POINT('Ctrl Pts',(-32.1539925043496,-1.74888857310092,
306.214323717282));
#11534=CARTESIAN_POINT('Ctrl Pts',(-32.1656452705347,-1.75949256517752,
306.213244854934));
#11535=CARTESIAN_POINT('Ctrl Pts',(-32.1867381937233,-1.77830628013019,
306.211324776825));
#11536=CARTESIAN_POINT('Ctrl Pts',(-32.1961386417187,-1.78655836460439,
306.210480600691));
#11537=CARTESIAN_POINT('Ctrl Pts',(-32.2177381344329,-1.8052187640216,306.208566813081));
#11538=CARTESIAN_POINT('Ctrl Pts',(-32.2299780242117,-1.81557826269784,
306.207500654272));
#11539=CARTESIAN_POINT('Ctrl Pts',(-32.270451754839,-1.84913553923771,306.20403115786));
#11540=CARTESIAN_POINT('Ctrl Pts',(-32.2991181019938,-1.87180623836152,
306.201661702312));
#11541=CARTESIAN_POINT('Ctrl Pts',(-32.4843618834289,-2.01147006895618,
306.18681524043));
#11542=CARTESIAN_POINT('Ctrl Pts',(-32.6543842624245,-2.10940218869972,
306.175192372596));
#11543=CARTESIAN_POINT('Ctrl Pts',(-32.9163109393161,-2.21986215564156,
306.157537639525));
#11544=CARTESIAN_POINT('Ctrl Pts',(-32.9999738185638,-2.24973528604135,
306.151941586505));
#11545=CARTESIAN_POINT('Ctrl Pts',(-33.115442501059,-2.28379544737745,306.144145635967));
#11546=CARTESIAN_POINT('Ctrl Pts',(-33.1459516339184,-2.29213527986041,
306.142079543677));
#11547=CARTESIAN_POINT('Ctrl Pts',(-33.1985263609063,-2.30538284176792,
306.138503552515));
#11548=CARTESIAN_POINT('Ctrl Pts',(-33.2205125595828,-2.31058988832539,
306.137003503662));
#11549=CARTESIAN_POINT('Ctrl Pts',(-33.2656822936358,-2.3206082228344,306.133910656441));
#11550=CARTESIAN_POINT('Ctrl Pts',(-33.2888701246602,-2.32538802713199,
306.132317033865));
#11551=CARTESIAN_POINT('Ctrl Pts',(-33.3488620444505,-2.3368209025973,306.128177011067));
#11552=CARTESIAN_POINT('Ctrl Pts',(-33.3857576886613,-2.34295176486046,
306.12561439901));
#11553=CARTESIAN_POINT('Ctrl Pts',(-33.6262365606258,-2.37708957125409,
306.108796088669));
#11554=CARTESIAN_POINT('Ctrl Pts',(-33.8325529476159,-2.37940197182712,
306.093720019455));
#11555=CARTESIAN_POINT('Ctrl Pts',(-34.126972502786,-2.34434797367796,306.072136042513));
#11556=CARTESIAN_POINT('Ctrl Pts',(-34.2167289645676,-2.32837776913838,
306.065565053226));
#11557=CARTESIAN_POINT('Ctrl Pts',(-34.3262375765445,-2.30231034737386,
306.057716543538));
#11558=CARTESIAN_POINT('Ctrl Pts',(-34.3470553956057,-2.29705522775395,
306.056232348312));
#11559=CARTESIAN_POINT('Ctrl Pts',(-34.380648899234,-2.28808814338242,306.053853128423));
#11560=CARTESIAN_POINT('Ctrl Pts',(-34.393469273889,-2.28455024130282,306.052948901362));
#11561=CARTESIAN_POINT('Ctrl Pts',(-34.4191540553746,-2.27722923611528,
306.05114584765));
#11562=CARTESIAN_POINT('Ctrl Pts',(-34.4320174715421,-2.27344451513548,
306.050247145231));
#11563=CARTESIAN_POINT('Ctrl Pts',(-34.4658856509404,-2.2631668238753,306.047890616694));
#11564=CARTESIAN_POINT('Ctrl Pts',(-34.486833965104,-2.25649037965162,306.046442918235));
#11565=CARTESIAN_POINT('Ctrl Pts',(-34.6047302456006,-2.21710151706872,
306.038335284188));
#11566=CARTESIAN_POINT('Ctrl Pts',(-34.6995855484716,-2.17843006281214,
306.031963474114));
#11567=CARTESIAN_POINT('Ctrl Pts',(-34.9113097101002,-2.07567823304051,
306.01746871856));
#11568=CARTESIAN_POINT('Ctrl Pts',(-35.0258636949191,-2.00764917148078,
306.009410003655));
#11569=CARTESIAN_POINT('Ctrl Pts',(-35.196016047125,-1.88618734452235,305.996347629565));
#11570=CARTESIAN_POINT('Ctrl Pts',(-35.2557542629721,-1.83904853898069,
305.991524295012));
#11571=CARTESIAN_POINT('Ctrl Pts',(-35.3358804164165,-1.76931839192646,
305.984631950444));
#11572=CARTESIAN_POINT('Ctrl Pts',(-35.3582589062801,-1.74908022929873,
305.982657633036));
#11573=CARTESIAN_POINT('Ctrl Pts',(-35.3965439850316,-1.71310551705073,
305.979188325287));
#11574=CARTESIAN_POINT('Ctrl Pts',(-35.4126255547623,-1.69756027218825,
305.977701618089));
#11575=CARTESIAN_POINT('Ctrl Pts',(-35.4456331837544,-1.66473777929286,
305.974586456959));
#11576=CARTESIAN_POINT('Ctrl Pts',(-35.4625195510671,-1.64742447649363,
305.972956493689));
#11577=CARTESIAN_POINT('Ctrl Pts',(-35.5065962991275,-1.60082853033872,
305.968602387761));
#11578=CARTESIAN_POINT('Ctrl Pts',(-35.5333154085814,-1.57111290976394,
305.965858683439));
#11579=CARTESIAN_POINT('Ctrl Pts',(-35.6620786772266,-1.42041983279592,
305.952097224956));
#11580=CARTESIAN_POINT('Ctrl Pts',(-35.7525707753658,-1.29013223060072,
305.940632188562));
#11581=CARTESIAN_POINT('Ctrl Pts',(-35.8731574278445,-1.07307810265468,
305.922495958677));
#11582=CARTESIAN_POINT('Ctrl Pts',(-35.9123886869014,-0.991892828689847,
305.91590960323));
#11583=CARTESIAN_POINT('Ctrl Pts',(-35.9661029843121,-0.862388936626612,
305.905864771686));
#11584=CARTESIAN_POINT('Ctrl Pts',(-35.9838289698564,-0.815507983326928,
305.902318764643));
#11585=CARTESIAN_POINT('Ctrl Pts',(-36.0059387625847,-0.750916096054525,
305.89758579372));
#11586=CARTESIAN_POINT('Ctrl Pts',(-36.0116225368572,-0.733667421540767,
305.896336474399));
#11587=CARTESIAN_POINT('Ctrl Pts',(-36.0209395089188,-0.704260898569048,
305.894233216038));
#11588=CARTESIAN_POINT('Ctrl Pts',(-36.0246741966852,-0.692136375137347,
305.893373702854));
#11589=CARTESIAN_POINT('Ctrl Pts',(-36.0324735993946,-0.666074373641117,
305.891543112385));
#11590=CARTESIAN_POINT('Ctrl Pts',(-36.0365079058945,-0.652128717041853,
305.890573722865));
#11591=CARTESIAN_POINT('Ctrl Pts',(-36.0475598094166,-0.612567704092598,
305.887850082289));
#11592=CARTESIAN_POINT('Ctrl Pts',(-36.0542758042908,-0.586869431616941,
305.886111893029));
#11593=CARTESIAN_POINT('Ctrl Pts',(-36.0844985742969,-0.46273652068267,
305.877840317001));
#11594=CARTESIAN_POINT('Ctrl Pts',(-36.102123109679,-0.362968171454786,
305.87156408442));
#11595=CARTESIAN_POINT('Ctrl Pts',(-36.1229431829177,-0.1759154587442,305.859991865556));
#11596=CARTESIAN_POINT('Ctrl Pts',(-36.127802440045,-0.0889980115911998,
305.854690997065));
#11597=CARTESIAN_POINT('Ctrl Pts',(-36.1279659246806,0.103875004344682,
305.842791052475));
#11598=CARTESIAN_POINT('Ctrl Pts',(-36.120965002638,0.209636290981643,305.836170916785));
#11599=CARTESIAN_POINT('Ctrl Pts',(-36.1024399490108,0.348075470535023,
305.827151216386));
#11600=CARTESIAN_POINT('Ctrl Pts',(-36.0972406204719,0.381481081768892,
305.824947854604));
#11601=CARTESIAN_POINT('Ctrl Pts',(-36.0877118767881,0.435129918978208,
305.821359939336));
#11602=CARTESIAN_POINT('Ctrl Pts',(-36.0838282154977,0.455448229044223,
305.819989606697));
#11603=CARTESIAN_POINT('Ctrl Pts',(-36.0751208952325,0.497977929059514,
305.817095739372));
#11604=CARTESIAN_POINT('Ctrl Pts',(-36.070242749057,0.520175875309198,305.815570589025));
#11605=CARTESIAN_POINT('Ctrl Pts',(-36.057636892539,0.57384714034288,305.811845586991));
#11606=CARTESIAN_POINT('Ctrl Pts',(-36.0495818343527,0.605238024917801,
305.80963542613));
#11607=CARTESIAN_POINT('Ctrl Pts',(-36.0148728685773,0.729837443919163,
305.800731698052));
#11608=CARTESIAN_POINT('Ctrl Pts',(-35.9831617782423,0.821527477216697,
305.793879083827));
#11609=CARTESIAN_POINT('Ctrl Pts',(-35.9086552771279,1.00061965048489,305.779915052783));
#11610=CARTESIAN_POINT('Ctrl Pts',(-35.8659122748551,1.0878520503058,305.772816392382));
#11611=CARTESIAN_POINT('Ctrl Pts',(-35.7669961863955,1.26183644752888,305.758205094667));
#11612=CARTESIAN_POINT('Ctrl Pts',(-35.7102502153142,1.34804759267916,305.750709294088));
#11613=CARTESIAN_POINT('Ctrl Pts',(-35.6320043772519,1.45154808598281,305.74159551184));
#11614=CARTESIAN_POINT('Ctrl Pts',(-35.6155819954625,1.47252675604757,305.739742170307));
#11615=CARTESIAN_POINT('Ctrl Pts',(-35.5896585178091,1.50451705174639,305.736912108734));
#11616=CARTESIAN_POINT('Ctrl Pts',(-35.5804043233681,1.51572479714362,305.735919842129));
#11617=CARTESIAN_POINT('Ctrl Pts',(-35.5628833161761,1.53655152698258,305.734075669588));
#11618=CARTESIAN_POINT('Ctrl Pts',(-35.5546419090117,1.54618986876182,305.733222224587));
#11619=CARTESIAN_POINT('Ctrl Pts',(-35.5344335987826,1.56944331605833,305.731162297081));
#11620=CARTESIAN_POINT('Ctrl Pts',(-35.5223872628351,1.58298812865255,305.729961551632));
#11621=CARTESIAN_POINT('Ctrl Pts',(-35.4766481660143,1.6332445747544,305.725497050351));
#11622=CARTESIAN_POINT('Ctrl Pts',(-35.4419542858273,1.66903207742966,305.722298922237));
#11623=CARTESIAN_POINT('Ctrl Pts',(-35.3420568664534,1.76578231552372,305.713507004709));
#11624=CARTESIAN_POINT('Ctrl Pts',(-35.2745011740597,1.8241991677095,305.70802375722));
#11625=CARTESIAN_POINT('Ctrl Pts',(-35.0773840899219,1.97609527084552,305.692766908467));
#11626=CARTESIAN_POINT('Ctrl Pts',(-34.9414605609438,2.06049773492288,305.683032317465));
#11627=CARTESIAN_POINT('Ctrl Pts',(-34.7622727107826,2.14812926176825,305.670237655195));
#11628=CARTESIAN_POINT('Ctrl Pts',(-34.7260131489033,2.16474226498263,305.667652552869));
#11629=CARTESIAN_POINT('Ctrl Pts',(-34.6671345593397,2.18994234155288,305.663450776848));
#11630=CARTESIAN_POINT('Ctrl Pts',(-34.6447721295119,2.19911163713332,305.661854035819));
#11631=CARTESIAN_POINT('Ctrl Pts',(-34.6014474687311,2.21610737808209,305.658756758572));
#11632=CARTESIAN_POINT('Ctrl Pts',(-34.580506868106,2.22398209944306,305.657258049911));
#11633=CARTESIAN_POINT('Ctrl Pts',(-34.5310348788136,2.24179135665439,305.653711934233));
#11634=CARTESIAN_POINT('Ctrl Pts',(-34.5024194583771,2.25147909722816,305.651656585735));
#11635=CARTESIAN_POINT('Ctrl Pts',(-34.4008424240668,2.28371879329282,305.644342255474));
#11636=CARTESIAN_POINT('Ctrl Pts',(-34.3269913489357,2.30328921303756,305.638989361777));
#11637=CARTESIAN_POINT('Ctrl Pts',(-34.1212199201884,2.34731387183811,305.623986341933));
#11638=CARTESIAN_POINT('Ctrl Pts',(-33.9879743762071,2.36419466518143,305.61416025456));
#11639=CARTESIAN_POINT('Ctrl Pts',(-33.7532529304969,2.373892011994,305.597029142096));
#11640=CARTESIAN_POINT('Ctrl Pts',(-33.6523014203619,2.37162306320335,305.589724855603));
#11641=CARTESIAN_POINT('Ctrl Pts',(-33.5298977624896,2.3610381898577,305.581152138852));
#11642=CARTESIAN_POINT('Ctrl Pts',(-33.5080296976663,2.35884056619412,305.579631883657));
#11643=CARTESIAN_POINT('Ctrl Pts',(-33.4728752308131,2.35481341321378,305.577209494369));
#11644=CARTESIAN_POINT('Ctrl Pts',(-33.4595688447433,2.35317467649675,305.576297575623));
#11645=CARTESIAN_POINT('Ctrl Pts',(-33.4330896461668,2.34968547491862,305.574493784921));
#11646=CARTESIAN_POINT('Ctrl Pts',(-33.419917113684,2.34783685433853,305.573601861113));
#11647=CARTESIAN_POINT('Ctrl Pts',(-33.3855170966082,2.34271373261797,305.571285098924));
#11648=CARTESIAN_POINT('Ctrl Pts',(-33.364316755256,2.33926145292947,305.569869775426));
#11649=CARTESIAN_POINT('Ctrl Pts',(-33.2532968417066,2.31963115943838,305.562509799265));
#11650=CARTESIAN_POINT('Ctrl Pts',(-33.1644098621672,2.29856508625893,305.556793753889));
#11651=CARTESIAN_POINT('Ctrl Pts',(-32.9363808009395,2.23041226216226,305.542085719435));
#11652=CARTESIAN_POINT('Ctrl Pts',(-32.8001418803171,2.1754859432645,305.533235699134));
#11653=CARTESIAN_POINT('Ctrl Pts',(-32.6699490731214,2.10841540470401,305.524079281032));
#11654=CARTESIAN_POINT('',(-36.1278766586888,0.00131864288668422,305.651410108095));
#11655=CARTESIAN_POINT('Ctrl Pts',(-32.6699493942465,2.1084155701358,305.324530114841));
#11656=CARTESIAN_POINT('Ctrl Pts',(-32.7195768807531,2.13398181357011,305.328017442592));
#11657=CARTESIAN_POINT('Ctrl Pts',(-32.7701193673887,2.15780226145263,305.331544844162));
#11658=CARTESIAN_POINT('Ctrl Pts',(-32.8581171958471,2.19553294598891,305.33768650562));
#11659=CARTESIAN_POINT('Ctrl Pts',(-32.8951363359132,2.21031249032801,305.340270124394));
#11660=CARTESIAN_POINT('Ctrl Pts',(-32.9551696417961,2.23254322985126,305.344470151115));
#11661=CARTESIAN_POINT('Ctrl Pts',(-32.9779568722895,2.24058767821185,305.346066661418));
#11662=CARTESIAN_POINT('Ctrl Pts',(-33.0220727349457,2.25540750425207,305.349163938566));
#11663=CARTESIAN_POINT('Ctrl Pts',(-33.0433822310108,2.26223197533106,305.350662884598));
#11664=CARTESIAN_POINT('Ctrl Pts',(-33.0936966447019,2.27756395891887,305.354210295848));
#11665=CARTESIAN_POINT('Ctrl Pts',(-33.12277335312,2.28582032858097,305.356266716568));
#11666=CARTESIAN_POINT('Ctrl Pts',(-33.2259568644129,2.31299956258742,305.363590255575));
#11667=CARTESIAN_POINT('Ctrl Pts',(-33.3008061838628,2.32888988597712,305.368951590077));
#11668=CARTESIAN_POINT('Ctrl Pts',(-33.509063948275,2.36267900777135,305.383994759033));
#11669=CARTESIAN_POINT('Ctrl Pts',(-33.6434255365436,2.37288537119634,305.393853831767));
#11670=CARTESIAN_POINT('Ctrl Pts',(-33.8781237761705,2.37072938042785,305.41096735164));
#11671=CARTESIAN_POINT('Ctrl Pts',(-33.9781856953145,2.36345828355269,305.418222840254));
#11672=CARTESIAN_POINT('Ctrl Pts',(-34.0992646054196,2.34689952656979,305.426749717038));
#11673=CARTESIAN_POINT('Ctrl Pts',(-34.1209915457414,2.34362001095034,305.428269590526));
#11674=CARTESIAN_POINT('Ctrl Pts',(-34.1558978222545,2.33785395229119,305.430691603334));
#11675=CARTESIAN_POINT('Ctrl Pts',(-34.169106564501,2.33555683188511,305.431603517906));
#11676=CARTESIAN_POINT('Ctrl Pts',(-34.1953817134525,2.3307574612693,305.433407411194));
#11677=CARTESIAN_POINT('Ctrl Pts',(-34.208447926001,2.32825704056831,305.43429943965));
#11678=CARTESIAN_POINT('Ctrl Pts',(-34.2425615476118,2.32143084862783,305.436616876364));
#11679=CARTESIAN_POINT('Ctrl Pts',(-34.2635729825365,2.31692865894822,305.438032759862));
#11680=CARTESIAN_POINT('Ctrl Pts',(-34.3736798250611,2.29176591605543,305.445405903074));
#11681=CARTESIAN_POINT('Ctrl Pts',(-34.4615957309223,2.26624803299343,305.451133574464));
#11682=CARTESIAN_POINT('Ctrl Pts',(-34.7408377638245,2.16736421187913,305.469439474914));
#11683=CARTESIAN_POINT('Ctrl Pts',(-34.9241705581056,2.07431766408141,305.481717622589));
#11684=CARTESIAN_POINT('Ctrl Pts',(-35.1242853600399,1.93771784646349,305.497297234415));
#11685=CARTESIAN_POINT('Ctrl Pts',(-35.1547861086452,1.91581841452697,305.499735793412));
#11686=CARTESIAN_POINT('Ctrl Pts',(-35.2036736582598,1.87892752774865,305.503759018806));
#11687=CARTESIAN_POINT('Ctrl Pts',(-35.2223786762482,1.86436743602134,305.505326837107));
#11688=CARTESIAN_POINT('Ctrl Pts',(-35.2584678116655,1.83539640179127,305.508409952337));
#11689=CARTESIAN_POINT('Ctrl Pts',(-35.2758705904157,1.82101269222123,305.509924047344));
#11690=CARTESIAN_POINT('Ctrl Pts',(-35.3170782708204,1.78595166804947,305.513577148768));
#11691=CARTESIAN_POINT('Ctrl Pts',(-35.3406808016547,1.76504428104584,305.515725505224));
#11692=CARTESIAN_POINT('Ctrl Pts',(-35.428436535069,1.68413024192097,305.52393295459));
#11693=CARTESIAN_POINT('Ctrl Pts',(-35.4896491678435,1.62105258684898,305.530120152592));
#11694=CARTESIAN_POINT('Ctrl Pts',(-35.6709507099456,1.41218872643857,305.549953012934));
#11695=CARTESIAN_POINT('Ctrl Pts',(-35.777215392898,1.2553971505819,305.563985155322));
#11696=CARTESIAN_POINT('Ctrl Pts',(-35.8826613653697,1.05106930596526,305.580369580621));
#11697=CARTESIAN_POINT('Ctrl Pts',(-35.9005971175389,1.01397410522387,305.583271377605));
#11698=CARTESIAN_POINT('Ctrl Pts',(-35.9240485500601,0.962061761883848,
305.587215089976));
#11699=CARTESIAN_POINT('Ctrl Pts',(-35.9303953447993,0.947630666368683,
305.588299131218));
#11700=CARTESIAN_POINT('Ctrl Pts',(-35.9415781457625,0.921499695257981,
305.590238643671));
#11701=CARTESIAN_POINT('Ctrl Pts',(-35.9464652518913,0.9098223853355,305.591097004448));
#11702=CARTESIAN_POINT('Ctrl Pts',(-35.9566272859836,0.884984548943407,
305.592904421192));
#11703=CARTESIAN_POINT('Ctrl Pts',(-35.9618780728703,0.871814998228795,
305.593852091933));
#11704=CARTESIAN_POINT('Ctrl Pts',(-35.9762990463627,0.834681128292523,
305.596496519875));
#11705=CARTESIAN_POINT('Ctrl Pts',(-35.9851992106731,0.810613170955293,
305.598178312866));
#11706=CARTESIAN_POINT('Ctrl Pts',(-36.0433604898388,0.645125094243305,
305.609554450537));
#11707=CARTESIAN_POINT('Ctrl Pts',(-36.0795280818733,0.499442076294542,
305.61865449061));
#11708=CARTESIAN_POINT('Ctrl Pts',(-36.1190741471813,0.235401644859499,
305.635020122626));
#11709=CARTESIAN_POINT('Ctrl Pts',(-36.1278170067582,0.118383906896199,
305.642229472726));
#11710=CARTESIAN_POINT('Ctrl Pts',(-36.1278767173156,0.00120860362354279,
305.649679341437));
#11711=CARTESIAN_POINT('Ctrl Pts',(-36.1278766586888,0.00131864288668422,
305.651410108095));
#11712=CARTESIAN_POINT('Ctrl Pts',(-36.1279213776981,-0.0791142741799706,
305.656783719909));
#11713=CARTESIAN_POINT('Ctrl Pts',(-36.1238701842287,-0.159550669184445,
305.662157331723));
#11714=CARTESIAN_POINT('Ctrl Pts',(-36.1157484705838,-0.239551032677529,
305.667530943537));
#11715=CARTESIAN_POINT('Ctrl Pts',(-36.1076245801917,-0.319572837528005,
305.672905995564));
#11716=CARTESIAN_POINT('Ctrl Pts',(-36.0954280477296,-0.399157927229441,
305.678281047591));
#11717=CARTESIAN_POINT('Ctrl Pts',(-36.079236009608,-0.477873110072393,
305.683656099617));
#11718=CARTESIAN_POINT('Ctrl Pts',(-36.0630218193141,-0.556695982403609,
305.689038505201));
#11719=CARTESIAN_POINT('Ctrl Pts',(-36.0428012976816,-0.63464612534666,
305.694420910785));
#11720=CARTESIAN_POINT('Ctrl Pts',(-36.0187024588884,-0.711301953905909,
305.699803316369));
#11721=CARTESIAN_POINT('Ctrl Pts',(-35.9945873950798,-0.788009392503775,
305.705189345763));
#11722=CARTESIAN_POINT('Ctrl Pts',(-35.9665889709448,-0.863420355153572,
305.710575375157));
#11723=CARTESIAN_POINT('Ctrl Pts',(-35.9348838261372,-0.937132255938665,
305.715961404551));
#11724=CARTESIAN_POINT('Ctrl Pts',(-35.9031124904097,-1.0109980452665,305.721358678373));
#11725=CARTESIAN_POINT('Ctrl Pts',(-35.8676191689213,-1.08315727524832,
305.726755952196));
#11726=CARTESIAN_POINT('Ctrl Pts',(-35.8286271023704,-1.15323089312922,
305.732153226018));
#11727=CARTESIAN_POINT('Ctrl Pts',(-35.7904076459934,-1.2219160339456,305.7374435553));
#11728=CARTESIAN_POINT('Ctrl Pts',(-35.7488271282622,-1.28859716976929,
305.742733884581));
#11729=CARTESIAN_POINT('Ctrl Pts',(-35.7041344894103,-1.35294677726268,
305.748024213863));
#11730=CARTESIAN_POINT('Ctrl Pts',(-35.6590907331093,-1.41780193266302,
305.753356105401));
#11731=CARTESIAN_POINT('Ctrl Pts',(-35.6107192482689,-1.48052804985976,
305.758687996939));
#11732=CARTESIAN_POINT('Ctrl Pts',(-35.559248273395,-1.54076339099012,305.764019888477));
#11733=CARTESIAN_POINT('Ctrl Pts',(-35.5078517500581,-1.60091160313684,
305.769344067561));
#11734=CARTESIAN_POINT('Ctrl Pts',(-35.4533649419751,-1.6585758405409,305.774668246645));
#11735=CARTESIAN_POINT('Ctrl Pts',(-35.3960588605108,-1.71342395168949,
305.779992425729));
#11736=CARTESIAN_POINT('Ctrl Pts',(-35.3388195537606,-1.76820815222248,
305.785310400924));
#11737=CARTESIAN_POINT('Ctrl Pts',(-35.2787678387905,-1.82018242492944,
305.79062837612));
#11738=CARTESIAN_POINT('Ctrl Pts',(-35.2162133962421,-1.86904945139643,
305.795946351316));
#11739=CARTESIAN_POINT('Ctrl Pts',(-35.1536988713225,-1.91788529453343,
305.801260932972));
#11740=CARTESIAN_POINT('Ctrl Pts',(-35.0886851571728,-1.96361753912731,
305.806575514628));
#11741=CARTESIAN_POINT('Ctrl Pts',(-35.021516102623,-2.0059881717957,305.811890096285));
#11742=CARTESIAN_POINT('Ctrl Pts',(-34.954368982389,-2.04834496816933,305.817202942444));
#11743=CARTESIAN_POINT('Ctrl Pts',(-34.8850683155989,-2.08734208247314,
305.822515788603));
#11744=CARTESIAN_POINT('Ctrl Pts',(-34.8139868734757,-2.12276484897125,
305.827828634762));
#11745=CARTESIAN_POINT('Ctrl Pts',(-34.7429064967397,-2.15818708454371,
305.833141401291));
#11746=CARTESIAN_POINT('Ctrl Pts',(-34.6700458179381,-2.19003487088063,
305.838454167819));
#11747=CARTESIAN_POINT('Ctrl Pts',(-34.5958008016666,-2.21814021461921,
305.843766934348));
#11748=CARTESIAN_POINT('Ctrl Pts',(-34.521481688898,-2.24627360747983,305.849085003016));
#11749=CARTESIAN_POINT('Ctrl Pts',(-34.4457759183066,-2.27065693028045,
305.854403071683));
#11750=CARTESIAN_POINT('Ctrl Pts',(-34.3690974088338,-2.29117117897341,
305.859721140351));
#11751=CARTESIAN_POINT('Ctrl Pts',(-34.2923821790316,-2.3116952516702,305.865041755772));
#11752=CARTESIAN_POINT('Ctrl Pts',(-34.2146937413942,-2.32834646070103,
305.870362371193));
#11753=CARTESIAN_POINT('Ctrl Pts',(-34.1364565640286,-2.34105692037555,
305.875682986613));
#11754=CARTESIAN_POINT('Ctrl Pts',(-34.0580766698169,-2.35379056591616,
305.881013307669));
#11755=CARTESIAN_POINT('Ctrl Pts',(-33.9791465028503,-2.3625690456559,305.886343628724));
#11756=CARTESIAN_POINT('Ctrl Pts',(-33.900095825025,-2.3673764058961,305.891673949779));
#11757=CARTESIAN_POINT('Ctrl Pts',(-33.8246509406918,-2.37196448467352,
305.896761135197));
#11758=CARTESIAN_POINT('Ctrl Pts',(-33.749096658507,-2.37293585714187,305.901848320614));
#11759=CARTESIAN_POINT('Ctrl Pts',(-33.6738031839495,-2.37032083221919,
305.906935506032));
#11760=CARTESIAN_POINT('Ctrl Pts',(-33.5948879495595,-2.36758001960665,
305.912267394777));
#11761=CARTESIAN_POINT('Ctrl Pts',(-33.5159602124537,-2.36088871336514,
305.917599283523));
#11762=CARTESIAN_POINT('Ctrl Pts',(-33.4374476763346,-2.35024286725224,
305.922931172269));
#11763=CARTESIAN_POINT('Ctrl Pts',(-33.359048705301,-2.33961241990854,305.928255348661));
#11764=CARTESIAN_POINT('Ctrl Pts',(-33.2810642032751,-2.32503885442818,
305.933579525054));
#11765=CARTESIAN_POINT('Ctrl Pts',(-33.2039201677124,-2.30657010493505,
305.938903701446));
#11766=CARTESIAN_POINT('Ctrl Pts',(-33.1268660202592,-2.28812287519991,
305.944221674117));
#11767=CARTESIAN_POINT('Ctrl Pts',(-33.0506508467579,-2.26578958936141,
305.949539646787));
#11768=CARTESIAN_POINT('Ctrl Pts',(-32.9756923053248,-2.2396695538457,305.954857619458));
#11769=CARTESIAN_POINT('Ctrl Pts',(-32.9007815954792,-2.21356618571358,
305.960172198691));
#11770=CARTESIAN_POINT('Ctrl Pts',(-32.8271263676736,-2.18368101780014,
305.965486777925));
#11771=CARTESIAN_POINT('Ctrl Pts',(-32.7551297436213,-2.1501633669693,305.970801357159));
#11772=CARTESIAN_POINT('Ctrl Pts',(-32.6831566289195,-2.11665666079334,
305.976114201001));
#11773=CARTESIAN_POINT('Ctrl Pts',(-32.6128414672458,-2.07952002472724,
305.981427044843));
#11774=CARTESIAN_POINT('Ctrl Pts',(-32.5445666044412,-2.03895056566143,
305.986739888686));
#11775=CARTESIAN_POINT('Ctrl Pts',(-32.4762927635464,-1.99838171382254,
305.992052653008));
#11776=CARTESIAN_POINT('Ctrl Pts',(-32.4100595631882,-1.95438038175849,
305.99736541733));
#11777=CARTESIAN_POINT('Ctrl Pts',(-32.346222675646,-1.90718845095239,306.002678181652));
#11778=CARTESIAN_POINT('Ctrl Pts',(-32.2823220765991,-1.85994942090588,
306.007996248304));
#11779=CARTESIAN_POINT('Ctrl Pts',(-32.2208229458303,-1.80951371035004,
306.013314314955));
#11780=CARTESIAN_POINT('Ctrl Pts',(-32.1620494969452,-1.75616482604265,
306.018632381606));
#11781=CARTESIAN_POINT('Ctrl Pts',(-32.1032479011064,-1.7027903926378,306.023952995112));
#11782=CARTESIAN_POINT('Ctrl Pts',(-32.0471749189374,-1.64650033876582,
306.029273608617));
#11783=CARTESIAN_POINT('Ctrl Pts',(-31.99411750502,-1.58761472438755,306.034594222122));
#11784=CARTESIAN_POINT('Ctrl Pts',(-31.9409633040926,-1.52862169123154,
306.039924541458));
#11785=CARTESIAN_POINT('Ctrl Pts',(-31.8908359604425,-1.46702400086003,
306.045254860794));
#11786=CARTESIAN_POINT('Ctrl Pts',(-31.8439816394093,-1.40317428920256,
306.050585180129));
#11787=CARTESIAN_POINT('Ctrl Pts',(-31.7992643215169,-1.34223673231215,
306.055672386153));
#11788=CARTESIAN_POINT('Ctrl Pts',(-31.7575281364002,-1.27924842454727,
306.060759592177));
#11789=CARTESIAN_POINT('Ctrl Pts',(-31.7189481061582,-1.21453699576303,
306.065846798201));
#11790=CARTESIAN_POINT('Ctrl Pts',(-31.6785125504094,-1.14671323902197,
306.071178675898));
#11791=CARTESIAN_POINT('Ctrl Pts',(-31.6413911575609,-1.07673942831649,
306.076510553594));
#11792=CARTESIAN_POINT('Ctrl Pts',(-31.6078189698145,-1.00497291576352,
306.081842431291));
#11793=CARTESIAN_POINT('Ctrl Pts',(-31.5742953443195,-0.933310213645913,
306.087166596414));
#11794=CARTESIAN_POINT('Ctrl Pts',(-31.5443109256388,-0.859860380399543,
306.092490761536));
#11795=CARTESIAN_POINT('Ctrl Pts',(-31.5180561351155,-0.785007486077892,
306.097814926659));
#11796=CARTESIAN_POINT('Ctrl Pts',(-31.4918319380809,-0.710241814359655,
306.103132887779));
#11797=CARTESIAN_POINT('Ctrl Pts',(-31.4693288871985,-0.634076770637978,
306.108450848899));
#11798=CARTESIAN_POINT('Ctrl Pts',(-31.4506897016496,-0.556917237491704,
306.113768810019));
#11799=CARTESIAN_POINT('Ctrl Pts',(-31.4320624105057,-0.479806942909443,
306.119083377537));
#11800=CARTESIAN_POINT('Ctrl Pts',(-31.4172942005321,-0.401703873022735,
306.124397945055));
#11801=CARTESIAN_POINT('Ctrl Pts',(-31.4064778772932,-0.323027775849396,
306.129712512573));
#11802=CARTESIAN_POINT('Ctrl Pts',(-31.3956650862638,-0.244377371367967,
306.13502534455));
#11803=CARTESIAN_POINT('Ctrl Pts',(-31.3888016831451,-0.165154775304011,
306.140338176528));
#11804=CARTESIAN_POINT('Ctrl Pts',(-31.3859290471889,-0.085788153373663,
306.145651008505));
#11805=CARTESIAN_POINT('Ctrl Pts',(-31.3830564543013,-0.00642272136167781,
306.150963760829));
#11806=CARTESIAN_POINT('Ctrl Pts',(-31.3841745252713,0.073086263643561,
306.156276513153));
#11807=CARTESIAN_POINT('Ctrl Pts',(-31.3892725537851,0.15230880923493,306.161589265477));
#11808=CARTESIAN_POINT('Ctrl Pts',(-31.3943756702046,0.231610420064857,
306.166907320004));
#11809=CARTESIAN_POINT('Ctrl Pts',(-31.4034666487077,0.310624551427704,
306.172225374531));
#11810=CARTESIAN_POINT('Ctrl Pts',(-31.4164827532814,0.38892511246911,306.177543429058));
#11811=CARTESIAN_POINT('Ctrl Pts',(-31.429505091142,0.467263170893507,306.18286403035));
#11812=CARTESIAN_POINT('Ctrl Pts',(-31.4464561995775,0.544886519556357,
306.188184631642));
#11813=CARTESIAN_POINT('Ctrl Pts',(-31.4672224352513,0.621380592188205,
306.193505232934));
#11814=CARTESIAN_POINT('Ctrl Pts',(-31.4880265526266,0.698014205065533,
306.19883554005));
#11815=CARTESIAN_POINT('Ctrl Pts',(-31.5126595583196,0.773513978588081,
306.204165847166));
#11816=CARTESIAN_POINT('Ctrl Pts',(-31.5409583331658,0.847481992773977,
306.209496154282));
#11817=CARTESIAN_POINT('Ctrl Pts',(-31.5679670391485,0.91807799412496,306.214583466311));
#11818=CARTESIAN_POINT('Ctrl Pts',(-31.5983143888503,0.987278539532674,
306.219670778341));
#11819=CARTESIAN_POINT('Ctrl Pts',(-31.6318197407079,1.0547590356613,306.22475809037));
#11820=CARTESIAN_POINT('Ctrl Pts',(-31.6669302309801,1.12547231492948,306.230089119881));
#11821=CARTESIAN_POINT('Ctrl Pts',(-31.70564191788,1.19456452682633,306.235420149392));
#11822=CARTESIAN_POINT('Ctrl Pts',(-31.7477817782138,1.26164473255218,306.240751178903));
#11823=CARTESIAN_POINT('Ctrl Pts',(-31.7898643495412,1.32863374295119,306.246074960896));
#11824=CARTESIAN_POINT('Ctrl Pts',(-31.8353655959063,1.39361578338627,306.251398742889));
#11825=CARTESIAN_POINT('Ctrl Pts',(-31.8840658378854,1.45622284463428,306.256722524882));
#11826=CARTESIAN_POINT('Ctrl Pts',(-31.9327150532832,1.51876430817316,306.262040728784));
#11827=CARTESIAN_POINT('Ctrl Pts',(-31.9845563219832,1.57893536591941,306.267358932686));
#11828=CARTESIAN_POINT('Ctrl Pts',(-32.0393265503279,1.63639670978073,306.272677136587));
#11829=CARTESIAN_POINT('Ctrl Pts',(-32.094058522837,1.69381791811966,306.277991625837));
#11830=CARTESIAN_POINT('Ctrl Pts',(-32.1517150689476,1.74853283334435,306.283306115087));
#11831=CARTESIAN_POINT('Ctrl Pts',(-32.2119936138942,1.80023611518357,306.288620604337));
#11832=CARTESIAN_POINT('Ctrl Pts',(-32.2722481476732,1.85191880169874,306.29393297663));
#11833=CARTESIAN_POINT('Ctrl Pts',(-32.3351222478881,1.90059193545501,306.299245348923));
#11834=CARTESIAN_POINT('Ctrl Pts',(-32.4002784866108,1.94598890098306,306.304557721215));
#11835=CARTESIAN_POINT('Ctrl Pts',(-32.4654418309203,1.99139081725853,306.309870672847));
#11836=CARTESIAN_POINT('Ctrl Pts',(-32.5328874271204,2.03351558229234,306.315183624478));
#11837=CARTESIAN_POINT('Ctrl Pts',(-32.6022479731971,2.07213927999928,306.32049657611));
#11838=CARTESIAN_POINT('Ctrl Pts',(-32.624620279292,2.08459738819613,306.322210273404));
#11839=CARTESIAN_POINT('Ctrl Pts',(-32.6471916083291,2.09669159721057,306.323923970699));
#11840=CARTESIAN_POINT('Ctrl Pts',(-32.6699490794746,2.10841540797695,306.325637667993));
#11841=CARTESIAN_POINT('Origin',(-33.7561270252576,0.,302.151410108095));
#11842=CARTESIAN_POINT('',(-32.669948905789,2.10841531850051,307.52304986714));
#11843=CARTESIAN_POINT('',(-32.6683119391961,2.11155019427352,307.325629814339));
#11844=CARTESIAN_POINT('',(-32.6699490794746,2.10841540797695,302.151410108095));
#11845=CARTESIAN_POINT('',(-36.127877017276,-0.000194578459783513,306.846254750936));
#11846=CARTESIAN_POINT('Ctrl Pts',(-32.669948905789,2.10841531850051,307.52304986714));
#11847=CARTESIAN_POINT('Ctrl Pts',(-32.6291536046931,2.08739907799101,307.519703664692));
#11848=CARTESIAN_POINT('Ctrl Pts',(-32.5889626779185,2.06519595461221,307.516347061658));
#11849=CARTESIAN_POINT('Ctrl Pts',(-32.463472090138,1.99103245979216,307.505708193501));
#11850=CARTESIAN_POINT('Ctrl Pts',(-32.3808016729988,1.93485161061858,307.498456265159));
#11851=CARTESIAN_POINT('Ctrl Pts',(-32.2809745266202,1.85737063800947,307.489581439048));
#11852=CARTESIAN_POINT('Ctrl Pts',(-32.2603089829766,1.84076861973144,307.48773765135));
#11853=CARTESIAN_POINT('Ctrl Pts',(-32.2287706654417,1.8145498124291,307.484918969574));
#11854=CARTESIAN_POINT('Ctrl Pts',(-32.2177012029804,1.80517436519654,307.483928713116));
#11855=CARTESIAN_POINT('Ctrl Pts',(-32.1971102178872,1.78740753440575,307.482086024239));
#11856=CARTESIAN_POINT('Ctrl Pts',(-32.1875694449029,1.77904081578627,307.48123208744));
#11857=CARTESIAN_POINT('Ctrl Pts',(-32.1645217353442,1.75849972073287,307.479167942608));
#11858=CARTESIAN_POINT('Ctrl Pts',(-32.1510868622955,1.74624591422736,307.477963533858));
#11859=CARTESIAN_POINT('Ctrl Pts',(-32.1010312430896,1.69952490619419,307.473465557447));
#11860=CARTESIAN_POINT('Ctrl Pts',(-32.0653663687863,1.66404812675948,307.470238901108));
#11861=CARTESIAN_POINT('Ctrl Pts',(-31.9686412486793,1.56150974645989,307.461330643034));
#11862=CARTESIAN_POINT('Ctrl Pts',(-31.9102574576355,1.4920407832551,307.455763108366));
#11863=CARTESIAN_POINT('Ctrl Pts',(-31.7618294183545,1.29334116534389,307.440559666581));
#11864=CARTESIAN_POINT('Ctrl Pts',(-31.6804534809308,1.15824326746686,307.430955875689));
#11865=CARTESIAN_POINT('Ctrl Pts',(-31.5959157346897,0.979941685904312,
307.418300152065));
#11866=CARTESIAN_POINT('Ctrl Pts',(-31.579694916916,0.94336710970338,307.415707152027));
#11867=CARTESIAN_POINT('Ctrl Pts',(-31.5551614972478,0.88404419762547,307.411495744531));
#11868=CARTESIAN_POINT('Ctrl Pts',(-31.5462584197052,0.86154748692908,307.409897441728));
#11869=CARTESIAN_POINT('Ctrl Pts',(-31.5297912858489,0.818002037920552,
307.406799257714));
#11870=CARTESIAN_POINT('Ctrl Pts',(-31.5221777350071,0.796974697133103,
307.405301236171));
#11871=CARTESIAN_POINT('Ctrl Pts',(-31.505001215033,0.747354998155642,307.401760133146));
#11872=CARTESIAN_POINT('Ctrl Pts',(-31.4956840415227,0.718682320381088,
307.399709175678));
#11873=CARTESIAN_POINT('Ctrl Pts',(-31.4648482700424,0.617248992593758,
307.392433501489));
#11874=CARTESIAN_POINT('Ctrl Pts',(-31.4462785702959,0.54364750578791,307.387116218976));
#11875=CARTESIAN_POINT('Ctrl Pts',(-31.4050818909819,0.33955925022164,307.372275708274));
#11876=CARTESIAN_POINT('Ctrl Pts',(-31.3898014674528,0.207873854870359,
307.36258171725));
#11877=CARTESIAN_POINT('Ctrl Pts',(-31.3822919101746,-0.0275512204801254,
307.34540000574));
#11878=CARTESIAN_POINT('Ctrl Pts',(-31.3857390502401,-0.13083361538035,
307.337919144375));
#11879=CARTESIAN_POINT('Ctrl Pts',(-31.3980717522607,-0.255454347045799,
307.329180950194));
#11880=CARTESIAN_POINT('Ctrl Pts',(-31.4005415966385,-0.277306635222439,
307.327659755259));
#11881=CARTESIAN_POINT('Ctrl Pts',(-31.4050062455816,-0.312424299571121,
307.325236244969));
#11882=CARTESIAN_POINT('Ctrl Pts',(-31.4068102012905,-0.32571206095583,
307.32432412947));
#11883=CARTESIAN_POINT('Ctrl Pts',(-31.4106274339495,-0.352145659643509,
307.32252034031));
#11884=CARTESIAN_POINT('Ctrl Pts',(-31.4126387662875,-0.365291251296927,
307.321628610258));
#11885=CARTESIAN_POINT('Ctrl Pts',(-31.4181852859462,-0.399608804941246,
307.319312920007));
#11886=CARTESIAN_POINT('Ctrl Pts',(-31.4218975913983,-0.420751475337849,
307.317898458906));
#11887=CARTESIAN_POINT('Ctrl Pts',(-31.4428452991858,-0.53122765141641,
307.310557736726));
#11888=CARTESIAN_POINT('Ctrl Pts',(-31.4649251696897,-0.61957480390495,
307.304858643912));
#11889=CARTESIAN_POINT('Ctrl Pts',(-31.5532868691836,-0.902767303017338,
307.286523586627));
#11890=CARTESIAN_POINT('Ctrl Pts',(-31.6398114074909,-1.09027448089469,
307.274194698425));
#11891=CARTESIAN_POINT('Ctrl Pts',(-31.7693483967489,-1.29587977526629,
307.2585658805));
#11892=CARTESIAN_POINT('Ctrl Pts',(-31.7900055127924,-1.32701155225187,
307.25613904528));
#11893=CARTESIAN_POINT('Ctrl Pts',(-31.8249358002462,-1.37704707161445,
307.252130037151));
#11894=CARTESIAN_POINT('Ctrl Pts',(-31.8387725274328,-1.39624849015093,
307.250564474461));
#11895=CARTESIAN_POINT('Ctrl Pts',(-31.8663784218923,-1.4333732806422,307.247482109363));
#11896=CARTESIAN_POINT('Ctrl Pts',(-31.8801210435141,-1.45131328138309,
307.245966455723));
#11897=CARTESIAN_POINT('Ctrl Pts',(-31.9137231717789,-1.49390361330038,
307.242303216889));
#11898=CARTESIAN_POINT('Ctrl Pts',(-31.93382345473,-1.51835749833102,307.240146147827));
#11899=CARTESIAN_POINT('Ctrl Pts',(-32.0123060027435,-1.61003511820792,
307.231846787389));
#11900=CARTESIAN_POINT('Ctrl Pts',(-32.0739611617507,-1.67434747359036,
307.225572526693));
#11901=CARTESIAN_POINT('Ctrl Pts',(-32.2835017710116,-1.8696386891287,307.205021418415));
#11902=CARTESIAN_POINT('Ctrl Pts',(-32.4441533212775,-1.98567190297956,
307.190315173605));
#11903=CARTESIAN_POINT('Ctrl Pts',(-32.6480129420326,-2.09726151902507,
307.173852996177));
#11904=CARTESIAN_POINT('Ctrl Pts',(-32.6790799459142,-2.11338415854509,
307.17140125084));
#11905=CARTESIAN_POINT('Ctrl Pts',(-32.7248046178473,-2.13584324003085,
307.167886455046));
#11906=CARTESIAN_POINT('Ctrl Pts',(-32.7391859621059,-2.14272797248362,
307.166794199414));
#11907=CARTESIAN_POINT('Ctrl Pts',(-32.7649688993926,-2.15475288603087,
307.164860893863));
#11908=CARTESIAN_POINT('Ctrl Pts',(-32.7763430621495,-2.15994857207763,
307.164016672615));
#11909=CARTESIAN_POINT('Ctrl Pts',(-32.8024597365458,-2.17162983084127,
307.162097771747));
#11910=CARTESIAN_POINT('Ctrl Pts',(-32.8172279211728,-2.17805553846788,
307.161026627419));
#11911=CARTESIAN_POINT('Ctrl Pts',(-32.8651627584999,-2.19833404354466,
307.157591101519));
#11912=CARTESIAN_POINT('Ctrl Pts',(-32.898580766007,-2.21158419117673,307.155259228338));
#11913=CARTESIAN_POINT('Ctrl Pts',(-32.9824506994427,-2.24265120677377,
307.149531937816));
#11914=CARTESIAN_POINT('Ctrl Pts',(-33.0332296848043,-2.25953084197437,
307.146174555644));
#11915=CARTESIAN_POINT('Ctrl Pts',(-33.1776413132687,-2.30216767044983,
307.136822321827));
#11916=CARTESIAN_POINT('Ctrl Pts',(-33.2723458175848,-2.32391447656752,
307.130913013371));
#11917=CARTESIAN_POINT('Ctrl Pts',(-33.4941140570786,-2.36069028902384,
307.117108850802));
#11918=CARTESIAN_POINT('Ctrl Pts',(-33.6215764974871,-2.371370927097,307.109191088827));
#11919=CARTESIAN_POINT('Ctrl Pts',(-33.7838572571033,-2.37184007913191,
307.098721271738));
#11920=CARTESIAN_POINT('Ctrl Pts',(-33.8184406679319,-2.37118348851954,
307.096468703635));
#11921=CARTESIAN_POINT('Ctrl Pts',(-33.8737970864208,-2.36892068858804,
307.092822555602));
#11922=CARTESIAN_POINT('Ctrl Pts',(-33.8945855277575,-2.36779658511583,
307.091444131109));
#11923=CARTESIAN_POINT('Ctrl Pts',(-33.937916761463,-2.36488093778276,307.088550453095));
#11924=CARTESIAN_POINT('Ctrl Pts',(-33.9604540225239,-2.36304036673669,
307.087033797287));
#11925=CARTESIAN_POINT('Ctrl Pts',(-34.0145491136094,-2.35784289459128,
307.083363943893));
#11926=CARTESIAN_POINT('Ctrl Pts',(-34.0460718556148,-2.35417435975609,
307.081201174547));
#11927=CARTESIAN_POINT('Ctrl Pts',(-34.1665114209254,-2.33770230992993,
307.072840528105));
#11928=CARTESIAN_POINT('Ctrl Pts',(-34.254738461866,-2.32048499372037,307.066508068907));
#11929=CARTESIAN_POINT('Ctrl Pts',(-34.5393270065787,-2.24796789465653,
307.045429536507));
#11930=CARTESIAN_POINT('Ctrl Pts',(-34.7295558522013,-2.17237028144524,
307.030220244785));
#11931=CARTESIAN_POINT('Ctrl Pts',(-34.9341073994896,-2.05875400215761,
307.013725392309));
#11932=CARTESIAN_POINT('Ctrl Pts',(-34.9601663288664,-2.04362309802117,
307.011623146056));
#11933=CARTESIAN_POINT('Ctrl Pts',(-34.9988112104367,-2.02018835145821,
307.008512000459));
#11934=CARTESIAN_POINT('Ctrl Pts',(-35.0116168706243,-2.01225501326667,
307.007482158663));
#11935=CARTESIAN_POINT('Ctrl Pts',(-35.0349676077063,-1.99747911242623,
307.005607520721));
#11936=CARTESIAN_POINT('Ctrl Pts',(-35.0455346995024,-1.99067423254084,
307.004760553942));
#11937=CARTESIAN_POINT('Ctrl Pts',(-35.0704385735836,-1.97435539521378,
307.002767124403));
#11938=CARTESIAN_POINT('Ctrl Pts',(-35.0847266784049,-1.9647689630405,307.001625399393));
#11939=CARTESIAN_POINT('Ctrl Pts',(-35.1343392524853,-1.93069327637295,
306.997663130212));
#11940=CARTESIAN_POINT('Ctrl Pts',(-35.1691033488349,-1.9053986232599,306.99489053457));
#11941=CARTESIAN_POINT('Ctrl Pts',(-35.2586541431049,-1.83644097495435,
306.987703199578));
#11942=CARTESIAN_POINT('Ctrl Pts',(-35.3122289333961,-1.79127086295319,
306.983356113053));
#11943=CARTESIAN_POINT('Ctrl Pts',(-35.5017791844257,-1.61652458723488,
306.967479284102));
#11944=CARTESIAN_POINT('Ctrl Pts',(-35.624216946341,-1.47332560575195,306.956156254573));
#11945=CARTESIAN_POINT('Ctrl Pts',(-35.7506777173988,-1.28396343557345,
306.941551397319));
#11946=CARTESIAN_POINT('Ctrl Pts',(-35.7720237750796,-1.25018181106343,
306.938961502858));
#11947=CARTESIAN_POINT('Ctrl Pts',(-35.8049033167822,-1.19511448344296,
306.934753883871));
#11948=CARTESIAN_POINT('Ctrl Pts',(-35.8169824648313,-1.17416255506173,
306.933156196315));
#11949=CARTESIAN_POINT('Ctrl Pts',(-35.8396121876671,-1.13348484492079,
306.930058373272));
#11950=CARTESIAN_POINT('Ctrl Pts',(-35.8502082629263,-1.11378724464323,
306.928560084849));
#11951=CARTESIAN_POINT('Ctrl Pts',(-35.8744401003821,-1.06717294373351,
306.925017024253));
#11952=CARTESIAN_POINT('Ctrl Pts',(-35.8878436423616,-1.04014061246904,
306.922964350476));
#11953=CARTESIAN_POINT('Ctrl Pts',(-35.9332106445632,-0.944081936041073,
306.915673591037));
#11954=CARTESIAN_POINT('Ctrl Pts',(-35.9623630611649,-0.873787255719231,
306.910342415322));
#11955=CARTESIAN_POINT('Ctrl Pts',(-36.0260686944148,-0.696543641088698,
306.89691609023));
#11956=CARTESIAN_POINT('Ctrl Pts',(-36.056495417909,-0.588310919215101,
306.888725877847));
#11957=CARTESIAN_POINT('Ctrl Pts',(-36.1019991305066,-0.367326364621391,
306.872245732569));
#11958=CARTESIAN_POINT('Ctrl Pts',(-36.116873116569,-0.254807449769235,
306.863977309298));
#11959=CARTESIAN_POINT('Ctrl Pts',(-36.125250290397,-0.114790745098507,
306.854119245306));
#11960=CARTESIAN_POINT('Ctrl Pts',(-36.1264001201571,-0.0879065852303928,
306.852246352496));
#11961=CARTESIAN_POINT('Ctrl Pts',(-36.1274096809125,-0.048671399532048,
306.849547474942));
#11962=CARTESIAN_POINT('Ctrl Pts',(-36.1276308264995,-0.0363328465487193,
306.848703708325));
#11963=CARTESIAN_POINT('Ctrl Pts',(-36.1278359145932,-0.0160603911082621,
306.847326153347));
#11964=CARTESIAN_POINT('Ctrl Pts',(-36.1278763664462,-0.00812765307939112,
306.846789323244));
#11965=CARTESIAN_POINT('Ctrl Pts',(-36.127877017276,-0.000194578459783513,
306.846254750936));
#11966=CARTESIAN_POINT('Ctrl Pts',(-36.1278770172634,-0.000194731713651253,
306.846254761263));
#11967=CARTESIAN_POINT('Ctrl Pts',(-36.1278774563459,0.00515310811414783,
306.845894395659));
#11968=CARTESIAN_POINT('Ctrl Pts',(-36.1278598079454,0.0105009685530968,
306.845535050245));
#11969=CARTESIAN_POINT('Ctrl Pts',(-36.1277582570605,0.0256975957702179,
306.844516710825));
#11970=CARTESIAN_POINT('Ctrl Pts',(-36.1276310938811,0.0355461262819293,
306.843860077856));
#11971=CARTESIAN_POINT('Ctrl Pts',(-36.1270154865911,0.0677046885558121,
306.841725987912));
#11972=CARTESIAN_POINT('Ctrl Pts',(-36.1262735210064,0.0900094268948125,
306.840261568538));
#11973=CARTESIAN_POINT('Ctrl Pts',(-36.1197048925516,0.228580092810293,
306.831243183719));
#11974=CARTESIAN_POINT('Ctrl Pts',(-36.1056389628918,0.344310022035404,
306.824054824637));
#11975=CARTESIAN_POINT('Ctrl Pts',(-36.0608152101483,0.571776512456467,
306.809824522904));
#11976=CARTESIAN_POINT('Ctrl Pts',(-36.0302701490589,0.683218723248633,
306.80279845525));
#11977=CARTESIAN_POINT('Ctrl Pts',(-35.9664306693679,0.863422495560842,
306.790851462533));
#11978=CARTESIAN_POINT('Ctrl Pts',(-35.9377191958462,0.933592260668311,
306.786045212838));
#11979=CARTESIAN_POINT('Ctrl Pts',(-35.8929660106762,1.02957532602775,306.779172980922));
#11980=CARTESIAN_POINT('Ctrl Pts',(-35.8797124208884,1.05664144027858,306.777200909041));
#11981=CARTESIAN_POINT('Ctrl Pts',(-35.85573235748,1.10333835807569,306.773734181727));
#11982=CARTESIAN_POINT('Ctrl Pts',(-35.8452370004536,1.12308394012621,306.772247771746));
#11983=CARTESIAN_POINT('Ctrl Pts',(-35.8228058219585,1.16388245970358,306.769131903066));
#11984=CARTESIAN_POINT('Ctrl Pts',(-35.8108238718769,1.1849069252816,306.7675009167));
#11985=CARTESIAN_POINT('Ctrl Pts',(-35.778172505885,1.24021470579082,306.763140767886));
#11986=CARTESIAN_POINT('Ctrl Pts',(-35.7569540314417,1.27416301722768,306.760391945756));
#11987=CARTESIAN_POINT('Ctrl Pts',(-35.6314170739579,1.46414151122691,306.744581501467));
#11988=CARTESIAN_POINT('Ctrl Pts',(-35.5097406367729,1.60786764857421,306.730863155621));
#11989=CARTESIAN_POINT('Ctrl Pts',(-35.3028887619339,1.80048792503961,306.710246681824));
#11990=CARTESIAN_POINT('Ctrl Pts',(-35.2295071613655,1.86101662323564,306.703357205578));
#11991=CARTESIAN_POINT('Ctrl Pts',(-35.1314645679029,1.93244250150146,306.69484399385));
#11992=CARTESIAN_POINT('Ctrl Pts',(-35.1099875779095,1.94754951784499,306.693018863923));
#11993=CARTESIAN_POINT('Ctrl Pts',(-35.0764317457653,1.97032941381941,306.690233300838));
#11994=CARTESIAN_POINT('Ctrl Pts',(-35.0645276289194,1.97825439238528,306.689257645768));
#11995=CARTESIAN_POINT('Ctrl Pts',(-35.0418689585642,1.99304503340415,306.687425230021));
#11996=CARTESIAN_POINT('Ctrl Pts',(-35.0311296775771,1.99993226582504,306.68656718667));
#11997=CARTESIAN_POINT('Ctrl Pts',(-35.0071002039374,2.01507043276041,306.684669437456));
#11998=CARTESIAN_POINT('Ctrl Pts',(-34.9937827194217,2.02327733099054,306.683632505095));
#11999=CARTESIAN_POINT('Ctrl Pts',(-34.9461625215303,2.05197712434194,306.679973410174));
#12000=CARTESIAN_POINT('Ctrl Pts',(-34.9114223774695,2.07173542798703,306.677392893843));
#12001=CARTESIAN_POINT('Ctrl Pts',(-34.7086783487885,2.18035817473198,306.662739506664));
#12002=CARTESIAN_POINT('Ctrl Pts',(-34.530967085463,2.24965602621045,306.651420652043));
#12003=CARTESIAN_POINT('Ctrl Pts',(-34.2616230269383,2.31892659538957,306.634142759693));
#12004=CARTESIAN_POINT('Ctrl Pts',(-34.1752242892763,2.33608685157348,306.628591982323));
#12005=CARTESIAN_POINT('Ctrl Pts',(-34.0568391114912,2.35282078874392,306.62084867567));
#12006=CARTESIAN_POINT('Ctrl Pts',(-34.0255166080271,2.35661250970322,306.618787454681));
#12007=CARTESIAN_POINT('Ctrl Pts',(-33.9716618704988,2.36204417782628,306.615217182898));
#12008=CARTESIAN_POINT('Ctrl Pts',(-33.949164249989,2.36398911531894,306.613717897667));
#12009=CARTESIAN_POINT('Ctrl Pts',(-33.9030059654058,2.36731625444962,306.610624166743));
#12010=CARTESIAN_POINT('Ctrl Pts',(-33.8793455685378,2.36866561406213,306.609028863294));
#12011=CARTESIAN_POINT('Ctrl Pts',(-33.8181857857007,2.37123476112112,306.604878922486));
#12012=CARTESIAN_POINT('Ctrl Pts',(-33.7806718254818,2.37191965606312,306.602307923069));
#12013=CARTESIAN_POINT('Ctrl Pts',(-33.5382358164977,2.37059408799022,306.585518638005));
#12014=CARTESIAN_POINT('Ctrl Pts',(-33.3343521135606,2.3429185690601,306.570485717552));
#12015=CARTESIAN_POINT('Ctrl Pts',(-33.0484023640538,2.2655407613773,306.548919674832));
#12016=CARTESIAN_POINT('Ctrl Pts',(-32.9616345153684,2.23658986085814,306.542326023611));
#12017=CARTESIAN_POINT('Ctrl Pts',(-32.856794722381,2.19473483371029,306.5344552064));
#12018=CARTESIAN_POINT('Ctrl Pts',(-32.8369512080468,2.18649845195985,306.532970010008));
#12019=CARTESIAN_POINT('Ctrl Pts',(-32.8050063192341,2.17272741137367,306.530589592997));
#12020=CARTESIAN_POINT('Ctrl Pts',(-32.7928352520656,2.1673587578273,306.529685153995));
#12021=CARTESIAN_POINT('Ctrl Pts',(-32.7684909059324,2.15637488552004,306.527882095618));
#12022=CARTESIAN_POINT('Ctrl Pts',(-32.7563187983768,2.15075830414283,306.526983595275));
#12023=CARTESIAN_POINT('Ctrl Pts',(-32.7243250686593,2.13566510624946,306.52462823978));
#12024=CARTESIAN_POINT('Ctrl Pts',(-32.7045858611095,2.12601551960761,306.52318149419));
#12025=CARTESIAN_POINT('Ctrl Pts',(-32.6799621861859,2.1135512688101,306.521381323964));
#12026=CARTESIAN_POINT('Ctrl Pts',(-32.6749509397694,2.1109921821394,306.521015205799));
#12027=CARTESIAN_POINT('Ctrl Pts',(-32.669949078383,2.10841540741463,306.520649966606));
#12028=CARTESIAN_POINT('',(-36.12787621691,-0.00195816148385779,306.651410108095));
#12029=CARTESIAN_POINT('Ctrl Pts',(-32.6699490794746,2.10841540797695,306.325637667993));
#12030=CARTESIAN_POINT('Ctrl Pts',(-32.740580335012,2.14480202882853,306.330956386877));
#12031=CARTESIAN_POINT('Ctrl Pts',(-32.8130060340432,2.17761708796589,306.336275105761));
#12032=CARTESIAN_POINT('Ctrl Pts',(-32.8868275626125,2.20669810049877,306.341593824645));
#12033=CARTESIAN_POINT('Ctrl Pts',(-32.9606910905097,2.23579565811012,306.346915569511));
#12034=CARTESIAN_POINT('Ctrl Pts',(-33.0359515845324,2.26115479003096,306.352237314377));
#12035=CARTESIAN_POINT('Ctrl Pts',(-33.1121945935353,2.28266271837875,306.357559059243));
#12036=CARTESIAN_POINT('Ctrl Pts',(-33.1885688716104,2.30420767734527,306.36288996666));
#12037=CARTESIAN_POINT('Ctrl Pts',(-33.2659285853022,2.32188808823443,306.368220874078));
#12038=CARTESIAN_POINT('Ctrl Pts',(-33.3438488339219,2.33564225759189,306.373551781495));
#12039=CARTESIAN_POINT('Ctrl Pts',(-33.3931441306437,2.34434366539857,306.376924315177));
#12040=CARTESIAN_POINT('Ctrl Pts',(-33.4426636274186,2.35147471381064,306.380296848858));
#12041=CARTESIAN_POINT('Ctrl Pts',(-33.4922993170496,2.35703054771926,306.38366938254));
#12042=CARTESIAN_POINT('Ctrl Pts',(-33.5707719805349,2.36581416869707,306.38900126576));
#12043=CARTESIAN_POINT('Ctrl Pts',(-33.6498324657182,2.37069126356453,306.394333148981));
#12044=CARTESIAN_POINT('Ctrl Pts',(-33.7290582212338,2.37159552671798,306.399665032201));
#12045=CARTESIAN_POINT('Ctrl Pts',(-33.8081693780082,2.37249848186977,306.404989202941));
#12046=CARTESIAN_POINT('Ctrl Pts',(-33.8874448655169,2.36944001201456,306.410313373681));
#12047=CARTESIAN_POINT('Ctrl Pts',(-33.9664562485564,2.36240548600924,306.415637544421));
#12048=CARTESIAN_POINT('Ctrl Pts',(-34.0453755650935,2.35537915685075,306.420955511273));
#12049=CARTESIAN_POINT('Ctrl Pts',(-34.1240309241399,2.34438601973636,306.426273478125));
#12050=CARTESIAN_POINT('Ctrl Pts',(-34.2019946575969,2.32946348263547,306.431591444977));
#12051=CARTESIAN_POINT('Ctrl Pts',(-34.2799086403339,2.31455046800011,306.436906018293));
#12052=CARTESIAN_POINT('Ctrl Pts',(-34.3571314142341,2.29571311813722,306.44222059161));
#12053=CARTESIAN_POINT('Ctrl Pts',(-34.4332424076483,2.2730404355026,306.447535164926));
#12054=CARTESIAN_POINT('Ctrl Pts',(-34.5093285469098,2.25037515666464,306.452848002761));
#12055=CARTESIAN_POINT('Ctrl Pts',(-34.5843031776156,2.22387716576713,306.458160840596));
#12056=CARTESIAN_POINT('Ctrl Pts',(-34.6577593209395,2.19368577191067,306.463473678431));
#12057=CARTESIAN_POINT('Ctrl Pts',(-34.7312143636644,2.16349483041418,306.468786436664));
#12058=CARTESIAN_POINT('Ctrl Pts',(-34.8031505310992,2.12961077542176,306.474099194896));
#12059=CARTESIAN_POINT('Ctrl Pts',(-34.8731807112876,2.09222109850439,306.479411953129));
#12060=CARTESIAN_POINT('Ctrl Pts',(-34.9432807830373,2.0547941059198,306.484730013603));
#12061=CARTESIAN_POINT('Ctrl Pts',(-35.0114706530401,2.0138547236573,306.490048074078));
#12062=CARTESIAN_POINT('Ctrl Pts',(-35.0773882690518,1.96963620705639,306.495366134552));
#12063=CARTESIAN_POINT('Ctrl Pts',(-35.1433374527221,1.9253965144008,306.500686741823));
#12064=CARTESIAN_POINT('Ctrl Pts',(-35.2070118383397,1.87787483980058,306.506007349093));
#12065=CARTESIAN_POINT('Ctrl Pts',(-35.2680809106938,1.82734602930435,306.511327956364));
#12066=CARTESIAN_POINT('Ctrl Pts',(-35.3292613847221,1.77672504458852,306.51665826944));
#12067=CARTESIAN_POINT('Ctrl Pts',(-35.3878267019854,1.72308627990384,306.521988582516));
#12068=CARTESIAN_POINT('Ctrl Pts',(-35.4434819562292,1.66674275142438,306.527318895592));
#12069=CARTESIAN_POINT('Ctrl Pts',(-35.496599423864,1.61296839370921,306.532406155298));
#12070=CARTESIAN_POINT('Ctrl Pts',(-35.5470662239413,1.5567308559791,306.537493415003));
#12071=CARTESIAN_POINT('Ctrl Pts',(-35.5946614695316,1.49832878892391,306.542580674709));
#12072=CARTESIAN_POINT('Ctrl Pts',(-35.6443558396156,1.43735097700345,306.547892301183));
#12073=CARTESIAN_POINT('Ctrl Pts',(-35.6911130175382,1.37377573384131,306.553203927657));
#12074=CARTESIAN_POINT('Ctrl Pts',(-35.734648440398,1.30791860309843,306.558515554131));
#12075=CARTESIAN_POINT('Ctrl Pts',(-35.7781234778771,1.24215281884183,306.563819813166));
#12076=CARTESIAN_POINT('Ctrl Pts',(-35.8183853700947,1.17411181772676,306.569124072201));
#12077=CARTESIAN_POINT('Ctrl Pts',(-35.8551894739287,1.10414441948464,306.574428331236));
#12078=CARTESIAN_POINT('Ctrl Pts',(-35.891954203411,1.03425187487723,306.579726915584));
#12079=CARTESIAN_POINT('Ctrl Pts',(-35.9252682694939,0.962437439897806,
306.585025499932));
#12080=CARTESIAN_POINT('Ctrl Pts',(-35.954930930203,0.889077865036043,306.59032408428));
#12081=CARTESIAN_POINT('Ctrl Pts',(-35.9845742172474,0.815766203738364,
306.595619207947));
#12082=CARTESIAN_POINT('Ctrl Pts',(-36.0105706539352,0.740911841440301,
306.600914331614));
#12083=CARTESIAN_POINT('Ctrl Pts',(-36.0327666015562,0.664913755407971,
306.606209455282));
#12084=CARTESIAN_POINT('Ctrl Pts',(-36.0549533461896,0.588947180057778,
306.61150238346));
#12085=CARTESIAN_POINT('Ctrl Pts',(-36.0733426017308,0.511838276606008,
306.616795311638));
#12086=CARTESIAN_POINT('Ctrl Pts',(-36.08783034275,0.434001960473747,306.622088239817));
#12087=CARTESIAN_POINT('Ctrl Pts',(-36.1023225761047,0.356141508981568,
306.627382809218));
#12088=CARTESIAN_POINT('Ctrl Pts',(-36.1129107851658,0.277553657859791,
306.632677378619));
#12089=CARTESIAN_POINT('Ctrl Pts',(-36.1195421286928,0.198663311545526,
306.63797194802));
#12090=CARTESIAN_POINT('Ctrl Pts',(-36.1251524719885,0.131919381942699,
306.642451334712));
#12091=CARTESIAN_POINT('Ctrl Pts',(-36.1279314652037,0.0649592490742431,
306.646930721403));
#12092=CARTESIAN_POINT('Ctrl Pts',(-36.12787621691,-0.00195816148385779,
306.651410108095));
#12093=CARTESIAN_POINT('Ctrl Pts',(-36.1261829184293,-0.00197080147836691,
306.651411048457));
#12094=CARTESIAN_POINT('Ctrl Pts',(-36.128116703496,-0.251180220789445,
306.668104687931));
#12095=CARTESIAN_POINT('Ctrl Pts',(-35.9771376933501,-1.28886751917914,
306.737768758128));
#12096=CARTESIAN_POINT('Ctrl Pts',(-34.4707053354124,-2.71176214819284,
306.860403259048));
#12097=CARTESIAN_POINT('Ctrl Pts',(-31.8635119515384,-2.06936810284668,
307.019314551217));
#12098=CARTESIAN_POINT('Ctrl Pts',(-31.0125546758027,0.408963281941028,
307.174390069647));
#12099=CARTESIAN_POINT('Ctrl Pts',(-32.0218921613136,1.77375560660345,307.276495157355));
#12100=CARTESIAN_POINT('Ctrl Pts',(-32.6683119391961,2.11155019427352,307.325629814339));
#12101=CARTESIAN_POINT('Origin',(-33.7561270252576,0.,302.151410108095));
#12102=CARTESIAN_POINT('',(-32.6699490794739,2.10841540797657,308.52497223169));
#12103=CARTESIAN_POINT('',(-32.6699491752354,2.10841545730937,308.326094215555));
#12104=CARTESIAN_POINT('',(-32.6699490794746,2.10841540797695,302.151410108095));
#12105=CARTESIAN_POINT('Ctrl Pts',(-32.6699490794745,2.10841540797688,308.52497223169));
#12106=CARTESIAN_POINT('Ctrl Pts',(-32.6697542748568,2.10831505181432,308.524957834865));
#12107=CARTESIAN_POINT('Ctrl Pts',(-32.6695594840382,2.10821466859727,308.524943437104));
#12108=CARTESIAN_POINT('Ctrl Pts',(-32.648369882537,2.09729113332925,308.523377016956));
#12109=CARTESIAN_POINT('Ctrl Pts',(-32.6275385802355,2.0861553247313,308.52181433451));
#12110=CARTESIAN_POINT('Ctrl Pts',(-32.5873096832505,2.06387123670633,308.518749964238));
#12111=CARTESIAN_POINT('Ctrl Pts',(-32.5678966164551,2.05275592723339,308.51724958258));
#12112=CARTESIAN_POINT('Ctrl Pts',(-32.521426213119,2.02526837387622,308.51360388372));
#12113=CARTESIAN_POINT('Ctrl Pts',(-32.4945341167153,2.00862670649824,308.511448912638));
#12114=CARTESIAN_POINT('Ctrl Pts',(-32.3989261999558,1.94678408147741,308.503618667244));
#12115=CARTESIAN_POINT('Ctrl Pts',(-32.3322464250881,1.89855831636061,308.497833801045));
#12116=CARTESIAN_POINT('Ctrl Pts',(-32.2579515648505,1.83870659476065,308.491006349664));
#12117=CARTESIAN_POINT('Ctrl Pts',(-32.2477606154721,1.83035581706245,308.490061111339));
#12118=CARTESIAN_POINT('Ctrl Pts',(-32.0926299878261,1.70106156965988,308.475539419776));
#12119=CARTESIAN_POINT('Ctrl Pts',(-31.9625763998646,1.56333137965069,308.461499449945));
#12120=CARTESIAN_POINT('Ctrl Pts',(-31.8284628308755,1.38226118142892,308.445515867498));
#12121=CARTESIAN_POINT('Ctrl Pts',(-31.807379373289,1.35237500724561,308.44295086956));
#12122=CARTESIAN_POINT('Ctrl Pts',(-31.7779592063255,1.30855373612376,308.439306908925));
#12123=CARTESIAN_POINT('Ctrl Pts',(-31.7690620906967,1.29500339137565,308.438195816581));
#12124=CARTESIAN_POINT('Ctrl Pts',(-31.7535476924234,1.27083849590288,308.43624344493));
#12125=CARTESIAN_POINT('Ctrl Pts',(-31.7468745208969,1.26026142564978,308.435398700216));
#12126=CARTESIAN_POINT('Ctrl Pts',(-31.73193690934,1.23616482292314,308.433496277736));
#12127=CARTESIAN_POINT('Ctrl Pts',(-31.7237238573915,1.22261461344489,308.432441845368));
#12128=CARTESIAN_POINT('Ctrl Pts',(-31.6981014985519,1.17937006123461,308.429121724834));
#12129=CARTESIAN_POINT('Ctrl Pts',(-31.6812016812521,1.14937718787041,308.426885573243));
#12130=CARTESIAN_POINT('Ctrl Pts',(-31.5714809950463,0.944337749136008,
308.411969255072));
#12131=CARTESIAN_POINT('Ctrl Pts',(-31.5002498458649,0.758609238711452,
308.400196080818));
#12132=CARTESIAN_POINT('Ctrl Pts',(-31.4316686244342,0.479619053799077,
308.382355799246));
#12133=CARTESIAN_POINT('Ctrl Pts',(-31.4152906630639,0.391948818370953,
308.376738581987));
#12134=CARTESIAN_POINT('Ctrl Pts',(-31.3998323773657,0.272169253142799,
308.36891803522));
#12135=CARTESIAN_POINT('Ctrl Pts',(-31.3964091478656,0.240690575271756,
308.366849687097));
#12136=CARTESIAN_POINT('Ctrl Pts',(-31.3916242167409,0.186642134752707,
308.363271045692));
#12137=CARTESIAN_POINT('Ctrl Pts',(-31.3899531614768,0.164103638394417,
308.361770641594));
#12138=CARTESIAN_POINT('Ctrl Pts',(-31.3871922228285,0.1179234957643,308.358678194116));
#12139=CARTESIAN_POINT('Ctrl Pts',(-31.3861336141789,0.0942826059095021,
308.357085341973));
#12140=CARTESIAN_POINT('Ctrl Pts',(-31.3843168457758,0.0333032031595571,
308.352949865781));
#12141=CARTESIAN_POINT('Ctrl Pts',(-31.384086551998,-0.00404323980376545,
308.350391098596));
#12142=CARTESIAN_POINT('Ctrl Pts',(-31.3883276229169,-0.247101946770624,
308.333559524211));
#12143=CARTESIAN_POINT('Ctrl Pts',(-31.4186730931841,-0.451453949153685,
308.318463712881));
#12144=CARTESIAN_POINT('Ctrl Pts',(-31.4998741205617,-0.736743829507453,
308.296871488298));
#12145=CARTESIAN_POINT('Ctrl Pts',(-31.5297829911895,-0.822717608745344,
308.290310819784));
#12146=CARTESIAN_POINT('Ctrl Pts',(-31.5727648889355,-0.926600496625176,
308.282472474566));
#12147=CARTESIAN_POINT('Ctrl Pts',(-31.5812396044316,-0.946321027588535,
308.280988738936));
#12148=CARTESIAN_POINT('Ctrl Pts',(-31.5953968071521,-0.978069430686514,
308.278610069112));
#12149=CARTESIAN_POINT('Ctrl Pts',(-31.6009146153508,-0.990168863814282,
308.277705939843));
#12150=CARTESIAN_POINT('Ctrl Pts',(-31.6122004359407,-1.01437500641261,
308.275902892951));
#12151=CARTESIAN_POINT('Ctrl Pts',(-31.6179699313795,-1.02648046168159,
308.275004101913));
#12152=CARTESIAN_POINT('Ctrl Pts',(-31.6334714183632,-1.05830754001571,
308.272647047806));
#12153=CARTESIAN_POINT('Ctrl Pts',(-31.6433758114949,-1.07794437218729,
308.271198920616));
#12154=CARTESIAN_POINT('Ctrl Pts',(-31.7014952220605,-1.18929464050435,
308.263006364641));
#12155=CARTESIAN_POINT('Ctrl Pts',(-31.7554116824241,-1.27791894335982,
308.256557735778));
#12156=CARTESIAN_POINT('Ctrl Pts',(-31.8908308417353,-1.47081793333816,
308.242046205086));
#12157=CARTESIAN_POINT('Ctrl Pts',(-31.9755938651227,-1.57236639485723,
308.234042502347));
#12158=CARTESIAN_POINT('Ctrl Pts',(-32.121613255749,-1.72026352478538,308.221054644192));
#12159=CARTESIAN_POINT('Ctrl Pts',(-32.1774096619966,-1.77160708026099,
308.216247889956));
#12160=CARTESIAN_POINT('Ctrl Pts',(-32.2586921250765,-1.83950944134362,
308.209375063999));
#12161=CARTESIAN_POINT('Ctrl Pts',(-32.2821853972595,-1.85838699053612,
308.207402925673));
#12162=CARTESIAN_POINT('Ctrl Pts',(-32.323726049381,-1.89048288397758,308.203936122047));
#12163=CARTESIAN_POINT('Ctrl Pts',(-32.3416129004449,-1.90390331228865,
308.202449703314));
#12164=CARTESIAN_POINT('Ctrl Pts',(-32.3792454311392,-1.93131579081057,
308.199333855758));
#12165=CARTESIAN_POINT('Ctrl Pts',(-32.3990207738363,-1.94526248993868,
308.197702899811));
#12166=CARTESIAN_POINT('Ctrl Pts',(-32.4520654778456,-1.9814700983897,308.193342930609));
#12167=CARTESIAN_POINT('Ctrl Pts',(-32.4856896329674,-2.0031946394492,308.190594260586));
#12168=CARTESIAN_POINT('Ctrl Pts',(-32.65372404966,-2.1058290152217,308.176923033223));
#12169=CARTESIAN_POINT('Ctrl Pts',(-32.7953644104614,-2.1741040331218,308.165562217286));
#12170=CARTESIAN_POINT('Ctrl Pts',(-33.0281375237343,-2.25909403744493,
308.14746299889));
#12171=CARTESIAN_POINT('Ctrl Pts',(-33.115322881501,-2.28535468439157,308.140810319842));
#12172=CARTESIAN_POINT('Ctrl Pts',(-33.2528059330067,-2.31827624780975,
308.130680020555));
#12173=CARTESIAN_POINT('Ctrl Pts',(-33.3021729215608,-2.32844655809023,
308.12711337567));
#12174=CARTESIAN_POINT('Ctrl Pts',(-33.3697585590679,-2.34013856792791,
308.122358014188));
#12175=CARTESIAN_POINT('Ctrl Pts',(-33.3877227448265,-2.34303381254994,
308.121106214314));
#12176=CARTESIAN_POINT('Ctrl Pts',(-33.4182710689383,-2.34759717188068,
308.119000127986));
#12177=CARTESIAN_POINT('Ctrl Pts',(-33.4308382168061,-2.34937148003678,
308.118140229852));
#12178=CARTESIAN_POINT('Ctrl Pts',(-33.4577927696138,-2.35295664436021,
308.116310374752));
#12179=CARTESIAN_POINT('Ctrl Pts',(-33.4721834001099,-2.35473657625174,
308.115342083902));
#12180=CARTESIAN_POINT('Ctrl Pts',(-33.5128952934578,-2.3593934419375,308.11262481515));
#12181=CARTESIAN_POINT('Ctrl Pts',(-33.53925055855,-2.36196186042849,308.110891781249));
#12182=CARTESIAN_POINT('Ctrl Pts',(-33.6643944532447,-2.3720451162905,308.102762338388));
#12183=CARTESIAN_POINT('Ctrl Pts',(-33.7635567364719,-2.37380745681212,
308.09661197928));
#12184=CARTESIAN_POINT('Ctrl Pts',(-33.9889953647975,-2.36368180310672,
308.082730119426));
#12185=CARTESIAN_POINT('Ctrl Pts',(-34.114781457606,-2.34788956288181,308.075048713537));
#12186=CARTESIAN_POINT('Ctrl Pts',(-34.3139541748837,-2.30649818637312,
308.062343340631));
#12187=CARTESIAN_POINT('Ctrl Pts',(-34.3883919737379,-2.28721321442363,
308.057471349542));
#12188=CARTESIAN_POINT('Ctrl Pts',(-34.4906580942736,-2.25534443709275,
308.050521765373));
#12189=CARTESIAN_POINT('Ctrl Pts',(-34.5193825206474,-2.24578612796657,
308.048541113089));
#12190=CARTESIAN_POINT('Ctrl Pts',(-34.5690119733194,-2.22820937687997,
308.045064525627));
#12191=CARTESIAN_POINT('Ctrl Pts',(-34.5900013818312,-2.22043970079052,
308.043576980269));
#12192=CARTESIAN_POINT('Ctrl Pts',(-34.6333985245347,-2.20367322980368,
308.040463796503));
#12193=CARTESIAN_POINT('Ctrl Pts',(-34.6557850189734,-2.19462899060574,
308.038836700144));
#12194=CARTESIAN_POINT('Ctrl Pts',(-34.7146582443577,-2.1697918044283,308.034499482581));
#12195=CARTESIAN_POINT('Ctrl Pts',(-34.750891256558,-2.15342108385763,308.031770072265));
#12196=CARTESIAN_POINT('Ctrl Pts',(-34.9321409666564,-2.06597867834001,
308.017801287286));
#12197=CARTESIAN_POINT('Ctrl Pts',(-35.0700184466392,-1.98114859418881,
308.006093034955));
#12198=CARTESIAN_POINT('Ctrl Pts',(-35.2681226563116,-1.82943339383273,
307.987866453835));
#12199=CARTESIAN_POINT('Ctrl Pts',(-35.3350220046007,-1.77201844289353,
307.981430235382));
#12200=CARTESIAN_POINT('Ctrl Pts',(-35.4342506891282,-1.67676612268595,
307.971579549188));
#12201=CARTESIAN_POINT('Ctrl Pts',(-35.4688498730938,-1.64140942128715,
307.968080914963));
#12202=CARTESIAN_POINT('Ctrl Pts',(-35.5145546470336,-1.59168376047633,
307.963399416128));
#12203=CARTESIAN_POINT('Ctrl Pts',(-35.5266364951789,-1.57823355756364,
307.962155852577));
#12204=CARTESIAN_POINT('Ctrl Pts',(-35.5469252043895,-1.55512076283722,
307.960059141527));
#12205=CARTESIAN_POINT('Ctrl Pts',(-35.5552103448498,-1.54552837104443,
307.959200507061));
#12206=CARTESIAN_POINT('Ctrl Pts',(-35.5728457011268,-1.52477645431676,
307.957368134114));
#12207=CARTESIAN_POINT('Ctrl Pts',(-35.5821706416015,-1.51359661794947,
307.95639613445));
#12208=CARTESIAN_POINT('Ctrl Pts',(-35.6083369626702,-1.481631536107,307.953657381288));
#12209=CARTESIAN_POINT('Ctrl Pts',(-35.6249310273757,-1.46064554547021,
307.951906969884));
#12210=CARTESIAN_POINT('Ctrl Pts',(-35.7049666369477,-1.35582950369665,
307.943370944638));
#12211=CARTESIAN_POINT('Ctrl Pts',(-35.7631474918,-1.26811793654532,307.9368633105));
#12212=CARTESIAN_POINT('Ctrl Pts',(-35.8634475536584,-1.09261434813488,
307.924444136605));
#12213=CARTESIAN_POINT('Ctrl Pts',(-35.9063626397152,-1.00553089679297,
307.918536730961));
#12214=CARTESIAN_POINT('Ctrl Pts',(-35.9805724135404,-0.828307100562886,
307.90663443121));
#12215=CARTESIAN_POINT('Ctrl Pts',(-36.012002414096,-0.738426161484981,
307.900654107954));
#12216=CARTESIAN_POINT('Ctrl Pts',(-36.0467432470147,-0.615885605863798,
307.892412700175));
#12217=CARTESIAN_POINT('Ctrl Pts',(-36.0549041411989,-0.584689115442946,
307.89030768033));
#12218=CARTESIAN_POINT('Ctrl Pts',(-36.0677220082109,-0.531264477556838,
307.886685800129));
#12219=CARTESIAN_POINT('Ctrl Pts',(-36.0727004682386,-0.509117602033948,
307.885179470436));
#12220=CARTESIAN_POINT('Ctrl Pts',(-36.0816130422755,-0.466628341438866,
307.882278619619));
#12221=CARTESIAN_POINT('Ctrl Pts',(-36.0855999907097,-0.446299092795844,
307.880885948514));
#12222=CARTESIAN_POINT('Ctrl Pts',(-36.0954232086945,-0.392487527835203,
307.877185802047));
#12223=CARTESIAN_POINT('Ctrl Pts',(-36.1008067832265,-0.358928567925944,
307.874864217193));
#12224=CARTESIAN_POINT('Ctrl Pts',(-36.1204886453171,-0.216770304780468,
307.86496553811));
#12225=CARTESIAN_POINT('Ctrl Pts',(-36.1279742159633,-0.107378564969787,
307.857182146614));
#12226=CARTESIAN_POINT('Ctrl Pts',(-36.1277925564576,0.0953097255528812,
307.842518464619));
#12227=CARTESIAN_POINT('Ctrl Pts',(-36.1222173954371,0.188405761762015,
307.835691019819));
#12228=CARTESIAN_POINT('Ctrl Pts',(-36.0993641809586,0.379986546714878,
307.821623522208));
#12229=CARTESIAN_POINT('Ctrl Pts',(-36.0813084448988,0.478210813311289,
307.814401901211));
#12230=CARTESIAN_POINT('Ctrl Pts',(-36.0517918752457,0.596324959568578,
307.805907049349));
#12231=CARTESIAN_POINT('Ctrl Pts',(-36.0461703700952,0.617561435737019,
307.80438752565));
#12232=CARTESIAN_POINT('Ctrl Pts',(-36.0366446524408,0.651626489706044,
307.801966016027));
#12233=CARTESIAN_POINT('Ctrl Pts',(-36.0329254416588,0.664504870916143,
307.801054257331));
#12234=CARTESIAN_POINT('Ctrl Pts',(-36.0252980093427,0.690100042069758,
307.799250520573));
#12235=CARTESIAN_POINT('Ctrl Pts',(-36.0213915898061,0.702816829367536,
307.79835849386));
#12236=CARTESIAN_POINT('Ctrl Pts',(-36.0108963036553,0.735985892266726,
307.796041053341));
#12237=CARTESIAN_POINT('Ctrl Pts',(-36.0041359747943,0.756383220297852,
307.794625165464));
#12238=CARTESIAN_POINT('Ctrl Pts',(-35.9671486370035,0.863102681964889,
307.787251906237));
#12239=CARTESIAN_POINT('Ctrl Pts',(-35.9322211667796,0.947724043275812,
307.78152415316));
#12240=CARTESIAN_POINT('Ctrl Pts',(-35.8035560887079,1.21456084626016,307.763218125622));
#12241=CARTESIAN_POINT('Ctrl Pts',(-35.6911234696286,1.3866900089454,307.750939954969));
#12242=CARTESIAN_POINT('Ctrl Pts',(-35.5335694788711,1.57076609099005,307.735360177558));
#12243=CARTESIAN_POINT('Ctrl Pts',(-35.5084820867311,1.59870549959886,307.732921535792));
#12244=CARTESIAN_POINT('Ctrl Pts',(-35.4664919964326,1.64329291781381,307.728898175018));
#12245=CARTESIAN_POINT('Ctrl Pts',(-35.4499835291377,1.6603041961926,307.727330306133));
#12246=CARTESIAN_POINT('Ctrl Pts',(-35.4172585068807,1.69302983611128,307.724247090564));
#12247=CARTESIAN_POINT('Ctrl Pts',(-35.4010669959496,1.70876571152136,307.722732945937));
#12248=CARTESIAN_POINT('Ctrl Pts',(-35.3617311550341,1.74591741009388,307.719079718324));
#12249=CARTESIAN_POINT('Ctrl Pts',(-35.3383801091086,1.76710702442154,307.716931284295));
#12250=CARTESIAN_POINT('Ctrl Pts',(-35.2483967040069,1.84554763981705,307.70872331868));
#12251=CARTESIAN_POINT('Ctrl Pts',(-35.179030927775,1.89954102569049,307.702535659541));
#12252=CARTESIAN_POINT('Ctrl Pts',(-34.9516381436544,2.0570853809518,307.682698436166));
#12253=CARTESIAN_POINT('Ctrl Pts',(-34.7841681281559,2.14568684717222,307.668662132311));
#12254=CARTESIAN_POINT('Ctrl Pts',(-34.5695888448959,2.22826602888145,307.652279204754));
#12255=CARTESIAN_POINT('Ctrl Pts',(-34.5308239999495,2.24203806835419,307.649382093788));
#12256=CARTESIAN_POINT('Ctrl Pts',(-34.4767343348253,2.25968395395205,307.645443157625));
#12257=CARTESIAN_POINT('Ctrl Pts',(-34.4617018226034,2.2644228195073,307.64435935515));
#12258=CARTESIAN_POINT('Ctrl Pts',(-34.4345130235691,2.27269679545539,307.642420089707));
#12259=CARTESIAN_POINT('Ctrl Pts',(-34.422373593407,2.27628509388628,307.641561740739));
#12260=CARTESIAN_POINT('Ctrl Pts',(-34.3965739802381,2.28368712128925,307.639754056385));
#12261=CARTESIAN_POINT('Ctrl Pts',(-34.382907431527,2.28747579621743,307.638806110259));
#12262=CARTESIAN_POINT('Ctrl Pts',(-34.3444059876715,2.29777829054088,307.636160367355));
#12263=CARTESIAN_POINT('Ctrl Pts',(-34.3194973208564,2.30401199038756,307.634477555899));
#12264=CARTESIAN_POINT('Ctrl Pts',(-34.1523543874522,2.34296868964753,307.623347343232));
#12265=CARTESIAN_POINT('Ctrl Pts',(-34.0074444705203,2.36291108848683,307.614463716015));
#12266=CARTESIAN_POINT('Ctrl Pts',(-33.7245743813617,2.37550356416093,307.597110497572));
#12267=CARTESIAN_POINT('Ctrl Pts',(-33.5872869385353,2.3697047077334,307.588677199415));
#12268=CARTESIAN_POINT('Ctrl Pts',(-33.4113105662334,2.34689664467568,307.577299817156));
#12269=CARTESIAN_POINT('Ctrl Pts',(-33.3714842033524,2.34069900728107,307.574688295764));
#12270=CARTESIAN_POINT('Ctrl Pts',(-33.3079754915257,2.32915144502778,307.570454291191));
#12271=CARTESIAN_POINT('Ctrl Pts',(-33.2841828526557,2.32444721938452,307.568852318163));
#12272=CARTESIAN_POINT('Ctrl Pts',(-33.2386181067272,2.31470986710964,307.565751938187));
#12273=CARTESIAN_POINT('Ctrl Pts',(-33.2168367007447,2.30973226508669,307.564255465589));
#12274=CARTESIAN_POINT('Ctrl Pts',(-33.1659765892476,2.29735081885887,307.560725816924));
#12275=CARTESIAN_POINT('Ctrl Pts',(-33.1369622148869,2.28970153411024,307.558684914724));
#12276=CARTESIAN_POINT('Ctrl Pts',(-33.0361861696619,2.26107769404405,307.551496810703));
#12277=CARTESIAN_POINT('Ctrl Pts',(-32.9652838867656,2.23726445359715,307.54626005412));
#12278=CARTESIAN_POINT('Ctrl Pts',(-32.8186507790181,2.18017441547123,307.535050914851));
#12279=CARTESIAN_POINT('Ctrl Pts',(-32.7433222279446,2.14621455870658,307.529068256111));
#12280=CARTESIAN_POINT('Ctrl Pts',(-32.669948905789,2.10841531850051,307.52304986714));
#12281=CARTESIAN_POINT('',(-36.1316341613132,-0.000310224732309534,307.651557338406));
#12282=CARTESIAN_POINT('Ctrl Pts',(-32.6683119391961,2.11155019427352,307.325629814339));
#12283=CARTESIAN_POINT('Ctrl Pts',(-32.7187757087736,2.13792065634783,307.329465588078));
#12284=CARTESIAN_POINT('Ctrl Pts',(-33.480627950877,2.49966777931651,307.38627179254));
#12285=CARTESIAN_POINT('Ctrl Pts',(-35.3072153547382,2.32488896510995,307.494865049128));
#12286=CARTESIAN_POINT('Ctrl Pts',(-36.1304027123948,0.767986961440899,
307.599622531977));
#12287=CARTESIAN_POINT('Ctrl Pts',(-36.1318916699647,-0.000319976874305989,
307.651409584103));
#12288=CARTESIAN_POINT('Ctrl Pts',(-36.127877019312,-0.000167937542783692,
307.653713125769));
#12289=CARTESIAN_POINT('Ctrl Pts',(-36.1278765090554,-0.00737419368197688,
307.654208311306));
#12290=CARTESIAN_POINT('Ctrl Pts',(-36.127843155871,-0.0145805378433049,
307.654701857024));
#12291=CARTESIAN_POINT('Ctrl Pts',(-36.127694085241,-0.0308079898488567,
307.655809365293));
#12292=CARTESIAN_POINT('Ctrl Pts',(-36.1275597397538,-0.039828880661449,
307.656422337782));
#12293=CARTESIAN_POINT('Ctrl Pts',(-36.1271115390896,-0.0615856206795041,
307.657893862826));
#12294=CARTESIAN_POINT('Ctrl Pts',(-36.1267465408413,-0.0743200882215176,
307.658749416002));
#12295=CARTESIAN_POINT('Ctrl Pts',(-36.1255781386497,-0.106132282250148,
307.660873635551));
#12296=CARTESIAN_POINT('Ctrl Pts',(-36.1246469054167,-0.125204933390442,
307.662135473233));
#12297=CARTESIAN_POINT('Ctrl Pts',(-36.1199726224132,-0.201908932090859,
307.667170518765));
#12298=CARTESIAN_POINT('Ctrl Pts',(-36.1143553003309,-0.259410452491916,
307.67085503912));
#12299=CARTESIAN_POINT('Ctrl Pts',(-36.0993672545264,-0.370666356698195,
307.677907012708));
#12300=CARTESIAN_POINT('Ctrl Pts',(-36.090231052281,-0.424413946499034,
307.681278500044));
#12301=CARTESIAN_POINT('Ctrl Pts',(-36.0790227014757,-0.478910244553418,
307.684701385748));
#12302=CARTESIAN_POINT('Ctrl Pts',(-36.078793770254,-0.480019308592317,
307.684771047274));
#12303=CARTESIAN_POINT('Ctrl Pts',(-36.0783012437081,-0.482396766123027,
307.684920382481));
#12304=CARTESIAN_POINT('Ctrl Pts',(-36.0780374032698,-0.483665108608161,
307.685000053608));
#12305=CARTESIAN_POINT('Ctrl Pts',(-36.0774696446138,-0.486383285530192,
307.685170803283));
#12306=CARTESIAN_POINT('Ctrl Pts',(-36.0771654069789,-0.487833052861174,
307.685261878618));
#12307=CARTESIAN_POINT('Ctrl Pts',(-36.0765105376764,-0.490939185927556,
307.685457018683));
#12308=CARTESIAN_POINT('Ctrl Pts',(-36.0761594902127,-0.492595463383139,
307.685561079404));
#12309=CARTESIAN_POINT('Ctrl Pts',(-36.0596340523472,-0.570154625741113,
307.690434331927));
#12310=CARTESIAN_POINT('Ctrl Pts',(-36.0397457800762,-0.64521800625907,
307.695168606122));
#12311=CARTESIAN_POINT('Ctrl Pts',(-35.981991286292,-0.826718830723631,
307.706901769611));
#12312=CARTESIAN_POINT('Ctrl Pts',(-35.9401401747814,-0.931674806330502,
307.71394249447));
#12313=CARTESIAN_POINT('Ctrl Pts',(-35.8763376098401,-1.06350127103369,
307.723402362815));
#12314=CARTESIAN_POINT('Ctrl Pts',(-35.8610534552305,-1.09344063211769,
307.725593587552));
#12315=CARTESIAN_POINT('Ctrl Pts',(-35.8342749221447,-1.14325228371779,
307.729317980128));
#12316=CARTESIAN_POINT('Ctrl Pts',(-35.8231186675002,-1.16330131682555,
307.730839070142));
#12317=CARTESIAN_POINT('Ctrl Pts',(-35.8001138563068,-1.20326756977821,
307.733917633036));
#12318=CARTESIAN_POINT('Ctrl Pts',(-35.7882607546979,-1.2231792384507,307.735475147773));
#12319=CARTESIAN_POINT('Ctrl Pts',(-35.7578663628417,-1.27257640502601,
307.739400647811));
#12320=CARTESIAN_POINT('Ctrl Pts',(-35.7389642822171,-1.30183227410116,
307.741781708271));
#12321=CARTESIAN_POINT('Ctrl Pts',(-35.6441790637803,-1.44168144016217,
307.753446055091));
#12322=CARTESIAN_POINT('Ctrl Pts',(-35.5596630212636,-1.5461026355357,307.763051597278));
#12323=CARTESIAN_POINT('Ctrl Pts',(-35.3868766020232,-1.72602583638157,
307.781207693843));
#12324=CARTESIAN_POINT('Ctrl Pts',(-35.3009953850314,-1.80330029230458,
307.789689672557));
#12325=CARTESIAN_POINT('Ctrl Pts',(-35.1645491797456,-1.90914359139318,
307.802112625275));
#12326=CARTESIAN_POINT('Ctrl Pts',(-35.1180058033821,-1.942619249809,307.806184784382));
#12327=CARTESIAN_POINT('Ctrl Pts',(-35.0544872931942,-1.98489775771553,
307.811482730365));
#12328=CARTESIAN_POINT('Ctrl Pts',(-35.0385566986853,-1.99522747699303,
307.812790575262));
#12329=CARTESIAN_POINT('Ctrl Pts',(-35.0116667774051,-2.01220830143521,
307.814961185446));
#12330=CARTESIAN_POINT('Ctrl Pts',(-35.0007746883969,-2.01896373041983,
307.815830413431));
#12331=CARTESIAN_POINT('Ctrl Pts',(-34.9777437091783,-2.03299063665592,
307.817646726324));
#12332=CARTESIAN_POINT('Ctrl Pts',(-34.9655936938365,-2.04024230288451,
307.818592598252));
#12333=CARTESIAN_POINT('Ctrl Pts',(-34.9313500427877,-2.0602670087037,307.821226206858));
#12334=CARTESIAN_POINT('Ctrl Pts',(-34.9091133892519,-2.0727932511646,307.822899176504));
#12335=CARTESIAN_POINT('Ctrl Pts',(-34.7604451424701,-2.15340731666415,
307.833869391093));
#12336=CARTESIAN_POINT('Ctrl Pts',(-34.6282403864116,-2.21025942671556,
307.8426198623));
#12337=CARTESIAN_POINT('Ctrl Pts',(-34.3963596429151,-2.28590358685133,
307.857566676457));
#12338=CARTESIAN_POINT('Ctrl Pts',(-34.2991573293271,-2.3109239275784,307.863719024815));
#12339=CARTESIAN_POINT('Ctrl Pts',(-34.1564474395464,-2.33815489656479,
307.872854373876));
#12340=CARTESIAN_POINT('Ctrl Pts',(-34.111997372899,-2.34533167942639,307.875712989716));
#12341=CARTESIAN_POINT('Ctrl Pts',(-34.0302851279116,-2.35614832473346,
307.881013752131));
#12342=CARTESIAN_POINT('Ctrl Pts',(-33.993089164764,-2.36017929145379,307.883443848311));
#12343=CARTESIAN_POINT('Ctrl Pts',(-33.9322230478898,-2.36532213622309,
307.887456743865));
#12344=CARTESIAN_POINT('Ctrl Pts',(-33.9086033020265,-2.3669620896453,307.889022865845));
#12345=CARTESIAN_POINT('Ctrl Pts',(-33.8626596055415,-2.3694615032158,307.892088353743));
#12346=CARTESIAN_POINT('Ctrl Pts',(-33.8403402065243,-2.37035969565154,
307.893586332386));
#12347=CARTESIAN_POINT('Ctrl Pts',(-33.7865919296176,-2.37176260438227,
307.897216290942));
#12348=CARTESIAN_POINT('Ctrl Pts',(-33.7551599587579,-2.37195802260147,
307.899357717033));
#12349=CARTESIAN_POINT('Ctrl Pts',(-33.6434878640738,-2.37043270973191,
307.90703586961));
#12350=CARTESIAN_POINT('Ctrl Pts',(-33.5633571785347,-2.36526448474291,
307.91267628221));
#12351=CARTESIAN_POINT('Ctrl Pts',(-33.4661784296475,-2.35402574484011,
307.91967042979));
#12352=CARTESIAN_POINT('Ctrl Pts',(-33.4487303293756,-2.35181092913946,
307.920932167285));
#12353=CARTESIAN_POINT('Ctrl Pts',(-33.2824230179605,-2.3288179950122,307.93301293664));
#12354=CARTESIAN_POINT('Ctrl Pts',(-33.1358408946272,-2.29412952272418,
307.944108376364));
#12355=CARTESIAN_POINT('Ctrl Pts',(-32.9322345423204,-2.22499208796223,
307.95963210317));
#12356=CARTESIAN_POINT('Ctrl Pts',(-32.8718095199361,-2.2016749775241,307.964249384));
#12357=CARTESIAN_POINT('Ctrl Pts',(-32.7943267188082,-2.16806981427336,
307.970121008768));
#12358=CARTESIAN_POINT('Ctrl Pts',(-32.7763418367738,-2.16000175882924,
307.971480292437));
#12359=CARTESIAN_POINT('Ctrl Pts',(-32.746713721265,-2.14626430107095,307.973711091706));
#12360=CARTESIAN_POINT('Ctrl Pts',(-32.7350128372068,-2.14072219474714,
307.974589856524));
#12361=CARTESIAN_POINT('Ctrl Pts',(-32.7108570364416,-2.12903770062934,
307.976398568031));
#12362=CARTESIAN_POINT('Ctrl Pts',(-32.6984097069005,-2.12288129181267,
307.977327663037));
#12363=CARTESIAN_POINT('Ctrl Pts',(-32.6643732758007,-2.10567328683639,
307.979862127884));
#12364=CARTESIAN_POINT('Ctrl Pts',(-32.6428978486329,-2.09439899572613,
307.98145447193));
#12365=CARTESIAN_POINT('Ctrl Pts',(-32.484685188987,-2.00821831807319,307.993163086215));
#12366=CARTESIAN_POINT('Ctrl Pts',(-32.3554405212278,-1.92031132432452,
308.002619572892));
#12367=CARTESIAN_POINT('Ctrl Pts',(-32.1314981972803,-1.73327106113856,
308.020509619051));
#12368=CARTESIAN_POINT('Ctrl Pts',(-32.0349323387032,-1.63741579241115,
308.028885978213));
#12369=CARTESIAN_POINT('Ctrl Pts',(-31.9230844722645,-1.50550078619912,
308.040011618715));
#12370=CARTESIAN_POINT('Ctrl Pts',(-31.8997341261551,-1.47661192513993,
308.042424881406));
#12371=CARTESIAN_POINT('Ctrl Pts',(-31.8626584672837,-1.42847223646105,
308.046417321166));
#12372=CARTESIAN_POINT('Ctrl Pts',(-31.8485251077224,-1.40954282181255,
308.047980161213));
#12373=CARTESIAN_POINT('Ctrl Pts',(-31.8215657861463,-1.37228681089711,
308.05104440554));
#12374=CARTESIAN_POINT('Ctrl Pts',(-31.8087116591879,-1.3539836083857,308.0525444976));
#12375=CARTESIAN_POINT('Ctrl Pts',(-31.7783218049435,-1.30938287163757,
308.0561887144));
#12376=CARTESIAN_POINT('Ctrl Pts',(-31.7610496040051,-1.28291188658631,
308.058342475401));
#12377=CARTESIAN_POINT('Ctrl Pts',(-31.7008491811293,-1.18649309442998,
308.066159037659));
#12378=CARTESIAN_POINT('Ctrl Pts',(-31.6610332297251,-1.11468030765325,
308.071930892358));
#12379=CARTESIAN_POINT('Ctrl Pts',(-31.6186200939947,-1.02784966403373,
308.078845886496));
#12380=CARTESIAN_POINT('Ctrl Pts',(-31.6123394703698,-1.01468503536244,
308.079892524471));
#12381=CARTESIAN_POINT('Ctrl Pts',(-31.5268419288237,-0.831138533660723,
308.094458681905));
#12382=CARTESIAN_POINT('Ctrl Pts',(-31.4680283704042,-0.652000157306974,
308.108431684514));
#12383=CARTESIAN_POINT('Ctrl Pts',(-31.4238007818546,-0.432172798124201,
308.124334417911));
#12384=CARTESIAN_POINT('Ctrl Pts',(-31.4174515582709,-0.396379160406,308.126883415748));
#12385=CARTESIAN_POINT('Ctrl Pts',(-31.4094695078673,-0.344467816460916,
308.130509128568));
#12386=CARTESIAN_POINT('Ctrl Pts',(-31.407175258702,-0.328458850252923,
308.131617553476));
#12387=CARTESIAN_POINT('Ctrl Pts',(-31.403397644424,-0.300031478304804,
308.133567134708));
#12388=CARTESIAN_POINT('Ctrl Pts',(-31.4018485040756,-0.287623177273709,
308.134411715774));
#12389=CARTESIAN_POINT('Ctrl Pts',(-31.3985552189583,-0.259432677195143,
308.13631611495));
#12390=CARTESIAN_POINT('Ctrl Pts',(-31.396871305245,-0.243644451177669,
308.137372650129));
#12391=CARTESIAN_POINT('Ctrl Pts',(-31.3920209420462,-0.193387045003184,
308.140707381243));
#12392=CARTESIAN_POINT('Ctrl Pts',(-31.3894502688549,-0.158863307025585,
308.142955670595));
#12393=CARTESIAN_POINT('Ctrl Pts',(-31.3772659998629,0.0733154598678785,
308.157865437777));
#12394=CARTESIAN_POINT('Ctrl Pts',(-31.3916651894792,0.271464154717219,
308.169624849468));
#12395=CARTESIAN_POINT('Ctrl Pts',(-31.4480025886223,0.552898853618975,
308.187448133103));
#12396=CARTESIAN_POINT('Ctrl Pts',(-31.4703968220572,0.63919516156767,308.193063406947));
#12397=CARTESIAN_POINT('Ctrl Pts',(-31.5072538147313,0.75416812576042,308.20088161175));
#12398=CARTESIAN_POINT('Ctrl Pts',(-31.5175201769259,0.784117020266229,
308.202949667796));
#12399=CARTESIAN_POINT('Ctrl Pts',(-31.5361368121047,0.835076152500721,
308.206527882576));
#12400=CARTESIAN_POINT('Ctrl Pts',(-31.544193850152,0.856189404091126,308.208028156098));
#12401=CARTESIAN_POINT('Ctrl Pts',(-31.5613027667926,0.899168767006922,
308.211120400115));
#12402=CARTESIAN_POINT('Ctrl Pts',(-31.570382662337,0.921020904430828,308.212713180184));
#12403=CARTESIAN_POINT('Ctrl Pts',(-31.5946314300359,0.977000226598203,
308.216848603413));
#12404=CARTESIAN_POINT('Ctrl Pts',(-31.6102816227445,1.01091042292533,308.219407391134));
#12405=CARTESIAN_POINT('Ctrl Pts',(-31.7173305104773,1.2291624155334,308.236238677221));
#12406=CARTESIAN_POINT('Ctrl Pts',(-31.8315760291555,1.40128623380289,308.251334134545));
#12407=CARTESIAN_POINT('Ctrl Pts',(-32.0262345803278,1.62509736453917,308.272926304669));
#12408=CARTESIAN_POINT('Ctrl Pts',(-32.0898228200421,1.69023755513334,308.27948724754));
#12409=CARTESIAN_POINT('Ctrl Pts',(-32.1728514796577,1.76603998074251,308.287325795958));
#12410=CARTESIAN_POINT('Ctrl Pts',(-32.1888976290546,1.78029513519444,308.288809479986));
#12411=CARTESIAN_POINT('Ctrl Pts',(-32.215195335303,1.80302645377075,308.291188046395));
#12412=CARTESIAN_POINT('Ctrl Pts',(-32.2253281891676,1.81163732946813,308.292092123479));
#12413=CARTESIAN_POINT('Ctrl Pts',(-32.2458231096099,1.82875912086157,308.293895033539));
#12414=CARTESIAN_POINT('Ctrl Pts',(-32.2561859809717,1.83726827810096,308.294793740374));
#12415=CARTESIAN_POINT('Ctrl Pts',(-32.2837318206295,1.85949829211333,308.297150505908));
#12416=CARTESIAN_POINT('Ctrl Pts',(-32.3010348300074,1.87306922624968,308.298598432046));
#12417=CARTESIAN_POINT('Ctrl Pts',(-32.400582607225,1.94893343472034,308.306761995695));
#12418=CARTESIAN_POINT('Ctrl Pts',(-32.4866436364809,2.00605563072422,308.313184456185));
#12419=CARTESIAN_POINT('Ctrl Pts',(-32.6070478095626,2.07511031170053,308.32173150813));
#12420=CARTESIAN_POINT('Ctrl Pts',(-32.6383186771404,2.09212059175199,308.323913715546));
#12421=CARTESIAN_POINT('Ctrl Pts',(-32.6699491752354,2.10841545730937,308.326094215555));
#12422=CARTESIAN_POINT('Origin',(-33.7561270252576,0.,302.151410108095));
#12423=CARTESIAN_POINT('',(-32.6699489539077,2.1084153432895,309.521847592916));
#12424=CARTESIAN_POINT('',(-32.6699490796625,2.10841540807375,309.323530658174));
#12425=CARTESIAN_POINT('',(-32.6699490794746,2.10841540797695,302.151410108095));
#12426=CARTESIAN_POINT('',(-36.1278768462125,-0.000921574914906319,308.850490323558));
#12427=CARTESIAN_POINT('Ctrl Pts',(-32.6699489539077,2.1084153432895,309.521847592916));
#12428=CARTESIAN_POINT('Ctrl Pts',(-32.582917846397,2.06358011630052,309.515816690897));
#12429=CARTESIAN_POINT('Ctrl Pts',(-32.498706923478,2.01337899071228,309.509858285855));
#12430=CARTESIAN_POINT('Ctrl Pts',(-32.404470529489,1.94896991467382,309.502811052731));
#12431=CARTESIAN_POINT('Ctrl Pts',(-32.3912276866308,1.93971874165601,309.501811619914));
#12432=CARTESIAN_POINT('Ctrl Pts',(-32.3584887098188,1.91634669603684,309.49931615118));
#12433=CARTESIAN_POINT('Ctrl Pts',(-32.3391113321401,1.90206309192492,309.497816975652));
#12434=CARTESIAN_POINT('Ctrl Pts',(-32.2629535455094,1.84411532160427,309.491826734868));
#12435=CARTESIAN_POINT('Ctrl Pts',(-32.2079506655363,1.79818710465182,309.487277956005));
#12436=CARTESIAN_POINT('Ctrl Pts',(-32.1350754708979,1.73151019749231,309.480868475922));
#12437=CARTESIAN_POINT('Ctrl Pts',(-32.11535460679,1.7128343404082,309.479092660394));
#12438=CARTESIAN_POINT('Ctrl Pts',(-32.0799060995893,1.67809020921673,309.475820547609));
#12439=CARTESIAN_POINT('Ctrl Pts',(-32.0640777482451,1.66212891405747,309.474328988195));
#12440=CARTESIAN_POINT('Ctrl Pts',(-32.0322127436525,1.62906936953523,309.471261400308));
#12441=CARTESIAN_POINT('Ctrl Pts',(-32.0161979822021,1.61195357177694,309.469684661158));
#12442=CARTESIAN_POINT('Ctrl Pts',(-31.9761000379658,1.56780502393637,309.465644563816));
#12443=CARTESIAN_POINT('Ctrl Pts',(-31.9523780890904,1.54045389148599,309.463166481503));
#12444=CARTESIAN_POINT('Ctrl Pts',(-31.8349685195819,1.39865047327097,309.450435618493));
#12445=CARTESIAN_POINT('Ctrl Pts',(-31.7515227476866,1.27617452644095,309.439786669305));
#12446=CARTESIAN_POINT('Ctrl Pts',(-31.6106455816979,1.02112816321664,309.418529871605));
#12447=CARTESIAN_POINT('Ctrl Pts',(-31.5527977401673,0.889460175178401,
309.407978794437));
#12448=CARTESIAN_POINT('Ctrl Pts',(-31.4990984677548,0.729158223731884,
309.396124782373));
#12449=CARTESIAN_POINT('Ctrl Pts',(-31.49138133326,0.704823883845353,309.394351693044));
#12450=CARTESIAN_POINT('Ctrl Pts',(-31.4799988534136,0.666812456690814,
309.391627796626));
#12451=CARTESIAN_POINT('Ctrl Pts',(-31.4760607809486,0.653219912869499,
309.390662759126));
#12452=CARTESIAN_POINT('Ctrl Pts',(-31.468788026443,0.62725006950077,309.388837145454));
#12453=CARTESIAN_POINT('Ctrl Pts',(-31.4654316795447,0.614879813954728,
309.387975475822));
#12454=CARTESIAN_POINT('Ctrl Pts',(-31.4573531918775,0.584120992718638,
309.38585136353));
#12455=CARTESIAN_POINT('Ctrl Pts',(-31.452751123251,0.565701319274591,309.384595566348));
#12456=CARTESIAN_POINT('Ctrl Pts',(-31.4351512027875,0.491479318968117,
309.379592894724));
#12457=CARTESIAN_POINT('Ctrl Pts',(-31.4239550887477,0.435265310580698,
309.375933915341));
#12458=CARTESIAN_POINT('Ctrl Pts',(-31.3963932157845,0.26486172104055,309.365081387851));
#12459=CARTESIAN_POINT('Ctrl Pts',(-31.3863064675317,0.14982963374252,309.358068847602));
#12460=CARTESIAN_POINT('Ctrl Pts',(-31.3826744987209,-0.0997217234533173,
309.342756795197));
#12461=CARTESIAN_POINT('Ctrl Pts',(-31.3921215190607,-0.233865917713545,
309.33445536906));
#12462=CARTESIAN_POINT('Ctrl Pts',(-31.4182392734203,-0.400861272744113,
309.32355316731));
#12463=CARTESIAN_POINT('Ctrl Pts',(-31.4243718042195,-0.43511640447206,
309.321287380491));
#12464=CARTESIAN_POINT('Ctrl Pts',(-31.4358388033042,-0.491932266233717,
309.317473366715));
#12465=CARTESIAN_POINT('Ctrl Pts',(-31.4407545355054,-0.514572596182473,
309.31593860045));
#12466=CARTESIAN_POINT('Ctrl Pts',(-31.4511987445333,-0.55949122248238,
309.312861983124));
#12467=CARTESIAN_POINT('Ctrl Pts',(-31.4567205429137,-0.581768486535565,
309.311320497478));
#12468=CARTESIAN_POINT('Ctrl Pts',(-31.4711326271638,-0.636498825868149,
309.307493059471));
#12469=CARTESIAN_POINT('Ctrl Pts',(-31.4803916634546,-0.668848648627756,
309.305195404129));
#12470=CARTESIAN_POINT('Ctrl Pts',(-31.5238445776484,-0.80930053743524,
309.295059102266));
#12471=CARTESIAN_POINT('Ctrl Pts',(-31.5650721323529,-0.91505416768145,
309.286996661471));
#12472=CARTESIAN_POINT('Ctrl Pts',(-31.6765407858452,-1.14977401429132,
309.268182170353));
#12473=CARTESIAN_POINT('Ctrl Pts',(-31.7515089609208,-1.27599579489191,
309.257363799474));
#12474=CARTESIAN_POINT('Ctrl Pts',(-31.8671769011031,-1.43512675390416,
309.243260663563));
#12475=CARTESIAN_POINT('Ctrl Pts',(-31.8979974935542,-1.47481416408846,
309.239702752355));
#12476=CARTESIAN_POINT('Ctrl Pts',(-31.9419637846782,-1.52786056471875,
309.234921798854));
#12477=CARTESIAN_POINT('Ctrl Pts',(-31.9540394178916,-1.54208510777342,
309.233637176521));
#12478=CARTESIAN_POINT('Ctrl Pts',(-31.9746559028175,-1.56579742707062,
309.231493424462));
#12479=CARTESIAN_POINT('Ctrl Pts',(-31.983107584576,-1.57536124047924,309.23062818555));
#12480=CARTESIAN_POINT('Ctrl Pts',(-32.0011829532596,-1.595485337511,309.22880690146));
#12481=CARTESIAN_POINT('Ctrl Pts',(-32.0108254596443,-1.60602759301231,
309.227852249285));
#12482=CARTESIAN_POINT('Ctrl Pts',(-32.0384107634363,-1.63564502771147,
309.225166456635));
#12483=CARTESIAN_POINT('Ctrl Pts',(-32.0565756312691,-1.654511713786,309.223451036351));
#12484=CARTESIAN_POINT('Ctrl Pts',(-32.1416706961535,-1.74001378523437,
309.215633528912));
#12485=CARTESIAN_POINT('Ctrl Pts',(-32.2122372569251,-1.80292132708271,
309.20975552791));
#12486=CARTESIAN_POINT('Ctrl Pts',(-32.4321362320836,-1.9765471002056,309.192497833265));
#12487=CARTESIAN_POINT('Ctrl Pts',(-32.5908981103255,-2.0741087536459,309.181299310397));
#12488=CARTESIAN_POINT('Ctrl Pts',(-32.7970256599932,-2.16957159527893,
309.166751130648));
#12489=CARTESIAN_POINT('Ctrl Pts',(-32.8350879524938,-2.18600160773769,
309.164067494005));
#12490=CARTESIAN_POINT('Ctrl Pts',(-32.8962828983008,-2.21053511335361,
309.159745472607));
#12491=CARTESIAN_POINT('Ctrl Pts',(-32.9191452966412,-2.21929243695327,
309.158129208124));
#12492=CARTESIAN_POINT('Ctrl Pts',(-32.9630581327344,-2.23533797374362,
309.155019640006));
#12493=CARTESIAN_POINT('Ctrl Pts',(-32.9840837980182,-2.24268663032945,
309.153528554313));
#12494=CARTESIAN_POINT('Ctrl Pts',(-33.0331796659499,-2.25907385531725,
309.150040173177));
#12495=CARTESIAN_POINT('Ctrl Pts',(-33.0613206132316,-2.26788700796187,
309.148035691317));
#12496=CARTESIAN_POINT('Ctrl Pts',(-33.1576495363788,-2.29609406856535,
309.141153906513));
#12497=CARTESIAN_POINT('Ctrl Pts',(-33.2265338182193,-2.31295320593156,
309.136197152153));
#12498=CARTESIAN_POINT('Ctrl Pts',(-33.4101614861645,-2.3492622620895,309.122892671633));
#12499=CARTESIAN_POINT('Ctrl Pts',(-33.5257547656435,-2.36339786748194,
309.114418367836));
#12500=CARTESIAN_POINT('Ctrl Pts',(-33.7581461584435,-2.37460246040821,
309.09742337872));
#12501=CARTESIAN_POINT('Ctrl Pts',(-33.8746497067424,-2.37164454226935,
309.088926563471));
#12502=CARTESIAN_POINT('Ctrl Pts',(-34.0173803038589,-2.35747235492378,
309.078846755644));
#12503=CARTESIAN_POINT('Ctrl Pts',(-34.0442409608706,-2.35434060703294,
309.076964791605));
#12504=CARTESIAN_POINT('Ctrl Pts',(-34.0855324296812,-2.34880902523242,
309.074100660093));
#12505=CARTESIAN_POINT('Ctrl Pts',(-34.1000035358569,-2.34673405636085,
309.073102389376));
#12506=CARTESIAN_POINT('Ctrl Pts',(-34.1269684144957,-2.34261285098788,
309.071253677709));
#12507=CARTESIAN_POINT('Ctrl Pts',(-34.1394657637297,-2.34060029159364,
309.070401594835));
#12508=CARTESIAN_POINT('Ctrl Pts',(-34.1696559622773,-2.33549019773581,
309.068353772767));
#12509=CARTESIAN_POINT('Ctrl Pts',(-34.1873307288394,-2.33229158999825,
309.067163591322));
#12510=CARTESIAN_POINT('Ctrl Pts',(-34.252615775204,-2.31970938051097,309.062793984578));
#12511=CARTESIAN_POINT('Ctrl Pts',(-34.299974193986,-2.30906554334728,309.059676620257));
#12512=CARTESIAN_POINT('Ctrl Pts',(-34.4295782247191,-2.27572759823802,
309.051207415679));
#12513=CARTESIAN_POINT('Ctrl Pts',(-34.5109794380923,-2.25003829031335,
309.045956629941));
#12514=CARTESIAN_POINT('Ctrl Pts',(-34.7464045103643,-2.16152159694816,
309.030528449423));
#12515=CARTESIAN_POINT('Ctrl Pts',(-34.89538899509,-2.08683993033501,309.020413185223));
#12516=CARTESIAN_POINT('Ctrl Pts',(-35.0684907215898,-1.97596801079345,
309.007220618518));
#12517=CARTESIAN_POINT('Ctrl Pts',(-35.1011077888881,-1.95391261525189,
309.004667502444));
#12518=CARTESIAN_POINT('Ctrl Pts',(-35.152754485657,-1.91708346639304,309.000504737959));
#12519=CARTESIAN_POINT('Ctrl Pts',(-35.1721351104655,-1.90281326229172,
308.998914331998));
#12520=CARTESIAN_POINT('Ctrl Pts',(-35.2091363711938,-1.87469040674458,
308.995820618641));
#12521=CARTESIAN_POINT('Ctrl Pts',(-35.2267844550389,-1.86087800379728,
308.994319007283));
#12522=CARTESIAN_POINT('Ctrl Pts',(-35.2679595766136,-1.82770041326181,
308.990751922248));
#12523=CARTESIAN_POINT('Ctrl Pts',(-35.2913138744813,-1.80812821747955,
308.988678232333));
#12524=CARTESIAN_POINT('Ctrl Pts',(-35.3734372298396,-1.73656612640412,
308.981199324187));
#12525=CARTESIAN_POINT('Ctrl Pts',(-35.4299901103301,-1.68212193645288,
308.975694338502));
#12526=CARTESIAN_POINT('Ctrl Pts',(-35.580920113046,-1.52165967802093,308.959970510257));
#12527=CARTESIAN_POINT('Ctrl Pts',(-35.6686330434314,-1.4098342691143,308.949551333526));
#12528=CARTESIAN_POINT('Ctrl Pts',(-35.7952550960688,-1.21466208266615,
308.932614583666));
#12529=CARTESIAN_POINT('Ctrl Pts',(-35.8402755650529,-1.13568282327124,
308.926061119853));
#12530=CARTESIAN_POINT('Ctrl Pts',(-35.890319192324,-1.03484018287382,308.918208815548));
#12531=CARTESIAN_POINT('Ctrl Pts',(-35.8997127471641,-1.01523925635252,
308.916705807547));
#12532=CARTESIAN_POINT('Ctrl Pts',(-35.9144414319581,-0.983389716297388,
308.914304071944));
#12533=CARTESIAN_POINT('Ctrl Pts',(-35.9199446176145,-0.971220809855372,
308.91339584066));
#12534=CARTESIAN_POINT('Ctrl Pts',(-35.9307430585327,-0.946795333458533,
308.911592528836));
#12535=CARTESIAN_POINT('Ctrl Pts',(-35.9360382010261,-0.934539235856524,
308.910697476923));
#12536=CARTESIAN_POINT('Ctrl Pts',(-35.949672660231,-0.902234482642457,
308.908362270637));
#12537=CARTESIAN_POINT('Ctrl Pts',(-35.9578408615002,-0.882114380772325,
308.906931915534));
#12538=CARTESIAN_POINT('Ctrl Pts',(-36.0008941077198,-0.771739135686172,
308.89920082097));
#12539=CARTESIAN_POINT('Ctrl Pts',(-36.0305111005879,-0.679515972858705,
308.89315761057));
#12540=CARTESIAN_POINT('Ctrl Pts',(-36.1031262460622,-0.394589597126578,
308.875018901751));
#12541=CARTESIAN_POINT('Ctrl Pts',(-36.1278002130236,-0.198143471055984,
308.863159774315));
#12542=CARTESIAN_POINT('Ctrl Pts',(-36.1278768462125,-0.000921574914906319,
308.850490323558));
#12543=CARTESIAN_POINT('Ctrl Pts',(-36.1278768471091,-0.000919264543416605,
308.850490175141));
#12544=CARTESIAN_POINT('Ctrl Pts',(-36.1278862217721,0.0232678484348831,
308.848936404638));
#12545=CARTESIAN_POINT('Ctrl Pts',(-36.1275256059454,0.0474531569991235,
308.847372543808));
#12546=CARTESIAN_POINT('Ctrl Pts',(-36.1261053066843,0.0944605704131066,
308.844310220116));
#12547=CARTESIAN_POINT('Ctrl Pts',(-36.1250856458576,0.117281064656113,
308.842813128077));
#12548=CARTESIAN_POINT('Ctrl Pts',(-36.1224986940257,0.161004483537275,
308.839922721874));
#12549=CARTESIAN_POINT('Ctrl Pts',(-36.1209835962592,0.181908408395625,
308.838531160638));
#12550=CARTESIAN_POINT('Ctrl Pts',(-36.117420451444,0.223429120442819,308.835746618048));
#12551=CARTESIAN_POINT('Ctrl Pts',(-36.1153788981696,0.244044604936424,
308.834353960904));
#12552=CARTESIAN_POINT('Ctrl Pts',(-36.1092757530738,0.298402547938392,
308.83065390751));
#12553=CARTESIAN_POINT('Ctrl Pts',(-36.1047586302258,0.33208792654728,308.828332403118));
#12554=CARTESIAN_POINT('Ctrl Pts',(-36.0816687472503,0.480061977446924,
308.818002625462));
#12555=CARTESIAN_POINT('Ctrl Pts',(-36.0554676865038,0.592983419147006,
308.809760530729));
#12556=CARTESIAN_POINT('Ctrl Pts',(-36.0025918769121,0.763217153179421,
308.796842910466));
#12557=CARTESIAN_POINT('Ctrl Pts',(-35.9816997077517,0.822150002649554,
308.79227828608));
#12558=CARTESIAN_POINT('Ctrl Pts',(-35.9271683739195,0.958596643332158,
308.781545072691));
#12559=CARTESIAN_POINT('Ctrl Pts',(-35.8916653789878,1.03528032714506,308.775382073959));
#12560=CARTESIAN_POINT('Ctrl Pts',(-35.8295735041397,1.15253826726458,308.765887137372));
#12561=CARTESIAN_POINT('Ctrl Pts',(-35.8057035077327,1.19447131913051,308.762477090076));
#12562=CARTESIAN_POINT('Ctrl Pts',(-35.7712314522354,1.25094902406481,308.757892123523));
#12563=CARTESIAN_POINT('Ctrl Pts',(-35.7617200882782,1.26614210407465,308.756659550395));
#12564=CARTESIAN_POINT('Ctrl Pts',(-35.7452018132878,1.29187447156993,308.754575295973));
#12565=CARTESIAN_POINT('Ctrl Pts',(-35.7382813044423,1.30246789090213,308.753718294113));
#12566=CARTESIAN_POINT('Ctrl Pts',(-35.7231722884601,1.32519631123206,308.751882307876));
#12567=CARTESIAN_POINT('Ctrl Pts',(-35.7149557654274,1.33731160380046,308.750905162207));
#12568=CARTESIAN_POINT('Ctrl Pts',(-35.6911909858697,1.37166384344761,308.748136478314));
#12569=CARTESIAN_POINT('Ctrl Pts',(-35.6753720793933,1.3937118805038,308.746361844236));
#12570=CARTESIAN_POINT('Ctrl Pts',(-35.5352506319563,1.58209836200981,308.731173211207));
#12571=CARTESIAN_POINT('Ctrl Pts',(-35.3899655465321,1.73173651632426,308.718867317132));
#12572=CARTESIAN_POINT('Ctrl Pts',(-35.1562189710855,1.91653027403662,308.700373004404));
#12573=CARTESIAN_POINT('Ctrl Pts',(-35.0822787592643,1.96841680140534,308.694686884142));
#12574=CARTESIAN_POINT('Ctrl Pts',(-34.9785567855332,2.03270099909018,308.686786311959));
#12575=CARTESIAN_POINT('Ctrl Pts',(-34.9512136998376,2.04889617916726,308.684710710447));
#12576=CARTESIAN_POINT('Ctrl Pts',(-34.9038651896521,2.07567020437022,308.681123539355));
#12577=CARTESIAN_POINT('Ctrl Pts',(-34.8840181907516,2.08652130346246,308.679621985114));
#12578=CARTESIAN_POINT('Ctrl Pts',(-34.8456201485913,2.10680702098609,308.67671931056));
#12579=CARTESIAN_POINT('Ctrl Pts',(-34.8270940940707,2.11628461671639,308.675319892015));
#12580=CARTESIAN_POINT('Ctrl Pts',(-34.7774980254699,2.14083906466294,308.671575000399));
#12581=CARTESIAN_POINT('Ctrl Pts',(-34.7462203805165,2.15548267205838,308.669214764579));
#12582=CARTESIAN_POINT('Ctrl Pts',(-34.5984720496493,2.22076136003469,308.658066403211));
#12583=CARTESIAN_POINT('Ctrl Pts',(-34.4783919752916,2.26266447026487,308.648992181369));
#12584=CARTESIAN_POINT('Ctrl Pts',(-34.2381554635698,2.3254180618445,308.630947206709));
#12585=CARTESIAN_POINT('Ctrl Pts',(-34.118578437241,2.34703003429443,308.622018407052));
#12586=CARTESIAN_POINT('Ctrl Pts',(-33.9394147706663,2.36538724422373,308.60905228964));
#12587=CARTESIAN_POINT('Ctrl Pts',(-33.8807495393507,2.36920274653735,308.60487347458));
#12588=CARTESIAN_POINT('Ctrl Pts',(-33.8028682399745,2.37136660309827,308.599462337036));
#12589=CARTESIAN_POINT('Ctrl Pts',(-33.7837315743911,2.37166657772787,308.598143676686));
#12590=CARTESIAN_POINT('Ctrl Pts',(-33.7517494603085,2.37178073355751,308.595960428266));
#12591=CARTESIAN_POINT('Ctrl Pts',(-33.7389056297561,2.37172225759975,308.595089213291));
#12592=CARTESIAN_POINT('Ctrl Pts',(-33.7119721109922,2.37138081452743,308.593274668689));
#12593=CARTESIAN_POINT('Ctrl Pts',(-33.6978834797453,2.37107662018926,308.592332473324));
#12594=CARTESIAN_POINT('Ctrl Pts',(-33.6585729303756,2.36987724468739,308.58972089853));
#12595=CARTESIAN_POINT('Ctrl Pts',(-33.6333605530284,2.36870502073593,308.588065889776));
#12596=CARTESIAN_POINT('Ctrl Pts',(-33.4614682681724,2.35796096139347,308.576889349087));
#12597=CARTESIAN_POINT('Ctrl Pts',(-33.3159165514741,2.33517228013113,308.567943942551));
#12598=CARTESIAN_POINT('Ctrl Pts',(-33.0779989715817,2.27486831545843,308.552901597502));
#12599=CARTESIAN_POINT('Ctrl Pts',(-32.9842027180859,2.24477497530487,308.546858397503));
#12600=CARTESIAN_POINT('Ctrl Pts',(-32.851053115634,2.1927208227923,308.537864870895));
#12601=CARTESIAN_POINT('Ctrl Pts',(-32.8100221092461,2.17533181889552,308.535034369012));
#12602=CARTESIAN_POINT('Ctrl Pts',(-32.7359475555572,2.14144666423182,308.529794219967));
#12603=CARTESIAN_POINT('Ctrl Pts',(-32.7027526725709,2.12531461068094,308.527396545889));
#12604=CARTESIAN_POINT('Ctrl Pts',(-32.6699490794745,2.10841540797688,308.52497223169));
#12605=CARTESIAN_POINT('Ctrl Pts',(-32.6699491752354,2.10841545730937,308.326094215555));
#12606=CARTESIAN_POINT('Ctrl Pts',(-32.755914322101,2.15270152914386,308.332020363251));
#12607=CARTESIAN_POINT('Ctrl Pts',(-32.8445355875257,2.19170323357068,308.337937841171));
#12608=CARTESIAN_POINT('Ctrl Pts',(-33.0065151287818,2.25145240174275,308.348726318251));
#12609=CARTESIAN_POINT('Ctrl Pts',(-33.0789197856405,2.27427891086674,308.353538732903));
#12610=CARTESIAN_POINT('Ctrl Pts',(-33.1814425011099,2.30127021402803,308.360418141556));
#12611=CARTESIAN_POINT('Ctrl Pts',(-33.2107385563569,2.30838865496917,308.362390941712));
#12612=CARTESIAN_POINT('Ctrl Pts',(-33.2619872288921,2.31981119091254,308.365858417377));
#12613=CARTESIAN_POINT('Ctrl Pts',(-33.2838802262251,2.3243667959624,308.367344834049));
#12614=CARTESIAN_POINT('Ctrl Pts',(-33.3295847869115,2.33320487479391,308.370460193041));
#12615=CARTESIAN_POINT('Ctrl Pts',(-33.353403909653,2.33743391038815,308.372090655622));
#12616=CARTESIAN_POINT('Ctrl Pts',(-33.4167673669361,2.34768671985371,308.376448084637));
#12617=CARTESIAN_POINT('Ctrl Pts',(-33.4564049945613,2.35307549354416,308.379194668971));
#12618=CARTESIAN_POINT('Ctrl Pts',(-33.6526684499597,2.37471847086801,308.392903945151));
#12619=CARTESIAN_POINT('Ctrl Pts',(-33.8104844659483,2.37634626975723,308.404308686156));
#12620=CARTESIAN_POINT('Ctrl Pts',(-34.0575130415806,2.35426703884362,308.422423511865));
#12621=CARTESIAN_POINT('Ctrl Pts',(-34.1472230007346,2.34103655628998,308.429048221489));
#12622=CARTESIAN_POINT('Ctrl Pts',(-34.2851867169996,2.31253555044959,308.439142452669));
#12623=CARTESIAN_POINT('Ctrl Pts',(-34.3340825891992,2.30080268812649,308.442700371206));
#12624=CARTESIAN_POINT('Ctrl Pts',(-34.4001058222401,2.2827220270776,308.447446213859));
#12625=CARTESIAN_POINT('Ctrl Pts',(-34.4175842939109,2.27771878802323,308.448696914189));
#12626=CARTESIAN_POINT('Ctrl Pts',(-34.4471614941797,2.26888307666137,308.450801698355));
#12627=CARTESIAN_POINT('Ctrl Pts',(-34.4592898474382,2.26515366580934,308.451661377836));
#12628=CARTESIAN_POINT('Ctrl Pts',(-34.4852184255709,2.25695241315396,308.453491388417));
#12629=CARTESIAN_POINT('Ctrl Pts',(-34.4990083913671,2.25245105798967,308.45446004502));
#12630=CARTESIAN_POINT('Ctrl Pts',(-34.5378785432566,2.23936715245333,308.457179628251));
#12631=CARTESIAN_POINT('Ctrl Pts',(-34.5628582088819,2.23048999547421,308.458914566906));
#12632=CARTESIAN_POINT('Ctrl Pts',(-34.6812408198761,2.18617061385757,308.467099168501));
#12633=CARTESIAN_POINT('Ctrl Pts',(-34.7725006788235,2.14526602339269,308.473298485368));
#12634=CARTESIAN_POINT('Ctrl Pts',(-34.9746165308118,2.03887012752612,308.487346527652));
#12635=CARTESIAN_POINT('Ctrl Pts',(-35.083260673448,1.96987899931533,308.495144083049));
#12636=CARTESIAN_POINT('Ctrl Pts',(-35.245421458766,1.84737304581892,308.507851467831));
#12637=CARTESIAN_POINT('Ctrl Pts',(-35.3028935556564,1.79952681061178,308.512594610753));
#12638=CARTESIAN_POINT('Ctrl Pts',(-35.3801318217029,1.72878759963456,308.51939242449));
#12639=CARTESIAN_POINT('Ctrl Pts',(-35.4018690274413,1.70810751176898,308.521356044168));
#12640=CARTESIAN_POINT('Ctrl Pts',(-35.4390982939029,1.67131830645251,308.524812996333));
#12641=CARTESIAN_POINT('Ctrl Pts',(-35.4547660930301,1.65539192691172,308.526298224071));
#12642=CARTESIAN_POINT('Ctrl Pts',(-35.4869673900299,1.62172063234602,308.529416591302));
#12643=CARTESIAN_POINT('Ctrl Pts',(-35.503458288442,1.60393876387111,308.531051326935));
#12644=CARTESIAN_POINT('Ctrl Pts',(-35.5466199436454,1.55594254872147,308.53543396001));
#12645=CARTESIAN_POINT('Ctrl Pts',(-35.5727971433412,1.52529716513599,308.538201885445));
#12646=CARTESIAN_POINT('Ctrl Pts',(-35.6852502820034,1.3866462902974,308.55060044161));
#12647=CARTESIAN_POINT('Ctrl Pts',(-35.7627564181842,1.27190105467278,308.560559329088));
#12648=CARTESIAN_POINT('Ctrl Pts',(-35.8803492441535,1.06005491438619,308.578232819097));
#12649=CARTESIAN_POINT('Ctrl Pts',(-35.9248289450757,0.965800034558325,
308.585870026231));
#12650=CARTESIAN_POINT('Ctrl Pts',(-35.9828715558642,0.818386804260248,
308.597248914254));
#12651=CARTESIAN_POINT('Ctrl Pts',(-36.0010304084179,0.767175312144135,
308.601102179311));
#12652=CARTESIAN_POINT('Ctrl Pts',(-36.0230435467245,0.697592755418938,
308.606166492897));
#12653=CARTESIAN_POINT('Ctrl Pts',(-36.0284612842857,0.679737624759728,
308.607451114757));
#12654=CARTESIAN_POINT('Ctrl Pts',(-36.0372290353312,0.649564888446928,
308.609594819222));
#12655=CARTESIAN_POINT('Ctrl Pts',(-36.0406912728289,0.637281064922245,
308.61046001159));
#12656=CARTESIAN_POINT('Ctrl Pts',(-36.047818419668,0.611189545029289,308.612281131709));
#12657=CARTESIAN_POINT('Ctrl Pts',(-36.0514580015008,0.597375797176231,
308.61323566757));
#12658=CARTESIAN_POINT('Ctrl Pts',(-36.0614141046315,0.558153201248831,
308.615920973423));
#12659=CARTESIAN_POINT('Ctrl Pts',(-36.0674352388617,0.532670625336184,
308.617636030936));
#12660=CARTESIAN_POINT('Ctrl Pts',(-36.109333487345,0.341237385765275,308.630335671899));
#12661=CARTESIAN_POINT('Ctrl Pts',(-36.1277245328718,0.171942280673287,
308.640560893311));
#12662=CARTESIAN_POINT('Ctrl Pts',(-36.1279869436714,-0.122117100655979,
308.658629064496));
#12663=CARTESIAN_POINT('Ctrl Pts',(-36.1183368969789,-0.246153070808098,
308.666341823443));
#12664=CARTESIAN_POINT('Ctrl Pts',(-36.0936659959656,-0.402857955791089,
308.676578386888));
#12665=CARTESIAN_POINT('Ctrl Pts',(-36.0875732146422,-0.436739556674402,
308.678820596967));
#12666=CARTESIAN_POINT('Ctrl Pts',(-36.0766216258432,-0.49085136791343,
308.682454397209));
#12667=CARTESIAN_POINT('Ctrl Pts',(-36.0722301204751,-0.511171852239556,
308.683831029533));
#12668=CARTESIAN_POINT('Ctrl Pts',(-36.0625009395971,-0.553488632726168,
308.686724420006));
#12669=CARTESIAN_POINT('Ctrl Pts',(-36.0571143997941,-0.575471406683232,
308.688242623345));
#12670=CARTESIAN_POINT('Ctrl Pts',(-36.0433885791615,-0.628210141620436,
308.691923089821));
#12671=CARTESIAN_POINT('Ctrl Pts',(-36.0347426417342,-0.658880943506679,
308.694095068142));
#12672=CARTESIAN_POINT('Ctrl Pts',(-35.9989869521985,-0.776586526600283,
308.702557309091));
#12673=CARTESIAN_POINT('Ctrl Pts',(-35.9674892081753,-0.862195433089648,
308.70898655651));
#12674=CARTESIAN_POINT('Ctrl Pts',(-35.8901584996685,-1.04003537782102,
308.722913369648));
#12675=CARTESIAN_POINT('Ctrl Pts',(-35.843086591684,-1.13153059083709,308.730429265905));
#12676=CARTESIAN_POINT('Ctrl Pts',(-35.7365967528101,-1.3091278227897,308.745548590452));
#12677=CARTESIAN_POINT('Ctrl Pts',(-35.6771147853955,-1.394950124037,308.753135071191));
#12678=CARTESIAN_POINT('Ctrl Pts',(-35.5955486732657,-1.49747751579554,
308.762338456356));
#12679=CARTESIAN_POINT('Ctrl Pts',(-35.5785740111191,-1.51809026146944,
308.764196117664));
#12680=CARTESIAN_POINT('Ctrl Pts',(-35.5518189085454,-1.54948388460021,
308.767031284715));
#12681=CARTESIAN_POINT('Ctrl Pts',(-35.5422818287423,-1.56046810101882,
308.768024420975));
#12682=CARTESIAN_POINT('Ctrl Pts',(-35.524244995528,-1.58085977046966,308.769869161196));
#12683=CARTESIAN_POINT('Ctrl Pts',(-35.5157703858732,-1.59028740222343,
308.770722320216));
#12684=CARTESIAN_POINT('Ctrl Pts',(-35.495014037886,-1.61300884614629,308.772780140531));
#12685=CARTESIAN_POINT('Ctrl Pts',(-35.482655050401,-1.62623079824287,308.77397909457));
#12686=CARTESIAN_POINT('Ctrl Pts',(-35.4358558556527,-1.67516276255752,
308.77842774005));
#12687=CARTESIAN_POINT('Ctrl Pts',(-35.4004470253281,-1.70993325723489,
308.781612404327));
#12688=CARTESIAN_POINT('Ctrl Pts',(-35.2988615960832,-1.80361088509888,
308.790349975863));
#12689=CARTESIAN_POINT('Ctrl Pts',(-35.2304360908608,-1.85996154405366,
308.795793965617));
#12690=CARTESIAN_POINT('Ctrl Pts',(-35.0294517869233,-2.00740194211723,
308.811077296235));
#12691=CARTESIAN_POINT('Ctrl Pts',(-34.8905789479158,-2.08902634527165,
308.820874153435));
#12692=CARTESIAN_POINT('Ctrl Pts',(-34.7083399199553,-2.17257300130964,
308.833734448743));
#12693=CARTESIAN_POINT('Ctrl Pts',(-34.6717421027349,-2.1882485176744,308.836315124534));
#12694=CARTESIAN_POINT('Ctrl Pts',(-34.61233394576,-2.21194284716722,308.840511423306));
#12695=CARTESIAN_POINT('Ctrl Pts',(-34.5897644520763,-2.22054723390368,
308.842107208608));
#12696=CARTESIAN_POINT('Ctrl Pts',(-34.5460416480166,-2.2364555874454,308.845203768806));
#12697=CARTESIAN_POINT('Ctrl Pts',(-34.5249085689044,-2.24380783147271,
308.846702733638));
#12698=CARTESIAN_POINT('Ctrl Pts',(-34.4749761263737,-2.26039123171864,
308.850251268059));
#12699=CARTESIAN_POINT('Ctrl Pts',(-34.44609856306,-2.26937252999342,308.852308813145));
#12700=CARTESIAN_POINT('Ctrl Pts',(-34.3434722823088,-2.29915080363941,
308.859643289767));
#12701=CARTESIAN_POINT('Ctrl Pts',(-34.2689025740789,-2.31692207183345,
308.865014844814));
#12702=CARTESIAN_POINT('Ctrl Pts',(-34.0699607968685,-2.35425872994888,
308.879448555513));
#12703=CARTESIAN_POINT('Ctrl Pts',(-33.9446694115968,-2.36758795579718,
308.888652647635));
#12704=CARTESIAN_POINT('Ctrl Pts',(-33.7188652186595,-2.37356872371103,
308.905139207028));
#12705=CARTESIAN_POINT('Ctrl Pts',(-33.6187293363754,-2.36988235198688,
308.912409854883));
#12706=CARTESIAN_POINT('Ctrl Pts',(-33.4927374355844,-2.3572286611839,308.921302908025));
#12707=CARTESIAN_POINT('Ctrl Pts',(-33.4664013695178,-2.35413683277247,
308.923147310719));
#12708=CARTESIAN_POINT('Ctrl Pts',(-33.4257440073174,-2.34867102171589,
308.925966683547));
#12709=CARTESIAN_POINT('Ctrl Pts',(-33.4113842059485,-2.34660625650908,
308.926957028393));
#12710=CARTESIAN_POINT('Ctrl Pts',(-33.3845016491944,-2.34248877007525,
308.92879969821));
#12711=CARTESIAN_POINT('Ctrl Pts',(-33.3719756757744,-2.34046721963082,
308.929653530175));
#12712=CARTESIAN_POINT('Ctrl Pts',(-33.3415454546462,-2.33530523906998,
308.931717159824));
#12713=CARTESIAN_POINT('Ctrl Pts',(-33.3236600595272,-2.33205935018824,
308.932921164455));
#12714=CARTESIAN_POINT('Ctrl Pts',(-33.2564835946808,-2.31906854220859,
308.937415846191));
#12715=CARTESIAN_POINT('Ctrl Pts',(-33.207465673826,-2.3079631694293,308.94063973599));
#12716=CARTESIAN_POINT('Ctrl Pts',(-33.0712250235661,-2.27251014506578,
308.949536773535));
#12717=CARTESIAN_POINT('Ctrl Pts',(-32.9849876004306,-2.24471360381062,
308.955096193031));
#12718=CARTESIAN_POINT('Ctrl Pts',(-32.7535954585549,-2.15521541119179,
308.970304752048));
#12719=CARTESIAN_POINT('Ctrl Pts',(-32.612689460885,-2.08388275956713,308.979921139783));
#12720=CARTESIAN_POINT('Ctrl Pts',(-32.4461915820827,-1.97759113447858,
308.992590229454));
#12721=CARTESIAN_POINT('Ctrl Pts',(-32.4130329258623,-1.95522262136585,
308.99518247027));
#12722=CARTESIAN_POINT('Ctrl Pts',(-32.3607517904557,-1.91799665832472,
308.999392876521));
#12723=CARTESIAN_POINT('Ctrl Pts',(-32.3412629222271,-1.90366560204967,
309.000990952808));
#12724=CARTESIAN_POINT('Ctrl Pts',(-32.3041866217484,-1.87551784264914,
309.004088845338));
#12725=CARTESIAN_POINT('Ctrl Pts',(-32.2865686646804,-1.86174549253468,
309.005586804461));
#12726=CARTESIAN_POINT('Ctrl Pts',(-32.2456607655036,-1.82882440575581,
309.009127987267));
#12727=CARTESIAN_POINT('Ctrl Pts',(-32.2225364958187,-1.80947698812294,
309.011179090235));
#12728=CARTESIAN_POINT('Ctrl Pts',(-32.1425164137073,-1.73989062023005,
309.01845670784));
#12729=CARTESIAN_POINT('Ctrl Pts',(-32.0876742642693,-1.68737126940459,
309.023775860508));
#12730=CARTESIAN_POINT('Ctrl Pts',(-31.9442990663464,-1.53623492793395,
309.038625039011));
#12731=CARTESIAN_POINT('Ctrl Pts',(-31.8613642150596,-1.43269210616283,
309.048326108341));
#12732=CARTESIAN_POINT('Ctrl Pts',(-31.730012592139,-1.23720934648075,309.06550529934));
#12733=CARTESIAN_POINT('Ctrl Pts',(-31.6781484869623,-1.14797047469972,
309.07297686459));
#12734=CARTESIAN_POINT('Ctrl Pts',(-31.622466512533,-1.03594128383417,309.081706291512));
#12735=CARTESIAN_POINT('Ctrl Pts',(-31.6129538847782,-1.01611539922906,
309.083227379392));
#12736=CARTESIAN_POINT('Ctrl Pts',(-31.5980864155893,-0.983991140975836,
309.085650720084));
#12737=CARTESIAN_POINT('Ctrl Pts',(-31.5925580023527,-0.97177515097817,
309.086562771749));
#12738=CARTESIAN_POINT('Ctrl Pts',(-31.5817539469891,-0.947352408465521,
309.088366424335));
#12739=CARTESIAN_POINT('Ctrl Pts',(-31.5764767853174,-0.93514689788185,
309.089258081777));
#12740=CARTESIAN_POINT('Ctrl Pts',(-31.5629511307058,-0.903126885636739,
309.091573551144));
#12741=CARTESIAN_POINT('Ctrl Pts',(-31.5548682273033,-0.883243149365324,
309.09298786618));
#12742=CARTESIAN_POINT('Ctrl Pts',(-31.5139528442966,-0.778540198584335,
309.10032657504));
#12743=CARTESIAN_POINT('Ctrl Pts',(-31.4857458779241,-0.691984869993243,
309.106023944894));
#12744=CARTESIAN_POINT('Ctrl Pts',(-31.41018886941,-0.405081611302546,309.124360917937));
#12745=CARTESIAN_POINT('Ctrl Pts',(-31.3839053947335,-0.200195316159489,
309.13669300718));
#12746=CARTESIAN_POINT('Ctrl Pts',(-31.3844702155783,0.0428572830394322,
309.152324877307));
#12747=CARTESIAN_POINT('Ctrl Pts',(-31.3854390539761,0.0801939125581355,
309.154750919709));
#12748=CARTESIAN_POINT('Ctrl Pts',(-31.3884611229818,0.141124724174767,
309.158758888039));
#12749=CARTESIAN_POINT('Ctrl Pts',(-31.3899869402004,0.164739315477346,
309.160324218774));
#12750=CARTESIAN_POINT('Ctrl Pts',(-31.393660131062,0.210852774566611,309.163406315914));
#12751=CARTESIAN_POINT('Ctrl Pts',(-31.3957762725766,0.233351626760168,
309.164921936481));
#12752=CARTESIAN_POINT('Ctrl Pts',(-31.4016279917619,0.287288205038647,
309.168585413533));
#12753=CARTESIAN_POINT('Ctrl Pts',(-31.4056720857848,0.318687338442184,
309.170742759238));
#12754=CARTESIAN_POINT('Ctrl Pts',(-31.4234890987241,0.438102982988947,
309.179045944625));
#12755=CARTESIAN_POINT('Ctrl Pts',(-31.4415869102768,0.525389936095793,
309.185323921831));
#12756=CARTESIAN_POINT('Ctrl Pts',(-31.5155473352017,0.802580054170454,
309.205907855014));
#12757=CARTESIAN_POINT('Ctrl Pts',(-31.5902538657047,0.986569568588838,
309.220645267947));
#12758=CARTESIAN_POINT('Ctrl Pts',(-31.7038788840297,1.18940258691148,309.237108940261));
#12759=CARTESIAN_POINT('Ctrl Pts',(-31.7214920819501,1.21928745545428,309.239538216271));
#12760=CARTESIAN_POINT('Ctrl Pts',(-31.7481213687615,1.26228515095993,309.243027246618));
#12761=CARTESIAN_POINT('Ctrl Pts',(-31.7566230287568,1.27570934090378,309.244115640839));
#12762=CARTESIAN_POINT('Ctrl Pts',(-31.7720554332601,1.29954389762906,309.246045040158));
#12763=CARTESIAN_POINT('Ctrl Pts',(-31.778934372778,1.30998612840426,309.246889156785));
#12764=CARTESIAN_POINT('Ctrl Pts',(-31.7948918446053,1.33379748643985,309.248811488785));
#12765=CARTESIAN_POINT('Ctrl Pts',(-31.8040248426327,1.34712890034042,309.249886108115));
#12766=CARTESIAN_POINT('Ctrl Pts',(-31.8340965072962,1.39007632419035,309.253346307005));
#12767=CARTESIAN_POINT('Ctrl Pts',(-31.8555794189489,1.41930709614109,309.255698722066));
#12768=CARTESIAN_POINT('Ctrl Pts',(-31.9922506111046,1.59659788922086,309.270028442402));
#12769=CARTESIAN_POINT('Ctrl Pts',(-32.1240057784157,1.73106326631051,309.28121503426));
#12770=CARTESIAN_POINT('Ctrl Pts',(-32.282649683095,1.85857901681812,309.293822207718));
#12771=CARTESIAN_POINT('Ctrl Pts',(-32.2951564162165,1.86842615819068,309.294810559461));
#12772=CARTESIAN_POINT('Ctrl Pts',(-32.3721397861375,1.92779324118059,309.300864819143));
#12773=CARTESIAN_POINT('Ctrl Pts',(-32.4390226271458,1.97409256572256,309.306002727732));
#12774=CARTESIAN_POINT('Ctrl Pts',(-32.5349622722325,2.03345744506234,309.313309597567));
#12775=CARTESIAN_POINT('Ctrl Pts',(-32.5621060663155,2.04951368137794,309.315369929092));
#12776=CARTESIAN_POINT('Ctrl Pts',(-32.6090239533855,2.07601837801412,309.318924330877));
#12777=CARTESIAN_POINT('Ctrl Pts',(-32.628640892351,2.08673733977612,309.320408456484));
#12778=CARTESIAN_POINT('Ctrl Pts',(-32.6555678616768,2.10096006507135,309.322443973274));
#12779=CARTESIAN_POINT('Ctrl Pts',(-32.6627490318879,2.10470620870534,309.322986666663));
#12780=CARTESIAN_POINT('Ctrl Pts',(-32.6699490796625,2.10841540807375,309.323530658174));
#12781=CARTESIAN_POINT('Origin',(-33.7561270252576,0.,302.151410108095));
#12782=CARTESIAN_POINT('',(-32.6699490276577,2.10841538128279,310.521403445152));
#12783=CARTESIAN_POINT('',(-32.6699491957805,2.10841546789345,310.326187962698));
#12784=CARTESIAN_POINT('',(-32.6699490794746,2.10841540797695,302.151410108095));
#12785=CARTESIAN_POINT('Ctrl Pts',(-32.6699490276577,2.10841538128279,310.521403445152));
#12786=CARTESIAN_POINT('Ctrl Pts',(-32.617780915958,2.081540290346,310.517169465957));
#12787=CARTESIAN_POINT('Ctrl Pts',(-32.5666123539571,2.05273010432393,310.51298201885));
#12788=CARTESIAN_POINT('Ctrl Pts',(-32.4979212472925,2.01062024751867,310.507361136708));
#12789=CARTESIAN_POINT('Ctrl Pts',(-32.4794493984791,1.99894219094549,310.50584972901));
#12790=CARTESIAN_POINT('Ctrl Pts',(-32.4499314133711,1.97970455000854,310.503437935968));
#12791=CARTESIAN_POINT('Ctrl Pts',(-32.4387837130318,1.97230416058991,310.502527910406));
#12792=CARTESIAN_POINT('Ctrl Pts',(-32.4166595225342,1.95734576613111,310.500724403869));
#12793=CARTESIAN_POINT('Ctrl Pts',(-32.4056829259026,1.94978880766032,310.499830912042));
#12794=CARTESIAN_POINT('Ctrl Pts',(-32.3770857407382,1.92974340384591,310.497504849177));
#12795=CARTESIAN_POINT('Ctrl Pts',(-32.3595705563464,1.91710578218941,310.496081936501));
#12796=CARTESIAN_POINT('Ctrl Pts',(-32.2718341734271,1.85196121953167,310.488949619804));
#12797=CARTESIAN_POINT('Ctrl Pts',(-32.204383184779,1.79582294601288,310.483449646956));
#12798=CARTESIAN_POINT('Ctrl Pts',(-32.0344935085815,1.63768951961566,310.469090477362));
#12799=CARTESIAN_POINT('Ctrl Pts',(-31.9380037174788,1.52986176405891,310.460373753602));
#12800=CARTESIAN_POINT('Ctrl Pts',(-31.8047547888782,1.35040866805719,310.446429939693));
#12801=CARTESIAN_POINT('Ctrl Pts',(-31.7608022339661,1.28457551727009,310.441420304982));
#12802=CARTESIAN_POINT('Ctrl Pts',(-31.7045524684001,1.19045081722967,310.434309054721));
#12803=CARTESIAN_POINT('Ctrl Pts',(-31.689389946886,1.16392827029874,310.432310892572));
#12804=CARTESIAN_POINT('Ctrl Pts',(-31.6639942893277,1.11744415155062,310.428814106828));
#12805=CARTESIAN_POINT('Ctrl Pts',(-31.653524015766,1.09761620895728,310.427324168857));
#12806=CARTESIAN_POINT('Ctrl Pts',(-31.6324151246718,1.05623084753417,310.424216064531));
#12807=CARTESIAN_POINT('Ctrl Pts',(-31.6218200309869,1.03465425145406,310.422596578696));
#12808=CARTESIAN_POINT('Ctrl Pts',(-31.5948051394383,0.977457907023186,
310.418304192467));
#12809=CARTESIAN_POINT('Ctrl Pts',(-31.5789383935358,0.941586744168151,
310.415612719643));
#12810=CARTESIAN_POINT('Ctrl Pts',(-31.4999109302933,0.750232567186608,
310.401249844646));
#12811=CARTESIAN_POINT('Ctrl Pts',(-31.4525059583483,0.588788427757955,
310.389065074152));
#12812=CARTESIAN_POINT('Ctrl Pts',(-31.4074573577671,0.340691815975887,
310.370646577878));
#12813=CARTESIAN_POINT('Ctrl Pts',(-31.3968220638381,0.256907712542552,
310.36448710201));
#12814=CARTESIAN_POINT('Ctrl Pts',(-31.3882549757538,0.13958673197959,310.356069232012));
#12815=CARTESIAN_POINT('Ctrl Pts',(-31.3865314368517,0.106392994363063,
310.353710832094));
#12816=CARTESIAN_POINT('Ctrl Pts',(-31.3847186964737,0.0476642880044788,
310.349590938743));
#12817=CARTESIAN_POINT('Ctrl Pts',(-31.38434307016,0.022143813624543,310.347818238616));
#12818=CARTESIAN_POINT('Ctrl Pts',(-31.384399591134,-0.0175286482664451,
310.345094803976));
#12819=CARTESIAN_POINT('Ctrl Pts',(-31.3845463736195,-0.031678289113071,
310.34412984637));
#12820=CARTESIAN_POINT('Ctrl Pts',(-31.3850646141794,-0.0584949798600393,
310.34231420799));
#12821=CARTESIAN_POINT('Ctrl Pts',(-31.3854109611377,-0.0711615784911806,
310.341462298766));
#12822=CARTESIAN_POINT('Ctrl Pts',(-31.3864178424604,-0.0996325236566917,
310.339559207885));
#12823=CARTESIAN_POINT('Ctrl Pts',(-31.3871350129761,-0.115434527747098,
310.33851106161));
#12824=CARTESIAN_POINT('Ctrl Pts',(-31.3898283746748,-0.164038186627979,
310.335308886666));
#12825=CARTESIAN_POINT('Ctrl Pts',(-31.392328262113,-0.196808244752479,
310.333180322093));
#12826=CARTESIAN_POINT('Ctrl Pts',(-31.4144484664309,-0.424317445746433,
310.318548859895));
#12827=CARTESIAN_POINT('Ctrl Pts',(-31.4574288397828,-0.616041280208117,
310.306910859396));
#12828=CARTESIAN_POINT('Ctrl Pts',(-31.5534541068269,-0.883921612430742,
310.289237425773));
#12829=CARTESIAN_POINT('Ctrl Pts',(-31.5880913327436,-0.965766077800881,
310.283639208161));
#12830=CARTESIAN_POINT('Ctrl Pts',(-31.6411756006865,-1.07386172696808,
310.275840741928));
#12831=CARTESIAN_POINT('Ctrl Pts',(-31.6556842466148,-1.10197028766911,
310.273774418547));
#12832=CARTESIAN_POINT('Ctrl Pts',(-31.6815129759689,-1.14964565064975,
310.27019815604));
#12833=CARTESIAN_POINT('Ctrl Pts',(-31.6925588526082,-1.1693566232149,310.268698070947));
#12834=CARTESIAN_POINT('Ctrl Pts',(-31.7157514323762,-1.20939073344391,
310.26560526524));
#12835=CARTESIAN_POINT('Ctrl Pts',(-31.7279241776211,-1.22969575271207,
310.264011722006));
#12836=CARTESIAN_POINT('Ctrl Pts',(-31.7601028662256,-1.28159425467662,
310.259872166975));
#12837=CARTESIAN_POINT('Ctrl Pts',(-31.7805550331742,-1.31290186374438,
310.25730995041));
#12838=CARTESIAN_POINT('Ctrl Pts',(-31.918175971827,-1.51306752384813,310.240490268461));
#12839=CARTESIAN_POINT('Ctrl Pts',(-32.0561170340056,-1.66654484642878,
310.22541216027));
#12840=CARTESIAN_POINT('Ctrl Pts',(-32.28118636391,-1.8595809317406,310.203827328488));
#12841=CARTESIAN_POINT('Ctrl Pts',(-32.3536758489939,-1.91484341022577,
310.197257402625));
#12842=CARTESIAN_POINT('Ctrl Pts',(-32.4469648231921,-1.97781527856887,
310.189409940672));
#12843=CARTESIAN_POINT('Ctrl Pts',(-32.4649216413154,-1.989584802377,310.187925793156));
#12844=CARTESIAN_POINT('Ctrl Pts',(-32.4942570836578,-2.00824778589239,
310.185546630712));
#12845=CARTESIAN_POINT('Ctrl Pts',(-32.5055378137275,-2.01529193096849,
310.184642414137));
#12846=CARTESIAN_POINT('Ctrl Pts',(-32.5283098034614,-2.02924683297065,
310.18283936426));
#12847=CARTESIAN_POINT('Ctrl Pts',(-32.5398015859561,-2.03615576203388,
310.181940655409));
#12848=CARTESIAN_POINT('Ctrl Pts',(-32.5702890977271,-2.05413480949034,
310.179584081289));
#12849=CARTESIAN_POINT('Ctrl Pts',(-32.5893817081587,-2.06503919017128,
310.17813634446));
#12850=CARTESIAN_POINT('Ctrl Pts',(-32.6982681886916,-2.12523524382535,
310.17002116307));
#12851=CARTESIAN_POINT('Ctrl Pts',(-32.791039864022,-2.16894027257489,310.163642523094));
#12852=CARTESIAN_POINT('Ctrl Pts',(-33.010013260102,-2.25525587068017,310.149146265593));
#12853=CARTESIAN_POINT('Ctrl Pts',(-33.1375441976546,-2.29351680066534,
310.141092421946));
#12854=CARTESIAN_POINT('Ctrl Pts',(-33.3420126780833,-2.33655489296651,
310.128036637481));
#12855=CARTESIAN_POINT('Ctrl Pts',(-33.4171214203097,-2.34862788633159,
310.123214762106));
#12856=CARTESIAN_POINT('Ctrl Pts',(-33.5226563965961,-2.3604236123529,310.116324136595));
#12857=CARTESIAN_POINT('Ctrl Pts',(-33.5526976167911,-2.36320217159593,
310.114350012421));
#12858=CARTESIAN_POINT('Ctrl Pts',(-33.6050885953104,-2.36704154711581,
310.110880929024));
#12859=CARTESIAN_POINT('Ctrl Pts',(-33.6274159413871,-2.36836054930079,
310.109394249748));
#12860=CARTESIAN_POINT('Ctrl Pts',(-33.6739188965614,-2.37044823043038,
310.106279035273));
#12861=CARTESIAN_POINT('Ctrl Pts',(-33.6980941896539,-2.37116323858992,
310.104648989197));
#12862=CARTESIAN_POINT('Ctrl Pts',(-33.7622348184521,-2.37207880041941,
310.100294384748));
#12863=CARTESIAN_POINT('Ctrl Pts',(-33.8021999788263,-2.37163911379809,
310.097550256542));
#12864=CARTESIAN_POINT('Ctrl Pts',(-34.0346691661393,-2.36320361995575,
310.081399749584));
#12865=CARTESIAN_POINT('Ctrl Pts',(-34.2256086487502,-2.33278338072927,
310.067296242362));
#12866=CARTESIAN_POINT('Ctrl Pts',(-34.4981928041521,-2.2545106110892,310.046623919629));
#12867=CARTESIAN_POINT('Ctrl Pts',(-34.5841519206054,-2.22437800336578,
310.040036786114));
#12868=CARTESIAN_POINT('Ctrl Pts',(-34.6919713809225,-2.17946278782804,
310.031844271626));
#12869=CARTESIAN_POINT('Ctrl Pts',(-34.715607614713,-2.16916109030955,310.030052994054));
#12870=CARTESIAN_POINT('Ctrl Pts',(-34.7519982980303,-2.15258918511878,
310.027307527367));
#12871=CARTESIAN_POINT('Ctrl Pts',(-34.7648715433247,-2.14658666615213,
310.02633876429));
#12872=CARTESIAN_POINT('Ctrl Pts',(-34.7891068588569,-2.13502008099317,
310.024520679855));
#12873=CARTESIAN_POINT('Ctrl Pts',(-34.8004794344954,-2.12948024999071,
310.023670062994));
#12874=CARTESIAN_POINT('Ctrl Pts',(-34.8258863576674,-2.11685148829953,
310.021774435141));
#12875=CARTESIAN_POINT('Ctrl Pts',(-34.8398958554453,-2.1097133474959,310.020732376939));
#12876=CARTESIAN_POINT('Ctrl Pts',(-34.8898555805891,-2.08362878467335,
310.017024047034));
#12877=CARTESIAN_POINT('Ctrl Pts',(-34.9253905723551,-2.06389742002811,
310.014400970146));
#12878=CARTESIAN_POINT('Ctrl Pts',(-34.9931603596588,-2.023954634972,310.00939247732));
#12879=CARTESIAN_POINT('Ctrl Pts',(-35.0254498462756,-2.00386218565342,
310.007003390462));
#12880=CARTESIAN_POINT('Ctrl Pts',(-35.1895291822863,-1.89620398754174,
309.994775976132));
#12881=CARTESIAN_POINT('Ctrl Pts',(-35.3127987851945,-1.79638725481243,
309.985265583974));
#12882=CARTESIAN_POINT('Ctrl Pts',(-35.4837163132796,-1.6270875709388,309.970281224965));
#12883=CARTESIAN_POINT('Ctrl Pts',(-35.5391561431348,-1.56613657863932,
309.965075060634));
#12884=CARTESIAN_POINT('Ctrl Pts',(-35.6109034908421,-1.47849887648018,
309.957733631995));
#12885=CARTESIAN_POINT('Ctrl Pts',(-35.6300252628258,-1.45418702860978,
309.955711518031));
#12886=CARTESIAN_POINT('Ctrl Pts',(-35.6622151622646,-1.41157056585536,
309.952186948418));
#12887=CARTESIAN_POINT('Ctrl Pts',(-35.6755087130556,-1.39344082244651,
309.950693585776));
#12888=CARTESIAN_POINT('Ctrl Pts',(-35.7023994313485,-1.35565224532729,
309.947591621277));
#12889=CARTESIAN_POINT('Ctrl Pts',(-35.7159610958578,-1.33597141879378,
309.945981881709));
#12890=CARTESIAN_POINT('Ctrl Pts',(-35.7506051559474,-1.28403267474382,
309.941746880429));
#12891=CARTESIAN_POINT('Ctrl Pts',(-35.771202121143,-1.2514611374297,309.939103948812));
#12892=CARTESIAN_POINT('Ctrl Pts',(-35.8937173743332,-1.04684719610391,
309.922570431501));
#12893=CARTESIAN_POINT('Ctrl Pts',(-35.9743155376931,-0.863013479281199,
309.907914220209));
#12894=CARTESIAN_POINT('Ctrl Pts',(-36.0575260875028,-0.581047003459746,
309.886500232778));
#12895=CARTESIAN_POINT('Ctrl Pts',(-36.0787686025283,-0.489278039980603,
309.879703371807));
#12896=CARTESIAN_POINT('Ctrl Pts',(-36.0981141772791,-0.37518124770799,
309.871633084149));
#12897=CARTESIAN_POINT('Ctrl Pts',(-36.1014346233969,-0.353832082105871,
309.870139296852));
#12898=CARTESIAN_POINT('Ctrl Pts',(-36.1063310679241,-0.31924385277318,
309.867748600777));
#12899=CARTESIAN_POINT('Ctrl Pts',(-36.1080879124043,-0.306032168361609,
309.866842336293));
#12900=CARTESIAN_POINT('Ctrl Pts',(-36.1111846713285,-0.281140080896377,
309.865148723406));
#12901=CARTESIAN_POINT('Ctrl Pts',(-36.1125492768417,-0.269463260520901,
309.864359978435));
#12902=CARTESIAN_POINT('Ctrl Pts',(-36.1160241749421,-0.237680810853592,
309.86222751003));
#12903=CARTESIAN_POINT('Ctrl Pts',(-36.117964386681,-0.21755705313128,309.86089290033));
#12904=CARTESIAN_POINT('Ctrl Pts',(-36.1250835619893,-0.132321735545387,
309.85529666732));
#12905=CARTESIAN_POINT('Ctrl Pts',(-36.127829502897,-0.0670302973384229,
309.851149010829));
#12906=CARTESIAN_POINT('Ctrl Pts',(-36.1279901248444,0.15664866291237,309.837165036705));
#12907=CARTESIAN_POINT('Ctrl Pts',(-36.1122453066982,0.314617161043366,
309.82765056468));
#12908=CARTESIAN_POINT('Ctrl Pts',(-36.0637290767035,0.554671677968412,
309.812434591545));
#12909=CARTESIAN_POINT('Ctrl Pts',(-36.041956299146,0.638490476428677,309.806978345435));
#12910=CARTESIAN_POINT('Ctrl Pts',(-36.0058908939347,0.751526639243565,
309.799299896309));
#12911=CARTESIAN_POINT('Ctrl Pts',(-35.9955073882524,0.781924025417422,
309.797202709811));
#12912=CARTESIAN_POINT('Ctrl Pts',(-35.9768223499762,0.833195326432809,
309.793604928395));
#12913=CARTESIAN_POINT('Ctrl Pts',(-35.9688355628786,0.854179750292814,
309.792114921734));
#12914=CARTESIAN_POINT('Ctrl Pts',(-35.9518895487267,0.896870280810288,
309.789046041881));
#12915=CARTESIAN_POINT('Ctrl Pts',(-35.9429034979679,0.918562980672566,
309.787466397287));
#12916=CARTESIAN_POINT('Ctrl Pts',(-35.9191653445074,0.973544502085842,
309.78340905261));
#12917=CARTESIAN_POINT('Ctrl Pts',(-35.9039665027997,1.00663250020668,309.780916374907));
#12918=CARTESIAN_POINT('Ctrl Pts',(-35.8689862834002,1.07838253660604,309.77539523487));
#12919=CARTESIAN_POINT('Ctrl Pts',(-35.8488927916008,1.11687697673336,309.772357032586));
#12920=CARTESIAN_POINT('Ctrl Pts',(-35.7820062703195,1.23686697344908,309.762643709851));
#12921=CARTESIAN_POINT('Ctrl Pts',(-35.7314247626472,1.3161392637049,309.755857333316));
#12922=CARTESIAN_POINT('Ctrl Pts',(-35.584849297343,1.51829988738251,309.737663284056));
#12923=CARTESIAN_POINT('Ctrl Pts',(-35.4812135343735,1.6350971198002,309.726177842687));
#12924=CARTESIAN_POINT('Ctrl Pts',(-35.3490517307395,1.75737818226608,309.713573402676));
#12925=CARTESIAN_POINT('Ctrl Pts',(-35.3309828979073,1.7735885340657,309.711889712769));
#12926=CARTESIAN_POINT('Ctrl Pts',(-35.302186875315,1.79863558047589,309.709272100488));
#12927=CARTESIAN_POINT('Ctrl Pts',(-35.2916259955825,1.80765979877798,309.708325589834));
#12928=CARTESIAN_POINT('Ctrl Pts',(-35.2710706828736,1.82491407084933,309.706510234453));
#12929=CARTESIAN_POINT('Ctrl Pts',(-35.2610872020172,1.83315589274702,309.705640638796));
#12930=CARTESIAN_POINT('Ctrl Pts',(-35.2357418108779,1.85373306285923,309.703461926363));
#12931=CARTESIAN_POINT('Ctrl Pts',(-35.2202923185473,1.86595987085937,309.702160255518));
#12932=CARTESIAN_POINT('Ctrl Pts',(-35.1535232965387,1.91746125030801,309.696637764405));
#12933=CARTESIAN_POINT('Ctrl Pts',(-35.1007583533388,1.95482534751463,309.692529715554));
#12934=CARTESIAN_POINT('Ctrl Pts',(-34.9209647787354,2.07141176346231,309.679121170559));
#12935=CARTESIAN_POINT('Ctrl Pts',(-34.7879732710474,2.14076875919909,309.670111006596));
#12936=CARTESIAN_POINT('Ctrl Pts',(-34.6294057650476,2.20523122917619,309.659512528632));
#12937=CARTESIAN_POINT('Ctrl Pts',(-34.6093750269977,2.21305859674719,309.658176665385));
#12938=CARTESIAN_POINT('Ctrl Pts',(-34.5164118667015,2.24793586736593,309.651982829893));
#12939=CARTESIAN_POINT('Ctrl Pts',(-34.4422891007593,2.27165765831294,309.647058934433));
#12940=CARTESIAN_POINT('Ctrl Pts',(-34.3370435804155,2.29971828706415,309.640000871605));
#12941=CARTESIAN_POINT('Ctrl Pts',(-34.3067932792655,2.3071486236396,309.637964966859));
#12942=CARTESIAN_POINT('Ctrl Pts',(-34.2544394194209,2.31891995768009,309.634424325861));
#12943=CARTESIAN_POINT('Ctrl Pts',(-34.2324037432807,2.32354587658817,309.632928918703));
#12944=CARTESIAN_POINT('Ctrl Pts',(-34.1869208595193,2.33241986476121,309.629830098033));
#12945=CARTESIAN_POINT('Ctrl Pts',(-34.1634688906183,2.33662968519359,309.628225647786));
#12946=CARTESIAN_POINT('Ctrl Pts',(-34.1022997063071,2.34666121141518,309.624021795088));
#12947=CARTESIAN_POINT('Ctrl Pts',(-34.0644996728687,2.35192695081531,309.62140520576));
#12948=CARTESIAN_POINT('Ctrl Pts',(-33.8919688502865,2.37173078929483,309.609370475106));
#12949=CARTESIAN_POINT('Ctrl Pts',(-33.756290696015,2.37561561810063,309.599632185729));
#12950=CARTESIAN_POINT('Ctrl Pts',(-33.4675075478428,2.35914108231101,309.578551909545));
#12951=CARTESIAN_POINT('Ctrl Pts',(-33.3151791031411,2.33546977943752,309.567217484439));
#12952=CARTESIAN_POINT('Ctrl Pts',(-33.1424761454034,2.29112002416459,309.554731548541));
#12953=CARTESIAN_POINT('Ctrl Pts',(-33.1188396788813,2.28465825093942,309.553031529024));
#12954=CARTESIAN_POINT('Ctrl Pts',(-33.0819199664729,2.27394748943518,309.550394472026));
#12955=CARTESIAN_POINT('Ctrl Pts',(-33.0685675297594,2.26994588214746,309.549444552077));
#12956=CARTESIAN_POINT('Ctrl Pts',(-33.0429083355688,2.26200885794384,309.547627481613));
#12957=CARTESIAN_POINT('Ctrl Pts',(-33.0305972661729,2.2580902439807,309.546759515801));
#12958=CARTESIAN_POINT('Ctrl Pts',(-32.9997299133956,2.24798666186072,309.54459165892));
#12959=CARTESIAN_POINT('Ctrl Pts',(-32.9812164482368,2.24167220678584,309.54329905416));
#12960=CARTESIAN_POINT('Ctrl Pts',(-32.903340755563,2.21403073670725,309.537885645701));
#12961=CARTESIAN_POINT('Ctrl Pts',(-32.8447587004936,2.19056745362947,309.533872113895));
#12962=CARTESIAN_POINT('Ctrl Pts',(-32.7475764827858,2.14706921873693,309.527203448312));
#12963=CARTESIAN_POINT('Ctrl Pts',(-32.7084862560888,2.12826834459275,309.524518071325));
#12964=CARTESIAN_POINT('Ctrl Pts',(-32.6699489539077,2.1084153432895,309.521847592916));
#12965=CARTESIAN_POINT('',(-36.1278762480309,-0.000944544423845245,309.649405795056));
#12966=CARTESIAN_POINT('Ctrl Pts',(-32.6699490796625,2.10841540807375,309.323530658174));
#12967=CARTESIAN_POINT('Ctrl Pts',(-32.6837670278073,2.11553390591377,309.324574657703));
#12968=CARTESIAN_POINT('Ctrl Pts',(-32.6976545041501,2.12251633343421,309.325623441197));
#12969=CARTESIAN_POINT('Ctrl Pts',(-32.7450521640656,2.14576634592794,309.329201953145));
#12970=CARTESIAN_POINT('Ctrl Pts',(-32.7788748771904,2.16138001081334,309.331754045084));
#12971=CARTESIAN_POINT('Ctrl Pts',(-32.8541195406299,2.19398816596706,309.33743146526));
#12972=CARTESIAN_POINT('Ctrl Pts',(-32.8956826396133,2.21061905175698,309.340567493712));
#12973=CARTESIAN_POINT('Ctrl Pts',(-33.0308283563419,2.26030693599979,309.350762875372));
#12974=CARTESIAN_POINT('Ctrl Pts',(-33.1260166795685,2.28866845150412,309.357946347631));
#12975=CARTESIAN_POINT('Ctrl Pts',(-33.3644469287239,2.34370424693655,309.375795128266));
#12976=CARTESIAN_POINT('Ctrl Pts',(-33.5089202630452,2.36331499526615,309.38649634971));
#12977=CARTESIAN_POINT('Ctrl Pts',(-33.679639658142,2.37065215195957,309.398475664489));
#12978=CARTESIAN_POINT('Ctrl Pts',(-33.7050082096984,2.37133484339931,309.400237987235));
#12979=CARTESIAN_POINT('Ctrl Pts',(-33.7445023091299,2.37176353723193,309.402949064332));
#12980=CARTESIAN_POINT('Ctrl Pts',(-33.7586220923958,2.37179071821195,309.40391184773));
#12981=CARTESIAN_POINT('Ctrl Pts',(-33.7855711077937,2.37160192899248,309.405736002992));
#12982=CARTESIAN_POINT('Ctrl Pts',(-33.7983995662419,2.37140795800151,309.406598428723));
#12983=CARTESIAN_POINT('Ctrl Pts',(-33.8302816621777,2.37066709246916,309.40872826764));
#12984=CARTESIAN_POINT('Ctrl Pts',(-33.849331968908,2.36999457172687,309.409988950329));
#12985=CARTESIAN_POINT('Ctrl Pts',(-33.9263358677854,2.36634618465872,309.415043980755));
#12986=CARTESIAN_POINT('Ctrl Pts',(-33.9841837939127,2.36147339752557,309.418748075766));
#12987=CARTESIAN_POINT('Ctrl Pts',(-34.1592156250369,2.34023655905682,309.429827470924));
#12988=CARTESIAN_POINT('Ctrl Pts',(-34.2754079031037,2.31722637098704,309.437012990825));
#12989=CARTESIAN_POINT('Ctrl Pts',(-34.5147457740534,2.25091366793179,309.452257173774));
#12990=CARTESIAN_POINT('Ctrl Pts',(-34.6370043581484,2.20593839645373,309.46031087037));
#12991=CARTESIAN_POINT('Ctrl Pts',(-34.786648644744,2.13645605753466,309.470950817336));
#12992=CARTESIAN_POINT('Ctrl Pts',(-34.818014148158,2.12104097693873,309.473225980454));
#12993=CARTESIAN_POINT('Ctrl Pts',(-34.8696117392651,2.09425114209687,309.477051216784));
#12994=CARTESIAN_POINT('Ctrl Pts',(-34.8900385637574,2.08326201249233,309.478587651));
#12995=CARTESIAN_POINT('Ctrl Pts',(-34.930326706358,2.06081990278973,309.48166402222));
#12996=CARTESIAN_POINT('Ctrl Pts',(-34.9501896520774,2.04937501252228,309.483203544001));
#12997=CARTESIAN_POINT('Ctrl Pts',(-34.9986690005221,2.02049750079732,309.487019258701));
#12998=CARTESIAN_POINT('Ctrl Pts',(-35.0270870577989,2.0027433950187,309.489306995416));
#12999=CARTESIAN_POINT('Ctrl Pts',(-35.1481737362104,1.9234796334618,309.4992832111));
#13000=CARTESIAN_POINT('Ctrl Pts',(-35.236816040945,1.85610390644244,309.507186323455));
#13001=CARTESIAN_POINT('Ctrl Pts',(-35.3910244388719,1.72079562743263,309.522031054723));
#13002=CARTESIAN_POINT('Ctrl Pts',(-35.457906786202,1.65468179327469,309.528916817575));
#13003=CARTESIAN_POINT('Ctrl Pts',(-35.5864278181724,1.51158079860509,309.542937993197));
#13004=CARTESIAN_POINT('Ctrl Pts',(-35.6475558899725,1.43435641010294,309.550056579666));
#13005=CARTESIAN_POINT('Ctrl Pts',(-35.7162397633653,1.3355290221792,309.558453820506));
#13006=CARTESIAN_POINT('Ctrl Pts',(-35.7285144458637,1.31733354366597,309.55997197576));
#13007=CARTESIAN_POINT('Ctrl Pts',(-35.7478739155931,1.28775849014213,309.562391805709));
#13008=CARTESIAN_POINT('Ctrl Pts',(-35.7551175980459,1.27648514147036,309.563303231245));
#13009=CARTESIAN_POINT('Ctrl Pts',(-35.7693628508485,1.25389656633207,309.565106792945));
#13010=CARTESIAN_POINT('Ctrl Pts',(-35.7763655046659,1.24258263102299,309.565998972036));
#13011=CARTESIAN_POINT('Ctrl Pts',(-35.7944343383787,1.21283290666031,309.568317518116));
#13012=CARTESIAN_POINT('Ctrl Pts',(-35.8053459783039,1.19430403396777,309.569734341045));
#13013=CARTESIAN_POINT('Ctrl Pts',(-35.8615069496667,1.0959015860009,309.577130488354));
#13014=CARTESIAN_POINT('Ctrl Pts',(-35.9023475588104,1.0135907143416,309.582878455362));
#13015=CARTESIAN_POINT('Ctrl Pts',(-35.9725480215865,0.848711841000923,
309.593950944079));
#13016=CARTESIAN_POINT('Ctrl Pts',(-36.0023104729367,0.766481700466652,
309.599274457109));
#13017=CARTESIAN_POINT('Ctrl Pts',(-36.0479015141048,0.614821737788254,
309.609006589604));
#13018=CARTESIAN_POINT('Ctrl Pts',(-36.0652728854282,0.545967628761038,
309.613393822181));
#13019=CARTESIAN_POINT('Ctrl Pts',(-36.0925180552505,0.413104409625198,
309.621918089787));
#13020=CARTESIAN_POINT('Ctrl Pts',(-36.1029097526244,0.349267828244329,
309.626038783868));
#13021=CARTESIAN_POINT('Ctrl Pts',(-36.1141506117227,0.256429903997621,
309.632115709324));
#13022=CARTESIAN_POINT('Ctrl Pts',(-36.1170971204671,0.227709507052592,
309.634007040841));
#13023=CARTESIAN_POINT('Ctrl Pts',(-36.1213347166058,0.177368079683672,
309.637345736844));
#13024=CARTESIAN_POINT('Ctrl Pts',(-36.122855290686,0.155769455874528,309.638785727079));
#13025=CARTESIAN_POINT('Ctrl Pts',(-36.1253583088053,0.111588552168876,
309.641748104397));
#13026=CARTESIAN_POINT('Ctrl Pts',(-36.1263140563778,0.0890070546941616,
309.643271178472));
#13027=CARTESIAN_POINT('Ctrl Pts',(-36.1275758177347,0.0439665759513204,
309.646328070369));
#13028=CARTESIAN_POINT('Ctrl Pts',(-36.1278857981901,0.0215101600079903,
309.647861594863));
#13029=CARTESIAN_POINT('Ctrl Pts',(-36.1278768363983,-0.000946495695927301,
309.649404906755));
#13030=CARTESIAN_POINT('Ctrl Pts',(-36.1278768371482,-0.000944614581569902,
309.649404777478));
#13031=CARTESIAN_POINT('Ctrl Pts',(-36.1278663893725,-0.0271770173666605,
309.651207573291));
#13032=CARTESIAN_POINT('Ctrl Pts',(-36.127420733878,-0.0534067147285239,
309.653023524514));
#13033=CARTESIAN_POINT('Ctrl Pts',(-36.1194844509716,-0.289673589458124,
309.669503194538));
#13034=CARTESIAN_POINT('Ctrl Pts',(-36.0845391621194,-0.497831258028484,
309.685015777814));
#13035=CARTESIAN_POINT('Ctrl Pts',(-36.0075251207054,-0.747691639858987,
309.703970158497));
#13036=CARTESIAN_POINT('Ctrl Pts',(-35.9908047306328,-0.796274034546403,
309.707665456643));
#13037=CARTESIAN_POINT('Ctrl Pts',(-35.9600788646211,-0.87693536270526,
309.713779306713));
#13038=CARTESIAN_POINT('Ctrl Pts',(-35.9469176782966,-0.909316207975562,
309.716227594138));
#13039=CARTESIAN_POINT('Ctrl Pts',(-35.9267201011362,-0.956021792803638,
309.719738387782));
#13040=CARTESIAN_POINT('Ctrl Pts',(-35.9202479323392,-0.970583692846614,
309.720830012436));
#13041=CARTESIAN_POINT('Ctrl Pts',(-35.9089485757408,-0.995331320502093,
309.722678749617));
#13042=CARTESIAN_POINT('Ctrl Pts',(-35.904194918026,-1.00554930731328,309.72344009382));
#13043=CARTESIAN_POINT('Ctrl Pts',(-35.8927618201674,-1.02967362877591,
309.725232923355));
#13044=CARTESIAN_POINT('Ctrl Pts',(-35.8860192958682,-1.04354922102529,
309.726260561577));
#13045=CARTESIAN_POINT('Ctrl Pts',(-35.8648396596177,-1.08607470020187,
309.729402105718));
#13046=CARTESIAN_POINT('Ctrl Pts',(-35.8499556748801,-1.11449946476577,
309.731490788564));
#13047=CARTESIAN_POINT('Ctrl Pts',(-35.7375741958693,-1.31891692569195,
309.746493594965));
#13048=CARTESIAN_POINT('Ctrl Pts',(-35.618601789144,-1.48218826075821,309.758438393318));
#13049=CARTESIAN_POINT('Ctrl Pts',(-35.4189706264659,-1.69356455869197,
309.77648994116));
#13050=CARTESIAN_POINT('Ctrl Pts',(-35.3538841758165,-1.75510093005289,
309.782130338333));
#13051=CARTESIAN_POINT('Ctrl Pts',(-35.261251713375,-1.83324919970288,309.789977731786));
#13052=CARTESIAN_POINT('Ctrl Pts',(-35.2366159366122,-1.85320138724587,
309.792048450123));
#13053=CARTESIAN_POINT('Ctrl Pts',(-35.1937405110199,-1.88652498316338,
309.795629794204));
#13054=CARTESIAN_POINT('Ctrl Pts',(-35.1756955497267,-1.90014057129233,
309.797130488479));
#13055=CARTESIAN_POINT('Ctrl Pts',(-35.1383784904002,-1.92746939987681,
309.800222268681));
#13056=CARTESIAN_POINT('Ctrl Pts',(-35.119090414151,-1.94115638997271,309.801814146026));
#13057=CARTESIAN_POINT('Ctrl Pts',(-35.0688787739199,-1.97566969418307,
309.805944240345));
#13058=CARTESIAN_POINT('Ctrl Pts',(-35.0376640581931,-1.99605872971316,
309.808498521476));
#13059=CARTESIAN_POINT('Ctrl Pts',(-34.8308610769926,-2.12428895000816,
309.825345307427));
#13060=CARTESIAN_POINT('Ctrl Pts',(-34.6423601482496,-2.20957364562771,
309.840463857755));
#13061=CARTESIAN_POINT('Ctrl Pts',(-34.3584009067633,-2.2958018602168,309.862065697617));
#13062=CARTESIAN_POINT('Ctrl Pts',(-34.2700802934869,-2.31717401524013,
309.86861459548));
#13063=CARTESIAN_POINT('Ctrl Pts',(-34.1596361441523,-2.33727164295446,
309.876441278761));
#13064=CARTESIAN_POINT('Ctrl Pts',(-34.1384765476125,-2.34082619314409,
309.877924424734));
#13065=CARTESIAN_POINT('Ctrl Pts',(-34.1041305850791,-2.3461177178856,309.880302347643));
#13066=CARTESIAN_POINT('Ctrl Pts',(-34.0909732178138,-2.34803170234124,
309.8812063107));
#13067=CARTESIAN_POINT('Ctrl Pts',(-34.0645141153359,-2.35165373469032,
309.883009217015));
#13068=CARTESIAN_POINT('Ctrl Pts',(-34.051212625637,-2.35335981013539,309.883908031345));
#13069=CARTESIAN_POINT('Ctrl Pts',(-34.0160567011594,-2.35756621374573,
309.886265424643));
#13070=CARTESIAN_POINT('Ctrl Pts',(-33.9941801606791,-2.35987556439513,
309.887713861324));
#13071=CARTESIAN_POINT('Ctrl Pts',(-33.8679243399572,-2.37142982273592,
309.89598317123));
#13072=CARTESIAN_POINT('Ctrl Pts',(-33.7630436674355,-2.374054647722,309.902501216431));
#13073=CARTESIAN_POINT('Ctrl Pts',(-33.527239143176,-2.36432241042568,309.917028335508));
#13074=CARTESIAN_POINT('Ctrl Pts',(-33.3968350491521,-2.34804567742497,
309.924982527676));
#13075=CARTESIAN_POINT('Ctrl Pts',(-33.1945207636331,-2.3055374268082,309.937903165899));
#13076=CARTESIAN_POINT('Ctrl Pts',(-33.1213851253045,-2.2864832071445,309.942694815755));
#13077=CARTESIAN_POINT('Ctrl Pts',(-33.0205524130896,-2.25500205691276,
309.949549776262));
#13078=CARTESIAN_POINT('Ctrl Pts',(-32.9919913588175,-2.2454845434132,309.951519841096));
#13079=CARTESIAN_POINT('Ctrl Pts',(-32.9425498621689,-2.227956467529,309.954984178094));
#13080=CARTESIAN_POINT('Ctrl Pts',(-32.9215868187212,-2.22018927273224,
309.956470237377));
#13081=CARTESIAN_POINT('Ctrl Pts',(-32.8781578490868,-2.20339607223984,
309.959586476187));
#13082=CARTESIAN_POINT('Ctrl Pts',(-32.85571416559,-2.19432010697264,309.961218198427));
#13083=CARTESIAN_POINT('Ctrl Pts',(-32.7964851949182,-2.16930693556733,
309.965583055382));
#13084=CARTESIAN_POINT('Ctrl Pts',(-32.7599597643281,-2.15277854667102,
309.968335928514));
#13085=CARTESIAN_POINT('Ctrl Pts',(-32.5838841110795,-2.06766074668186,
309.981915675507));
#13086=CARTESIAN_POINT('Ctrl Pts',(-32.4509112286364,-1.98639660849529,
309.993171890676));
#13087=CARTESIAN_POINT('Ctrl Pts',(-32.253541058487,-1.83735563336454,310.011235144592));
#13088=CARTESIAN_POINT('Ctrl Pts',(-32.1834932737139,-1.77776961265017,
310.017955747456));
#13089=CARTESIAN_POINT('Ctrl Pts',(-32.0804507354419,-1.67924830097529,
310.028173344617));
#13090=CARTESIAN_POINT('Ctrl Pts',(-32.0449531490419,-1.64306137473039,
310.031760900384));
#13091=CARTESIAN_POINT('Ctrl Pts',(-31.9982978420506,-1.59234635901782,
310.036538875745));
#13092=CARTESIAN_POINT('Ctrl Pts',(-31.9861106257484,-1.57878825748567,
310.037793120951));
#13093=CARTESIAN_POINT('Ctrl Pts',(-31.9657028575972,-1.55555152222233,
310.039901948594));
#13094=CARTESIAN_POINT('Ctrl Pts',(-31.9574016961712,-1.54594516736175,
310.040762180356));
#13095=CARTESIAN_POINT('Ctrl Pts',(-31.9397977724989,-1.52523958824999,
310.042591147213));
#13096=CARTESIAN_POINT('Ctrl Pts',(-31.9305189420888,-1.51412116755396,
310.043558238648));
#13097=CARTESIAN_POINT('Ctrl Pts',(-31.9046184925332,-1.48250151298038,
310.046268772998));
#13098=CARTESIAN_POINT('Ctrl Pts',(-31.8882358470808,-1.461806167278,310.047996394486));
#13099=CARTESIAN_POINT('Ctrl Pts',(-31.8134171943242,-1.36397939543674,
310.055971946254));
#13100=CARTESIAN_POINT('Ctrl Pts',(-31.7593855440788,-1.2835842972397,310.06198562576));
#13101=CARTESIAN_POINT('Ctrl Pts',(-31.6441839097512,-1.08721012277575,
310.075998394509));
#13102=CARTESIAN_POINT('Ctrl Pts',(-31.5874157525307,-0.969030480296554,
310.083934788113));
#13103=CARTESIAN_POINT('Ctrl Pts',(-31.5137490814012,-0.776293830706618,
310.096831249294));
#13104=CARTESIAN_POINT('Ctrl Pts',(-31.4901919021824,-0.704575967787306,
310.101617453138));
#13105=CARTESIAN_POINT('Ctrl Pts',(-31.4620768529805,-0.602857700253395,
310.108466000096));
#13106=CARTESIAN_POINT('Ctrl Pts',(-31.4546129942304,-0.573704304930778,
310.110435345184));
#13107=CARTESIAN_POINT('Ctrl Pts',(-31.4425749595652,-0.522661064059756,
310.113898856752));
#13108=CARTESIAN_POINT('Ctrl Pts',(-31.4377518384465,-0.500833488618011,
310.115384822435));
#13109=CARTESIAN_POINT('Ctrl Pts',(-31.4283485340707,-0.455227029343866,
310.118501295058));
#13110=CARTESIAN_POINT('Ctrl Pts',(-31.4238225814206,-0.431439749840212,
310.120133350641));
#13111=CARTESIAN_POINT('Ctrl Pts',(-31.4127687215022,-0.368074405734188,
310.124500173513));
#13112=CARTESIAN_POINT('Ctrl Pts',(-31.406879561581,-0.328394459872724,
310.127254711164));
#13113=CARTESIAN_POINT('Ctrl Pts',(-31.3831548633909,-0.134861487227556,
310.140793920795));
#13114=CARTESIAN_POINT('Ctrl Pts',(-31.3794155838814,0.0203158112070516,
310.152004045879));
#13115=CARTESIAN_POINT('Ctrl Pts',(-31.3976201757656,0.266758500495503,
310.170051719646));
#13116=CARTESIAN_POINT('Ctrl Pts',(-31.4097848335549,0.35832161174487,310.176802578874));
#13117=CARTESIAN_POINT('Ctrl Pts',(-31.4368709361756,0.498828620726649,
310.187059023653));
#13118=CARTESIAN_POINT('Ctrl Pts',(-31.4480879953059,0.548393537905482,
310.190655855371));
#13119=CARTESIAN_POINT('Ctrl Pts',(-31.4654861596984,0.615219763046917,
310.195443879524));
#13120=CARTESIAN_POINT('Ctrl Pts',(-31.4702866823658,0.632822969589049,
310.196699227583));
#13121=CARTESIAN_POINT('Ctrl Pts',(-31.4787719784252,0.662580777982345,
310.198809314407));
#13122=CARTESIAN_POINT('Ctrl Pts',(-31.4823520233285,0.67476408387007,310.199669719198));
#13123=CARTESIAN_POINT('Ctrl Pts',(-31.4902218096407,0.700771782705733,
310.201498367107));
#13124=CARTESIAN_POINT('Ctrl Pts',(-31.4945404827555,0.714586506803554,
310.202464976092));
#13125=CARTESIAN_POINT('Ctrl Pts',(-31.5070794391263,0.753443870667212,
310.205172723694));
#13126=CARTESIAN_POINT('Ctrl Pts',(-31.5155913363286,0.778391083264248,
310.206898092016));
#13127=CARTESIAN_POINT('Ctrl Pts',(-31.5810619047284,0.960296086317004,
310.219418400276));
#13128=CARTESIAN_POINT('Ctrl Pts',(-31.6540451703501,1.11101001867177,310.229484184463));
#13129=CARTESIAN_POINT('Ctrl Pts',(-31.8040129845266,1.35207740946097,310.246923069845));
#13130=CARTESIAN_POINT('Ctrl Pts',(-31.873007030978,1.44662277081856,310.254168720521));
#13131=CARTESIAN_POINT('Ctrl Pts',(-31.9739480148236,1.56542595776726,310.26417726903));
#13132=CARTESIAN_POINT('Ctrl Pts',(-31.9999404314216,1.59453090930713,310.266708295609));
#13133=CARTESIAN_POINT('Ctrl Pts',(-32.0430578587427,1.64047794353478,310.270844056999));
#13134=CARTESIAN_POINT('Ctrl Pts',(-32.0597420477038,1.65772488347278,310.272430019407));
#13135=CARTESIAN_POINT('Ctrl Pts',(-32.0925273976463,1.69060277795411,310.275521214851));
#13136=CARTESIAN_POINT('Ctrl Pts',(-32.108594411927,1.70626425323569,310.277024843648));
#13137=CARTESIAN_POINT('Ctrl Pts',(-32.1471329331801,1.74277816592017,310.280606732503));
#13138=CARTESIAN_POINT('Ctrl Pts',(-32.1697908189261,1.76342706415366,310.282693405203));
#13139=CARTESIAN_POINT('Ctrl Pts',(-32.2486176057592,1.83251580399968,310.289892003041));
#13140=CARTESIAN_POINT('Ctrl Pts',(-32.3066502320305,1.87875326611189,310.295090775305));
#13141=CARTESIAN_POINT('Ctrl Pts',(-32.3897864074735,1.93884487102298,310.302401196712));
#13142=CARTESIAN_POINT('Ctrl Pts',(-32.4131214640902,1.95508109611666,310.304438789964));
#13143=CARTESIAN_POINT('Ctrl Pts',(-32.5118214152301,2.02115428894747,310.31299357935));
#13144=CARTESIAN_POINT('Ctrl Pts',(-32.5896863653336,2.06706702007088,310.319594316565));
#13145=CARTESIAN_POINT('Ctrl Pts',(-32.6699491957805,2.10841546789345,310.326187962698));
#13146=CARTESIAN_POINT('Origin',(-33.7561270252576,0.,302.151410108095));
#13147=CARTESIAN_POINT('',(-32.6714234043919,2.10551637491534,311.522951534327));
#13148=CARTESIAN_POINT('',(-32.6699490813724,2.10841540895464,311.327581625012));
#13149=CARTESIAN_POINT('',(-32.6699490794746,2.10841540797695,302.151410108095));
#13150=CARTESIAN_POINT('',(-36.1295666873539,0.00193988692732453,310.848590956866));
#13151=CARTESIAN_POINT('Ctrl Pts',(-36.1295666873539,0.00193988692732453,
310.848590956866));
#13152=CARTESIAN_POINT('Ctrl Pts',(-36.123741267486,-0.652989171154178,
310.892622454172));
#13153=CARTESIAN_POINT('Ctrl Pts',(-35.5020848627001,-2.10550375003854,
310.989624382201));
#13154=CARTESIAN_POINT('Ctrl Pts',(-33.0415486194394,-2.71176251122329,
311.139596740952));
#13155=CARTESIAN_POINT('Ctrl Pts',(-31.0894948106476,-0.867957931798494,
311.298508033121));
#13156=CARTESIAN_POINT('Ctrl Pts',(-31.485743561134,1.2545895519984,311.426292964246));
#13157=CARTESIAN_POINT('Ctrl Pts',(-32.3803640906792,1.95726749312548,311.501107464648));
#13158=CARTESIAN_POINT('Ctrl Pts',(-32.671423404392,2.10551637491536,311.522951534327));
#13159=CARTESIAN_POINT('Ctrl Pts',(-36.1278762772803,0.00188362146629249,
310.847619667516));
#13160=CARTESIAN_POINT('Ctrl Pts',(-36.1277997378554,0.0982577215860634,
310.840595642696));
#13161=CARTESIAN_POINT('Ctrl Pts',(-36.1218491037786,0.194549688000836,
310.833625037494));
#13162=CARTESIAN_POINT('Ctrl Pts',(-36.1080209960884,0.306706121591654,
310.825735930453));
#13163=CARTESIAN_POINT('Ctrl Pts',(-36.1058155576088,0.323168273179709,
310.824583945188));
#13164=CARTESIAN_POINT('Ctrl Pts',(-36.1016682989013,0.351833521843165,
310.822589966578));
#13165=CARTESIAN_POINT('Ctrl Pts',(-36.0998037388827,0.364046936929179,
310.821744189674));
#13166=CARTESIAN_POINT('Ctrl Pts',(-36.0960462957189,0.387432907720725,
310.820132716905));
#13167=CARTESIAN_POINT('Ctrl Pts',(-36.094168651592,0.398607355240138,310.819366282987));
#13168=CARTESIAN_POINT('Ctrl Pts',(-36.0896392315116,0.424429498608024,
310.817603671748));
#13169=CARTESIAN_POINT('Ctrl Pts',(-36.0869295557214,0.439066292826559,
310.816610727732));
#13170=CARTESIAN_POINT('Ctrl Pts',(-36.078497069862,0.482335942655559,310.813691011211));
#13171=CARTESIAN_POINT('Ctrl Pts',(-36.0723829181109,0.510890802250861,
310.811784569628));
#13172=CARTESIAN_POINT('Ctrl Pts',(-36.0345657394104,0.672839206118621,
310.801050717806));
#13173=CARTESIAN_POINT('Ctrl Pts',(-35.9918668587651,0.803412498934501,
310.792691078824));
#13174=CARTESIAN_POINT('Ctrl Pts',(-35.8971067513509,1.02584260222284,310.777875130296));
#13175=CARTESIAN_POINT('Ctrl Pts',(-35.8497712513038,1.11928509156068,310.771455128697));
#13176=CARTESIAN_POINT('Ctrl Pts',(-35.7943400030282,1.21280774330486,310.764606838929));
#13177=CARTESIAN_POINT('Ctrl Pts',(-35.792247143385,1.21631806254776,310.764349157966));
#13178=CARTESIAN_POINT('Ctrl Pts',(-35.7827524367733,1.23215020131538,310.763184059302));
#13179=CARTESIAN_POINT('Ctrl Pts',(-35.7752478381601,1.24440982341308,310.76227387106));
#13180=CARTESIAN_POINT('Ctrl Pts',(-35.7506094756113,1.28384972943842,310.75931843913));
#13181=CARTESIAN_POINT('Ctrl Pts',(-35.7330352625072,1.31074942298467,310.757260247393));
#13182=CARTESIAN_POINT('Ctrl Pts',(-35.6963836132923,1.36443515809161,310.75305762165));
#13183=CARTESIAN_POINT('Ctrl Pts',(-35.6772848134762,1.39119786771531,310.750912764556));
#13184=CARTESIAN_POINT('Ctrl Pts',(-35.6440031310601,1.43584198213507,310.747243621427));
#13185=CARTESIAN_POINT('Ctrl Pts',(-35.6301068964989,1.45393183092294,310.74573057365));
#13186=CARTESIAN_POINT('Ctrl Pts',(-35.6014690727268,1.49011928878912,310.74264831544));
#13187=CARTESIAN_POINT('Ctrl Pts',(-35.5867169562676,1.50820529229695,310.741078788821));
#13188=CARTESIAN_POINT('Ctrl Pts',(-35.5487380710858,1.55338897513909,310.73708163383));
#13189=CARTESIAN_POINT('Ctrl Pts',(-35.5251628388251,1.58018471022434,310.734639906718));
#13190=CARTESIAN_POINT('Ctrl Pts',(-35.369041358055,1.74975939878078,310.71870987128));
#13191=CARTESIAN_POINT('Ctrl Pts',(-35.2199549257829,1.87625430744034,310.70448638847));
#13192=CARTESIAN_POINT('Ctrl Pts',(-34.9766504722834,2.03587437760495,310.683257777607));
#13193=CARTESIAN_POINT('Ctrl Pts',(-34.8930273885534,2.08372811627144,310.676276576912));
#13194=CARTESIAN_POINT('Ctrl Pts',(-34.7830563528748,2.1380624209283,310.667666419169));
#13195=CARTESIAN_POINT('Ctrl Pts',(-34.7591973574047,2.14935916338813,310.665831277558));
#13196=CARTESIAN_POINT('Ctrl Pts',(-34.7221026816098,2.16617044613488,310.663033868942));
#13197=CARTESIAN_POINT('Ctrl Pts',(-34.7089980623794,2.17196689289468,310.662056186275));
#13198=CARTESIAN_POINT('Ctrl Pts',(-34.6841369345618,2.18269516261417,310.660222393903));
#13199=CARTESIAN_POINT('Ctrl Pts',(-34.6723925373103,2.18765127092185,310.65936499887));
#13200=CARTESIAN_POINT('Ctrl Pts',(-34.6461917601799,2.19845992163519,310.657470947976));
#13201=CARTESIAN_POINT('Ctrl Pts',(-34.6317167273268,2.20426494899861,310.656437057341));
#13202=CARTESIAN_POINT('Ctrl Pts',(-34.5802524042987,2.22431708960753,310.652801694868));
#13203=CARTESIAN_POINT('Ctrl Pts',(-34.5429623386241,2.23778009846736,310.650241165652));
#13204=CARTESIAN_POINT('Ctrl Pts',(-34.3716287900983,2.29482442428157,310.63873319389));
#13205=CARTESIAN_POINT('Ctrl Pts',(-34.2341935962218,2.32734205370379,310.630194931516));
#13206=CARTESIAN_POINT('Ctrl Pts',(-34.0081380273211,2.35994337252435,310.616175615873));
#13207=CARTESIAN_POINT('Ctrl Pts',(-33.9209827474776,2.36762821606296,310.610779000097));
#13208=CARTESIAN_POINT('Ctrl Pts',(-33.7738841194592,2.3724361644907,310.601492310927));
#13209=CARTESIAN_POINT('Ctrl Pts',(-33.7141133020573,2.37213039410012,310.59767020961));
#13210=CARTESIAN_POINT('Ctrl Pts',(-33.6266274857506,2.36837536131658,310.591967537359));
#13211=CARTESIAN_POINT('Ctrl Pts',(-33.5988578156673,2.36669353114775,310.59014149255));
#13212=CARTESIAN_POINT('Ctrl Pts',(-33.5492963636181,2.36281580961202,310.586850762041));
#13213=CARTESIAN_POINT('Ctrl Pts',(-33.5274929867878,2.36080577219749,310.585392078989));
#13214=CARTESIAN_POINT('Ctrl Pts',(-33.480504217366,2.35581688450475,310.58222318753));
#13215=CARTESIAN_POINT('Ctrl Pts',(-33.4553327154184,2.35273539131512,310.580509905376));
#13216=CARTESIAN_POINT('Ctrl Pts',(-33.385985087246,2.34311482008521,310.575744184977));
#13217=CARTESIAN_POINT('Ctrl Pts',(-33.3419387945491,2.33573109690969,310.572665693933));
#13218=CARTESIAN_POINT('Ctrl Pts',(-33.1206453953002,2.29217842944934,310.5569292862));
#13219=CARTESIAN_POINT('Ctrl Pts',(-32.9477635913037,2.23706217026844,310.543689705198));
#13220=CARTESIAN_POINT('Ctrl Pts',(-32.7447408112159,2.14570340258205,310.527456132776));
#13221=CARTESIAN_POINT('Ctrl Pts',(-32.7070915797467,2.12754985697098,310.524417945537));
#13222=CARTESIAN_POINT('Ctrl Pts',(-32.6699490276577,2.10841538128279,310.521403445152));
#13223=CARTESIAN_POINT('Ctrl Pts',(-32.6699491957805,2.10841546789345,310.326187962698));
#13224=CARTESIAN_POINT('Ctrl Pts',(-32.7011651547407,2.12449677779882,310.328752374967));
#13225=CARTESIAN_POINT('Ctrl Pts',(-32.7327438450632,2.13988772362731,310.331315189771));
#13226=CARTESIAN_POINT('Ctrl Pts',(-32.8407968834382,2.18961015778526,310.339959090314));
#13227=CARTESIAN_POINT('Ctrl Pts',(-32.9187427467795,2.2205882806106,310.345987861254));
#13228=CARTESIAN_POINT('Ctrl Pts',(-33.0181583841927,2.25411739408484,310.353298628881));
#13229=CARTESIAN_POINT('Ctrl Pts',(-33.0382343955691,2.26059133674271,310.354756052346));
#13230=CARTESIAN_POINT('Ctrl Pts',(-33.0710297139317,2.27068590917734,310.357103245601));
#13231=CARTESIAN_POINT('Ctrl Pts',(-33.0836972328514,2.27446939410077,310.358001793112));
#13232=CARTESIAN_POINT('Ctrl Pts',(-33.109357742748,2.28190044662387,310.359804769643));
#13233=CARTESIAN_POINT('Ctrl Pts',(-33.1223514830096,2.28554342286929,310.360708933401));
#13234=CARTESIAN_POINT('Ctrl Pts',(-33.1569891127496,2.2949364484048,310.363097553758));
#13235=CARTESIAN_POINT('Ctrl Pts',(-33.1786851174518,2.30049135490378,310.364571379883));
#13236=CARTESIAN_POINT('Ctrl Pts',(-33.3209219379867,2.33476959987433,310.3741079119));
#13237=CARTESIAN_POINT('Ctrl Pts',(-33.4434925666836,2.35431946690266,310.381744712001));
#13238=CARTESIAN_POINT('Ctrl Pts',(-33.6838307343132,2.37354121205113,310.396535475821));
#13239=CARTESIAN_POINT('Ctrl Pts',(-33.8011445154506,2.37421491980774,310.403674663504));
#13240=CARTESIAN_POINT('Ctrl Pts',(-33.989033200692,2.36135946997745,310.415473373532));
#13241=CARTESIAN_POINT('Ctrl Pts',(-34.0597808871005,2.35330761298922,310.419997967251));
#13242=CARTESIAN_POINT('Ctrl Pts',(-34.1592111274655,2.33743299786717,310.426537674418));
#13243=CARTESIAN_POINT('Ctrl Pts',(-34.1882766951603,2.3322341965814,310.428471281707));
#13244=CARTESIAN_POINT('Ctrl Pts',(-34.239087638206,2.3221635025539,310.431894057213));
#13245=CARTESIAN_POINT('Ctrl Pts',(-34.2608759030105,2.31752514523289,310.43337562169));
#13246=CARTESIAN_POINT('Ctrl Pts',(-34.3064457169066,2.30715100055669,310.436504987604));
#13247=CARTESIAN_POINT('Ctrl Pts',(-34.3302102099487,2.30135282402204,310.43815464441));
#13248=CARTESIAN_POINT('Ctrl Pts',(-34.3938992285348,2.28476581835318,310.442625478366));
#13249=CARTESIAN_POINT('Ctrl Pts',(-34.4336366568528,2.27329904631556,310.445468144841));
#13250=CARTESIAN_POINT('Ctrl Pts',(-34.6644297296454,2.20011198467773,310.462301201178));
#13251=CARTESIAN_POINT('Ctrl Pts',(-34.8473012037357,2.11537641930732,310.477049787446));
#13252=CARTESIAN_POINT('Ctrl Pts',(-35.0681994526253,1.97668396422446,310.496026389641));
#13253=CARTESIAN_POINT('Ctrl Pts',(-35.1178919759337,1.94278424111017,310.500373170706));
#13254=CARTESIAN_POINT('Ctrl Pts',(-35.1975278676907,1.88389898116342,310.50741264381));
#13255=CARTESIAN_POINT('Ctrl Pts',(-35.2282391506601,1.85999947978935,310.510146403672));
#13256=CARTESIAN_POINT('Ctrl Pts',(-35.2711866912039,1.82484723277534,310.513981370183));
#13257=CARTESIAN_POINT('Ctrl Pts',(-35.2839128079579,1.81420612297897,310.515119286153));
#13258=CARTESIAN_POINT('Ctrl Pts',(-35.3051380561325,1.79607659807025,310.517018281238));
#13259=CARTESIAN_POINT('Ctrl Pts',(-35.3136967150599,1.78865955423097,310.517784268625));
#13260=CARTESIAN_POINT('Ctrl Pts',(-35.3334030914736,1.77133303173797,310.519548362446));
#13261=CARTESIAN_POINT('Ctrl Pts',(-35.3445109323848,1.76137931508517,310.520543200644));
#13262=CARTESIAN_POINT('Ctrl Pts',(-35.3772002035143,1.73152577397186,310.523474981431));
#13263=CARTESIAN_POINT('Ctrl Pts',(-35.3985077335048,1.71132859336754,310.525391338802));
#13264=CARTESIAN_POINT('Ctrl Pts',(-35.5655155115799,1.54703039420045,310.540509236142));
#13265=CARTESIAN_POINT('Ctrl Pts',(-35.6923717339977,1.38497942603709,310.552662713756));
#13266=CARTESIAN_POINT('Ctrl Pts',(-35.8426623924278,1.13122049304195,310.570970407338));
#13267=CARTESIAN_POINT('Ctrl Pts',(-35.8840569167221,1.05128560280513,310.576637715341));
#13268=CARTESIAN_POINT('Ctrl Pts',(-35.9337821107498,0.940225575741763,
310.584516362532));
#13269=CARTESIAN_POINT('Ctrl Pts',(-35.9461709236824,0.910995812467881,
310.586589911926));
#13270=CARTESIAN_POINT('Ctrl Pts',(-35.9663734723491,0.860534735303168,
310.590174585424));
#13271=CARTESIAN_POINT('Ctrl Pts',(-35.9744771348981,0.839423682258381,
310.591675728817));
#13272=CARTESIAN_POINT('Ctrl Pts',(-35.989457869753,0.79866427695291,310.594578335277));
#13273=CARTESIAN_POINT('Ctrl Pts',(-35.9963805706928,0.779034846686049,
310.59597810656));
#13274=CARTESIAN_POINT('Ctrl Pts',(-36.014110658502,0.726569259143648,310.5997257169));
#13275=CARTESIAN_POINT('Ctrl Pts',(-36.0244596740544,0.693584710690194,
310.602088360564));
#13276=CARTESIAN_POINT('Ctrl Pts',(-36.0695957214243,0.537891271594074,
310.613277026865));
#13277=CARTESIAN_POINT('Ctrl Pts',(-36.095163840843,0.412749445140688,310.622391794552));
#13278=CARTESIAN_POINT('Ctrl Pts',(-36.1221584435765,0.190660779698225,
310.638652919245));
#13279=CARTESIAN_POINT('Ctrl Pts',(-36.127945006094,0.0945276924360876,
310.645714167013));
#13280=CARTESIAN_POINT('Ctrl Pts',(-36.127820176964,-0.0806002356389265,
310.658426354757));
#13281=CARTESIAN_POINT('Ctrl Pts',(-36.1238258690541,-0.159466075687365,
310.664093559647));
#13282=CARTESIAN_POINT('Ctrl Pts',(-36.113775825447,-0.259115622435795,
310.671073991351));
#13283=CARTESIAN_POINT('Ctrl Pts',(-36.1113619065198,-0.280209750604536,
310.672541201763));
#13284=CARTESIAN_POINT('Ctrl Pts',(-36.1071481372164,-0.313114014761444,
310.674810657776));
#13285=CARTESIAN_POINT('Ctrl Pts',(-36.1055418423012,-0.324947208666862,
310.67562291337));
#13286=CARTESIAN_POINT('Ctrl Pts',(-36.1019855680653,-0.349739145417503,
310.677315793509));
#13287=CARTESIAN_POINT('Ctrl Pts',(-36.1000174415893,-0.362694777831795,
310.678195274048));
#13288=CARTESIAN_POINT('Ctrl Pts',(-36.0946919369852,-0.39589559677855,
310.680437293506));
#13289=CARTESIAN_POINT('Ctrl Pts',(-36.0911789053681,-0.416115318425081,
310.681791446722));
#13290=CARTESIAN_POINT('Ctrl Pts',(-36.073634358068,-0.50986352787359,310.68802824569));
#13291=CARTESIAN_POINT('Ctrl Pts',(-36.0563881264073,-0.582753977717598,
310.692758356123));
#13292=CARTESIAN_POINT('Ctrl Pts',(-35.9842428490252,-0.833950872259935,
310.709020862149));
#13293=CARTESIAN_POINT('Ctrl Pts',(-35.9118074477784,-1.00648822683653,
310.720174099892));
#13294=CARTESIAN_POINT('Ctrl Pts',(-35.7905839553706,-1.2205425411179,310.735698819306));
#13295=CARTESIAN_POINT('Ctrl Pts',(-35.7593238002128,-1.2711966317769,310.739505601598));
#13296=CARTESIAN_POINT('Ctrl Pts',(-35.7107269612745,-1.34369221357061,
310.745189809146));
#13297=CARTESIAN_POINT('Ctrl Pts',(-35.6948562992226,-1.36649126204861,
310.747013234048));
#13298=CARTESIAN_POINT('Ctrl Pts',(-35.6656508373592,-1.40691327633599,
310.750314432869));
#13299=CARTESIAN_POINT('Ctrl Pts',(-35.6524630644113,-1.424638805468,310.75178641817));
#13300=CARTESIAN_POINT('Ctrl Pts',(-35.6235481638065,-1.46239003212115,
310.754975912167));
#13301=CARTESIAN_POINT('Ctrl Pts',(-35.6077424310716,-1.48235171786822,
310.756696422019));
#13302=CARTESIAN_POINT('Ctrl Pts',(-35.5621913481358,-1.53801457702003,
310.761593465543));
#13303=CARTESIAN_POINT('Ctrl Pts',(-35.5317152852311,-1.57309980086646,
310.764799148994));
#13304=CARTESIAN_POINT('Ctrl Pts',(-35.4349289253846,-1.67812627068785,
310.774775494571));
#13305=CARTESIAN_POINT('Ctrl Pts',(-35.3653770303368,-1.74493389484704,
310.781672246029));
#13306=CARTESIAN_POINT('Ctrl Pts',(-35.1615873884098,-1.91811143424261,
310.801072519459));
#13307=CARTESIAN_POINT('Ctrl Pts',(-35.019606062074,-2.01447126675836,310.813749277259));
#13308=CARTESIAN_POINT('Ctrl Pts',(-34.8433151022023,-2.10808743869885,
310.827795331842));
#13309=CARTESIAN_POINT('Ctrl Pts',(-34.817899766245,-2.12100197762021,310.829781260168));
#13310=CARTESIAN_POINT('Ctrl Pts',(-34.7789892724057,-2.13989916102562,
310.832756291068));
#13311=CARTESIAN_POINT('Ctrl Pts',(-34.7656618557438,-2.14621877987346,
310.833763845253));
#13312=CARTESIAN_POINT('Ctrl Pts',(-34.7408176422288,-2.15771681752271,
310.8356197602));
#13313=CARTESIAN_POINT('Ctrl Pts',(-34.7293177098188,-2.16292796360799,
310.836469921439));
#13314=CARTESIAN_POINT('Ctrl Pts',(-34.7015809405718,-2.17523075422512,
310.838499911205));
#13315=CARTESIAN_POINT('Ctrl Pts',(-34.6853053822581,-2.18223270263717,
310.839674446356));
#13316=CARTESIAN_POINT('Ctrl Pts',(-34.625880913126,-2.20701245170155,310.843908111494));
#13317=CARTESIAN_POINT('Ctrl Pts',(-34.5822854946532,-2.22369931324647,
310.846910102509));
#13318=CARTESIAN_POINT('Ctrl Pts',(-34.4627731646253,-2.26544399276511,
310.854934171966));
#13319=CARTESIAN_POINT('Ctrl Pts',(-34.3860345883638,-2.28796926376351,
310.85986757118));
#13320=CARTESIAN_POINT('Ctrl Pts',(-34.1370252069085,-2.34757984237678,
310.875589682449));
#13321=CARTESIAN_POINT('Ctrl Pts',(-33.9617335596669,-2.36937418315864,
310.886273625737));
#13322=CARTESIAN_POINT('Ctrl Pts',(-33.7473612677611,-2.37204290143076,
310.900047971212));
#13323=CARTESIAN_POINT('Ctrl Pts',(-33.7090678545138,-2.3715921934932,310.902533460109));
#13324=CARTESIAN_POINT('Ctrl Pts',(-33.646968098546,-2.3693567203049,310.90661374708));
#13325=CARTESIAN_POINT('Ctrl Pts',(-33.6231474633208,-2.36813920737541,
310.908190729571));
#13326=CARTESIAN_POINT('Ctrl Pts',(-33.5768980168004,-2.36507533214119,
310.911277567799));
#13327=CARTESIAN_POINT('Ctrl Pts',(-33.5544690833012,-2.36326857934525,
310.91278601397));
#13328=CARTESIAN_POINT('Ctrl Pts',(-33.501143218091,-2.35820830147416,310.916401293583));
#13329=CARTESIAN_POINT('Ctrl Pts',(-33.4702785328113,-2.35466634883782,
310.918516978761));
#13330=CARTESIAN_POINT('Ctrl Pts',(-33.3566789596785,-2.3393635915529,310.926393573988));
#13331=CARTESIAN_POINT('Ctrl Pts',(-33.2745212113791,-2.32384030791728,
310.93226922914));
#13332=CARTESIAN_POINT('Ctrl Pts',(-33.0339827305574,-2.26508779780068,
310.949988907547));
#13333=CARTESIAN_POINT('Ctrl Pts',(-32.8790771650479,-2.209726640577,310.962113087648));
#13334=CARTESIAN_POINT('Ctrl Pts',(-32.6723886202642,-2.11067621743435,
310.978668577832));
#13335=CARTESIAN_POINT('Ctrl Pts',(-32.6148131747072,-2.08010751403149,
310.983319138181));
#13336=CARTESIAN_POINT('Ctrl Pts',(-32.5411323121964,-2.03700608768373,
310.989258587811));
#13337=CARTESIAN_POINT('Ctrl Pts',(-32.5238298355319,-2.02658571479267,
310.990652386875));
#13338=CARTESIAN_POINT('Ctrl Pts',(-32.4966730155643,-2.00975415550389,
310.992835940888));
#13339=CARTESIAN_POINT('Ctrl Pts',(-32.4867300418211,-2.00348882745538,
310.993634532443));
#13340=CARTESIAN_POINT('Ctrl Pts',(-32.4656085456678,-1.9899592519621,310.995328383309));
#13341=CARTESIAN_POINT('Ctrl Pts',(-32.4544438005594,-1.98267409685331,
310.996222184687));
#13342=CARTESIAN_POINT('Ctrl Pts',(-32.4253323756866,-1.96332656665103,
310.998550269952));
#13343=CARTESIAN_POINT('Ctrl Pts',(-32.40748772637,-1.95111192151577,310.999974863183));
#13344=CARTESIAN_POINT('Ctrl Pts',(-32.3125122588902,-1.88417558564402,
311.007558220214));
#13345=CARTESIAN_POINT('Ctrl Pts',(-32.2385309434519,-1.82511573794859,
311.013471186566));
#13346=CARTESIAN_POINT('Ctrl Pts',(-32.0203684351065,-1.6284909033104,311.031601301038));
#13347=CARTESIAN_POINT('Ctrl Pts',(-31.8898539949585,-1.47711259938662,
311.043560579194));
#13348=CARTESIAN_POINT('Ctrl Pts',(-31.7583907698772,-1.2789626928131,311.058832140836));
#13349=CARTESIAN_POINT('Ctrl Pts',(-31.7377894573017,-1.24619777822806,
311.061343190847));
#13350=CARTESIAN_POINT('Ctrl Pts',(-31.7057605646045,-1.19237921389586,
311.06545460981));
#13351=CARTESIAN_POINT('Ctrl Pts',(-31.6938336881706,-1.17163003286189,
311.067036628468));
#13352=CARTESIAN_POINT('Ctrl Pts',(-31.6713242652929,-1.13106151461868,
311.070125841539));
#13353=CARTESIAN_POINT('Ctrl Pts',(-31.660705300896,-1.11126524047784,311.071631516382));
#13354=CARTESIAN_POINT('Ctrl Pts',(-31.6361833143755,-1.06394889052385,
311.075227703906));
#13355=CARTESIAN_POINT('Ctrl Pts',(-31.6225328856648,-1.03630327122741,
311.077326817044));
#13356=CARTESIAN_POINT('Ctrl Pts',(-31.5747733609412,-0.934631931756852,
311.085043173236));
#13357=CARTESIAN_POINT('Ctrl Pts',(-31.5439502570335,-0.85913442564733,
311.090768986721));
#13358=CARTESIAN_POINT('Ctrl Pts',(-31.4661520933852,-0.636439012895046,
311.10763293523));
#13359=CARTESIAN_POINT('Ctrl Pts',(-31.4295872613367,-0.486051380277261,
311.119014638653));
#13360=CARTESIAN_POINT('Ctrl Pts',(-31.3972455062377,-0.258120009955602,
311.135709129886));
#13361=CARTESIAN_POINT('Ctrl Pts',(-31.390198264663,-0.182568591936165,
311.141147620841));
#13362=CARTESIAN_POINT('Ctrl Pts',(-31.3858381534039,-0.0858425750154427,
311.147893260664));
#13363=CARTESIAN_POINT('Ctrl Pts',(-31.3851714666234,-0.0648698664965462,
311.149342818771));
#13364=CARTESIAN_POINT('Ctrl Pts',(-31.3845630456225,-0.0319974685479178,
311.151591564983));
#13365=CARTESIAN_POINT('Ctrl Pts',(-31.3844323916645,-0.0201029392975533,
311.152400476924));
#13366=CARTESIAN_POINT('Ctrl Pts',(-31.3843457119273,0.00494473858801117,
311.154093142395));
#13367=CARTESIAN_POINT('Ctrl Pts',(-31.3844096002821,0.0180974924238778,
311.154975679065));
#13368=CARTESIAN_POINT('Ctrl Pts',(-31.3848564556179,0.0520098164421929,
311.157236475168));
#13369=CARTESIAN_POINT('Ctrl Pts',(-31.3854026180852,0.0727667103384232,
311.158606067397));
#13370=CARTESIAN_POINT('Ctrl Pts',(-31.3893124398446,0.171851837503754,
311.165087652848));
#13371=CARTESIAN_POINT('Ctrl Pts',(-31.3962861721802,0.249996089538851,
311.170031963315));
#13372=CARTESIAN_POINT('Ctrl Pts',(-31.4205701688313,0.424089741716131,
311.180951287466));
#13373=CARTESIAN_POINT('Ctrl Pts',(-31.4399467155586,0.51960348412311,311.18687805144));
#13374=CARTESIAN_POINT('Ctrl Pts',(-31.4982013077625,0.737087040896473,
311.200703774959));
#13375=CARTESIAN_POINT('Ctrl Pts',(-31.5411791309906,0.857628214759107,
311.208625300651));
#13376=CARTESIAN_POINT('Ctrl Pts',(-31.6078586044818,1.0056527199718,311.219099460598));
#13377=CARTESIAN_POINT('Ctrl Pts',(-31.6227532956709,1.03687556162286,311.221352276305));
#13378=CARTESIAN_POINT('Ctrl Pts',(-31.6476971418992,1.08634933751992,311.22499864719));
#13379=CARTESIAN_POINT('Ctrl Pts',(-31.6573135209117,1.10481368720382,311.226377041321));
#13380=CARTESIAN_POINT('Ctrl Pts',(-31.6778781454419,1.14306204359842,311.229270511901));
#13381=CARTESIAN_POINT('Ctrl Pts',(-31.6888686917713,1.16282077861736,311.230786988676));
#13382=CARTESIAN_POINT('Ctrl Pts',(-31.7159563908558,1.20992081289204,311.234456117076));
#13383=CARTESIAN_POINT('Ctrl Pts',(-31.7323225958819,1.23710147205929,311.236618333008));
#13384=CARTESIAN_POINT('Ctrl Pts',(-31.7970653899712,1.33990046159224,311.244973876571));
#13385=CARTESIAN_POINT('Ctrl Pts',(-31.8491700621936,1.41307020866272,311.251301573704));
#13386=CARTESIAN_POINT('Ctrl Pts',(-32.0324343847769,1.64177456238361,311.272335707828));
#13387=CARTESIAN_POINT('Ctrl Pts',(-32.1794436600721,1.78342479607702,311.28750245237));
#13388=CARTESIAN_POINT('Ctrl Pts',(-32.3672230682471,1.92277810416287,311.303993761918));
#13389=CARTESIAN_POINT('Ctrl Pts',(-32.3920859383549,1.94049528944322,311.306124413192));
#13390=CARTESIAN_POINT('Ctrl Pts',(-32.4297803163327,1.96627353454686,311.309268611703));
#13391=CARTESIAN_POINT('Ctrl Pts',(-32.4423572675321,1.9746990301849,311.310303730107));
#13392=CARTESIAN_POINT('Ctrl Pts',(-32.4655134866528,1.98989257028258,311.312182920752));
#13393=CARTESIAN_POINT('Ctrl Pts',(-32.4760666611977,1.99669757921589,311.313029251201));
#13394=CARTESIAN_POINT('Ctrl Pts',(-32.5011110436123,2.01256678264139,311.315014619128));
#13395=CARTESIAN_POINT('Ctrl Pts',(-32.5156469133437,2.02155863227588,311.316149041684));
#13396=CARTESIAN_POINT('Ctrl Pts',(-32.5664109883932,2.05220739436852,311.320053804251));
#13397=CARTESIAN_POINT('Ctrl Pts',(-32.6031212099061,2.07305512132193,311.322778031315));
#13398=CARTESIAN_POINT('Ctrl Pts',(-32.6501942717952,2.09815031230247,311.326172696658));
#13399=CARTESIAN_POINT('Ctrl Pts',(-32.6600539326407,2.10331779286902,311.326878375156));
#13400=CARTESIAN_POINT('Ctrl Pts',(-32.6699490813724,2.10841540895464,311.327581625012));
#13401=CARTESIAN_POINT('Origin',(-33.7561270252576,0.,302.151410108095));
#13402=CARTESIAN_POINT('',(-32.6699490794746,2.10841540797695,312.522795280203));
#13403=CARTESIAN_POINT('',(-32.6699490794746,2.10841540797695,312.325750055738));
#13404=CARTESIAN_POINT('',(-32.6699490794746,2.10841540797695,302.151410108095));
#13405=CARTESIAN_POINT('',(-36.1275260743337,0.000498864453422136,311.848589849175));
#13406=CARTESIAN_POINT('Ctrl Pts',(-36.1278769729119,0.000498298962362804,
311.848589891905));
#13407=CARTESIAN_POINT('Ctrl Pts',(-36.127894235934,-0.081668381915641,
311.854074130266));
#13408=CARTESIAN_POINT('Ctrl Pts',(-36.1236373039452,-0.163782429335775,
311.859558368627));
#13409=CARTESIAN_POINT('Ctrl Pts',(-36.1151485915037,-0.245388085459784,
311.865042606987));
#13410=CARTESIAN_POINT('Ctrl Pts',(-36.1062342578652,-0.331085421834301,
311.870801823222));
#13411=CARTESIAN_POINT('Ctrl Pts',(-36.0926527766679,-0.416221524668992,
311.876561039456));
#13412=CARTESIAN_POINT('Ctrl Pts',(-36.0745139142165,-0.500280217081753,
311.88232025569));
#13413=CARTESIAN_POINT('Ctrl Pts',(-36.0571874318221,-0.580574196822511,
311.88782153555));
#13414=CARTESIAN_POINT('Ctrl Pts',(-36.0357032078721,-0.659884812496487,
311.89332281541));
#13415=CARTESIAN_POINT('Ctrl Pts',(-36.0102078988994,-0.737778745683441,
311.898824095271));
#13416=CARTESIAN_POINT('Ctrl Pts',(-35.9846821853252,-0.815765571801945,
311.904331935719));
#13417=CARTESIAN_POINT('Ctrl Pts',(-35.9551360074727,-0.892331954147945,
311.909839776167));
#13418=CARTESIAN_POINT('Ctrl Pts',(-35.9217638730913,-0.967065202457874,
311.915347616615));
#13419=CARTESIAN_POINT('Ctrl Pts',(-35.8883222260357,-1.04195411680592,
311.920866929651));
#13420=CARTESIAN_POINT('Ctrl Pts',(-35.8510389023304,-1.11500189615293,
311.926386242686));
#13421=CARTESIAN_POINT('Ctrl Pts',(-35.8101539097133,-1.18582107437559,
311.931905555721));
#13422=CARTESIAN_POINT('Ctrl Pts',(-35.8046040044569,-1.19543437510799,
311.932654771081));
#13423=CARTESIAN_POINT('Ctrl Pts',(-35.7989877963167,-1.2050066569793,311.93340398644));
#13424=CARTESIAN_POINT('Ctrl Pts',(-35.7933059444162,-1.21453699566369,
311.934153201799));
#13425=CARTESIAN_POINT('Ctrl Pts',(-35.7528702987077,-1.2823609033043,311.939485091357));
#13426=CARTESIAN_POINT('Ctrl Pts',(-35.708967236505,-1.3482917795089,311.944816980916));
#13427=CARTESIAN_POINT('Ctrl Pts',(-35.6617993488414,-1.41195292330395,
311.950148870474));
#13428=CARTESIAN_POINT('Ctrl Pts',(-35.6146996891026,-1.47552198182783,
311.955473047503));
#13429=CARTESIAN_POINT('Ctrl Pts',(-35.5643448589644,-1.53682745428348,
311.960797224531));
#13430=CARTESIAN_POINT('Ctrl Pts',(-35.5109821719493,-1.59551918717068,
311.966121401559));
#13431=CARTESIAN_POINT('Ctrl Pts',(-35.4576816657471,-1.65414252958002,
311.971439374596));
#13432=CARTESIAN_POINT('Ctrl Pts',(-35.4013805814392,-1.71015783971322,
311.976757347633));
#13433=CARTESIAN_POINT('Ctrl Pts',(-35.3423672253538,-1.76324703036719,
311.98207532067));
#13434=CARTESIAN_POINT('Ctrl Pts',(-35.2833915279335,-1.81630234279122,
311.987389900106));
#13435=CARTESIAN_POINT('Ctrl Pts',(-35.2217073416918,-1.86643492922096,
311.992704479542));
#13436=CARTESIAN_POINT('Ctrl Pts',(-35.1576397857835,-1.91336354219033,
311.998019058978));
#13437=CARTESIAN_POINT('Ctrl Pts',(-35.0935931520858,-1.96027682992512,
312.003331902859));
#13438=CARTESIAN_POINT('Ctrl Pts',(-35.0271650721852,-2.00398794501738,
312.008644746741));
#13439=CARTESIAN_POINT('Ctrl Pts',(-34.9587125253792,-2.04425687656842,
312.013957590622));
#13440=CARTESIAN_POINT('Ctrl Pts',(-34.8902610052486,-2.08452520415186,
312.01927035482));
#13441=CARTESIAN_POINT('Ctrl Pts',(-34.8197854833435,-2.12135121424258,
312.024583119017));
#13442=CARTESIAN_POINT('Ctrl Pts',(-34.747669314551,-2.15453984670573,312.029895883215));
#13443=CARTESIAN_POINT('Ctrl Pts',(-34.6754811747129,-2.18776160101411,
312.035213949485));
#13444=CARTESIAN_POINT('Ctrl Pts',(-34.6016495440834,-2.21733852968924,
312.040532015756));
#13445=CARTESIAN_POINT('Ctrl Pts',(-34.5265790874744,-2.24312319820511,
312.045850082026));
#13446=CARTESIAN_POINT('Ctrl Pts',(-34.4514726811573,-2.26892021447198,
312.05117069501));
#13447=CARTESIAN_POINT('Ctrl Pts',(-34.3751267181411,-2.29092122274619,
312.056491307994));
#13448=CARTESIAN_POINT('Ctrl Pts',(-34.2979599335368,-2.30902905178901,
312.061811920978));
#13449=CARTESIAN_POINT('Ctrl Pts',(-34.2206523851189,-2.3271699122337,312.067142239559));
#13450=CARTESIAN_POINT('Ctrl Pts',(-34.1425214855963,-2.34140331815997,
312.072472558141));
#13451=CARTESIAN_POINT('Ctrl Pts',(-34.0639948541079,-2.35168353790619,
312.077802876723));
#13452=CARTESIAN_POINT('Ctrl Pts',(-33.9890497781242,-2.36149488261062,
312.082890082471));
#13453=CARTESIAN_POINT('Ctrl Pts',(-33.9137446419557,-2.36770579685038,
312.08797728822));
#13454=CARTESIAN_POINT('Ctrl Pts',(-33.8384508664992,-2.3703208322215,312.093064493968));
#13455=CARTESIAN_POINT('Ctrl Pts',(-33.7595355956675,-2.37306164609749,
312.098396385177));
#13456=CARTESIAN_POINT('Ctrl Pts',(-33.6803337729824,-2.37186234919343,
312.103728276385));
#13457=CARTESIAN_POINT('Ctrl Pts',(-33.6012717911821,-2.3666892316017,312.109060167594));
#13458=CARTESIAN_POINT('Ctrl Pts',(-33.522324169655,-2.36152359673589,312.114384346416));
#13459=CARTESIAN_POINT('Ctrl Pts',(-33.4435164512169,-2.3523955862334,312.119708525239));
#13460=CARTESIAN_POINT('Ctrl Pts',(-33.3652769327858,-2.33932346367807,
312.125032704061));
#13461=CARTESIAN_POINT('Ctrl Pts',(-33.2871285798085,-2.32626657288809,
312.130350679098));
#13462=CARTESIAN_POINT('Ctrl Pts',(-33.2095475711884,-2.30927477960603,
312.135668654135));
#13463=CARTESIAN_POINT('Ctrl Pts',(-33.1329574487279,-2.28841817450127,
312.140986629173));
#13464=CARTESIAN_POINT('Ctrl Pts',(-33.0564161995297,-2.26757487829723,
312.146301210733));
#13465=CARTESIAN_POINT('Ctrl Pts',(-32.9808650326342,-2.24287178808603,
312.151615792294));
#13466=CARTESIAN_POINT('Ctrl Pts',(-32.9067164581259,-2.21442989298486,
312.156930373854));
#13467=CARTESIAN_POINT('Ctrl Pts',(-32.8325920962496,-2.18599728536019,
312.16224321998));
#13468=CARTESIAN_POINT('Ctrl Pts',(-32.7598698547046,-2.15382846492925,
312.167556066106));
#13469=CARTESIAN_POINT('Ctrl Pts',(-32.6889448333807,-2.1180935370849,312.172868912231));
#13470=CARTESIAN_POINT('Ctrl Pts',(-32.618020874264,-2.08235914442396,312.178181678789));
#13471=CARTESIAN_POINT('Ctrl Pts',(-32.5488944999614,-2.04305896265678,
312.183494445347));
#13472=CARTESIAN_POINT('Ctrl Pts',(-32.4819373074894,-2.00040961446246,
312.188807211906));
#13473=CARTESIAN_POINT('Ctrl Pts',(-32.4149132905271,-1.95771770144649,
312.194125280701));
#13474=CARTESIAN_POINT('Ctrl Pts',(-32.3500631764176,-1.91167019732476,
312.199443349496));
#13475=CARTESIAN_POINT('Ctrl Pts',(-32.2877300672236,-1.86252743231786,
312.204761418291));
#13476=CARTESIAN_POINT('Ctrl Pts',(-32.2253671068937,-1.81336113299066,
312.210082033894));
#13477=CARTESIAN_POINT('Ctrl Pts',(-32.1655239064085,-1.76109692860741,
312.215402649496));
#13478=CARTESIAN_POINT('Ctrl Pts',(-32.108508934623,-1.70603419951466,312.220723265098));
#13479=CARTESIAN_POINT('Ctrl Pts',(-32.0513899576581,-1.65087102647119,
312.226053586424));
#13480=CARTESIAN_POINT('Ctrl Pts',(-31.9971098399933,-1.59289947081792,
312.23138390775));
#13481=CARTESIAN_POINT('Ctrl Pts',(-31.9459386196224,-1.53245424029687,
312.236714229077));
#13482=CARTESIAN_POINT('Ctrl Pts',(-31.8971015075738,-1.47476613994748,
312.241801414764));
#13483=CARTESIAN_POINT('Ctrl Pts',(-31.8510960450867,-1.41482542098347,
312.246888600451));
#13484=CARTESIAN_POINT('Ctrl Pts',(-31.8081195609236,-1.35294677700163,
312.251975786138));
#13485=CARTESIAN_POINT('Ctrl Pts',(-31.7630763027158,-1.28809233875003,
312.257307618718));
#13486=CARTESIAN_POINT('Ctrl Pts',(-31.7211899938245,-1.22086312288555,
312.262639451299));
#13487=CARTESIAN_POINT('Ctrl Pts',(-31.6827199018342,-1.15159930663276,
312.267971283879));
#13488=CARTESIAN_POINT('Ctrl Pts',(-31.6443054574035,-1.08243568151933,
312.273295403885));
#13489=CARTESIAN_POINT('Ctrl Pts',(-31.6092976422666,-1.01124370697533,
312.27861952389));
#13490=CARTESIAN_POINT('Ctrl Pts',(-31.5779130645903,-0.938393309894114,
312.283943643895));
#13491=CARTESIAN_POINT('Ctrl Pts',(-31.5465650569767,-0.865627799843034,
312.289261560109));
#13492=CARTESIAN_POINT('Ctrl Pts',(-31.5188320815638,-0.791208135782106,
312.294579476322));
#13493=CARTESIAN_POINT('Ctrl Pts',(-31.4948846034213,-0.715528316831581,
312.299897392535));
#13494=CARTESIAN_POINT('Ctrl Pts',(-31.4709524065829,-0.639896790495606,
312.305211915293));
#13495=CARTESIAN_POINT('Ctrl Pts',(-31.4508010535546,-0.563007151119864,
312.31052643805));
#13496=CARTESIAN_POINT('Ctrl Pts',(-31.4345522474832,-0.485271690604297,
312.315840960808));
#13497=CARTESIAN_POINT('Ctrl Pts',(-31.418308747079,-0.407561612783178,
312.321153748233));
#13498=CARTESIAN_POINT('Ctrl Pts',(-31.4059653591345,-0.329006720823476,
312.326466535658));
#13499=CARTESIAN_POINT('Ctrl Pts',(-31.3975930684317,-0.250031272042916,
312.331779323083));
#13500=CARTESIAN_POINT('Ctrl Pts',(-31.3892209028309,-0.171057003342323,
312.337092031122));
#13501=CARTESIAN_POINT('Ctrl Pts',(-31.3848197646244,-0.091662656688382,
312.342404739161));
#13502=CARTESIAN_POINT('Ctrl Pts',(-31.3844088052639,-0.0122779253132078,
312.347717447201));
#13503=CARTESIAN_POINT('Ctrl Pts',(-31.3839974357001,0.0671860447643005,
312.353035458175));
#13504=CARTESIAN_POINT('Ctrl Pts',(-31.3875842036757,0.146639910430197,
312.35835346915));
#13505=CARTESIAN_POINT('Ctrl Pts',(-31.395136085621,0.225654260881445,312.363671480124));
#13506=CARTESIAN_POINT('Ctrl Pts',(-31.4026915845848,0.304706455722512,
312.368992038191));
#13507=CARTESIAN_POINT('Ctrl Pts',(-31.4142159127505,0.383318251454429,
312.374312596259));
#13508=CARTESIAN_POINT('Ctrl Pts',(-31.4296244623578,0.46106820246088,312.379633154326));
#13509=CARTESIAN_POINT('Ctrl Pts',(-31.4450611235255,0.53896000149998,312.384963419289));
#13510=CARTESIAN_POINT('Ctrl Pts',(-31.4643960521091,0.615986357909321,
312.390293684253));
#13511=CARTESIAN_POINT('Ctrl Pts',(-31.487494128881,0.691738999896711,312.395623949216));
#13512=CARTESIAN_POINT('Ctrl Pts',(-31.5095411209127,0.764044495750783,
312.400711658913));
#13513=CARTESIAN_POINT('Ctrl Pts',(-31.5350160632737,0.835189354047978,
312.40579936861));
#13514=CARTESIAN_POINT('Ctrl Pts',(-31.5637612271422,0.904837150958008,
312.410887078307));
#13515=CARTESIAN_POINT('Ctrl Pts',(-31.5938795252724,0.977811969297648,
312.416217823964));
#13516=CARTESIAN_POINT('Ctrl Pts',(-31.6277023981692,1.04941960203306,312.421548569621));
#13517=CARTESIAN_POINT('Ctrl Pts',(-31.665084385894,1.11925812164284,312.426879315278));
#13518=CARTESIAN_POINT('Ctrl Pts',(-31.7024162474512,1.18900299354797,312.432202912844));
#13519=CARTESIAN_POINT('Ctrl Pts',(-31.7432975322467,1.25698305129138,312.43752651041));
#13520=CARTESIAN_POINT('Ctrl Pts',(-31.7875346475331,1.32281597845853,312.442850107976));
#13521=CARTESIAN_POINT('Ctrl Pts',(-31.8317262322102,1.3885811477424,312.448168226282));
#13522=CARTESIAN_POINT('Ctrl Pts',(-31.8792665293994,1.45220318731645,312.453486344589));
#13523=CARTESIAN_POINT('Ctrl Pts',(-31.9299166404324,1.51332537573932,312.458804462895));
#13524=CARTESIAN_POINT('Ctrl Pts',(-31.9807043723432,1.5746136386101,312.464137031004));
#13525=CARTESIAN_POINT('Ctrl Pts',(-32.0346185914475,1.63338804235399,312.469469599113));
#13526=CARTESIAN_POINT('Ctrl Pts',(-32.0913757049304,1.68931971632635,312.474802167222));
#13527=CARTESIAN_POINT('Ctrl Pts',(-32.1479238672211,1.74504547796029,312.480115103493));
#13528=CARTESIAN_POINT('Ctrl Pts',(-32.2072936865423,1.79794907900351,312.485428039764));
#13529=CARTESIAN_POINT('Ctrl Pts',(-32.2691668342109,1.8477411757988,312.490740976035));
#13530=CARTESIAN_POINT('Ctrl Pts',(-32.331382923209,1.89780925286208,312.496083360063));
#13531=CARTESIAN_POINT('Ctrl Pts',(-32.3961298253543,1.94473090088057,312.501425744091));
#13532=CARTESIAN_POINT('Ctrl Pts',(-32.4630506189796,1.98825337168764,312.506768128119));
#13533=CARTESIAN_POINT('Ctrl Pts',(-32.529971412605,2.03177584249472,312.512110512147));
#13534=CARTESIAN_POINT('Ctrl Pts',(-32.5990656820435,2.07189889291044,312.517452896175));
#13535=CARTESIAN_POINT('Ctrl Pts',(-32.6699490794746,2.10841540797695,312.522795280203));
#13536=CARTESIAN_POINT('Ctrl Pts',(-32.671423404392,2.10551637491536,311.522951534327));
#13537=CARTESIAN_POINT('Ctrl Pts',(-33.0861637626343,2.31676127052873,311.554077895371));
#13538=CARTESIAN_POINT('Ctrl Pts',(-34.370461869201,2.57526687590523,311.638174687139));
#13539=CARTESIAN_POINT('Ctrl Pts',(-35.8730654168255,1.52349643505371,311.746720658333));
#13540=CARTESIAN_POINT('Ctrl Pts',(-36.124914683777,0.366246935917719,311.824140268482));
#13541=CARTESIAN_POINT('Ctrl Pts',(-36.1242308850569,0.000504174819979179,
311.848589447908));
#13542=CARTESIAN_POINT('',(-36.1278763296291,0.00181651129381628,311.651410108134));
#13543=CARTESIAN_POINT('Ctrl Pts',(-32.6699490813724,2.10841540895464,311.327581625012));
#13544=CARTESIAN_POINT('Ctrl Pts',(-32.7205654232083,2.13449108354362,311.331178936796));
#13545=CARTESIAN_POINT('Ctrl Pts',(-32.7721103252405,2.15873867404495,311.334712996911));
#13546=CARTESIAN_POINT('Ctrl Pts',(-32.9896249628738,2.25164825657492,311.349290190744));
#13547=CARTESIAN_POINT('Ctrl Pts',(-33.162230184724,2.30319960325097,311.360115343024));
#13548=CARTESIAN_POINT('Ctrl Pts',(-33.3839627058096,2.34281417314571,311.374477384485));
#13549=CARTESIAN_POINT('Ctrl Pts',(-33.4291487138416,2.34954661143632,311.377423744701));
#13550=CARTESIAN_POINT('Ctrl Pts',(-33.4998834845089,2.3580057069336,311.382082448808));
#13551=CARTESIAN_POINT('Ctrl Pts',(-33.5253148392667,2.36063070297005,311.383766632749));
#13552=CARTESIAN_POINT('Ctrl Pts',(-33.572782540978,2.36475590794514,311.38692985141));
#13553=CARTESIAN_POINT('Ctrl Pts',(-33.594807188374,2.36636040310828,311.388405424546));
#13554=CARTESIAN_POINT('Ctrl Pts',(-33.6444342595934,2.36927969869497,311.391749439544));
#13555=CARTESIAN_POINT('Ctrl Pts',(-33.6720432953709,2.37042008473026,311.39362315748));
#13556=CARTESIAN_POINT('Ctrl Pts',(-33.7582624873515,2.37247320724289,311.399518872214));
#13557=CARTESIAN_POINT('Ctrl Pts',(-33.8168867716744,2.37169578604935,311.403592168914));
#13558=CARTESIAN_POINT('Ctrl Pts',(-33.9601713987383,2.36447992657897,311.413709141659));
#13559=CARTESIAN_POINT('Ctrl Pts',(-34.0446273250634,2.355666506971,311.419812539606));
#13560=CARTESIAN_POINT('Ctrl Pts',(-34.2604796936735,2.32135866298747,311.4356949175));
#13561=CARTESIAN_POINT('Ctrl Pts',(-34.3905255546372,2.28923944315662,311.445548742057));
#13562=CARTESIAN_POINT('Ctrl Pts',(-34.5630680812351,2.23078289284199,311.458594258394));
#13563=CARTESIAN_POINT('Ctrl Pts',(-34.608479469465,2.21382976447803,311.462022857776));
#13564=CARTESIAN_POINT('Ctrl Pts',(-34.6703974044628,2.18852625533206,311.4666623385));
#13565=CARTESIAN_POINT('Ctrl Pts',(-34.6873708936482,2.18135792748381,311.467930379396));
#13566=CARTESIAN_POINT('Ctrl Pts',(-34.7159236097044,2.16890536913153,311.470054998019));
#13567=CARTESIAN_POINT('Ctrl Pts',(-34.7275467076526,2.16372452414726,311.470917434055));
#13568=CARTESIAN_POINT('Ctrl Pts',(-34.7522230155996,2.152486440578,311.472742602199));
#13569=CARTESIAN_POINT('Ctrl Pts',(-34.7652636258918,2.14640360766929,311.473703807661));
#13570=CARTESIAN_POINT('Ctrl Pts',(-34.8023373674329,2.12869786672292,311.476429183158));
#13571=CARTESIAN_POINT('Ctrl Pts',(-34.826231543144,2.11678698863427,311.478176889936));
#13572=CARTESIAN_POINT('Ctrl Pts',(-34.937685953362,2.05885892858413,311.486311244375));
#13573=CARTESIAN_POINT('Ctrl Pts',(-35.0225214041157,2.00779256912676,311.492452690073));
#13574=CARTESIAN_POINT('Ctrl Pts',(-35.260429073613,1.84348809778238,311.510239716022));
#13575=CARTESIAN_POINT('Ctrl Pts',(-35.4033468398871,1.71698387361544,311.521727117173));
#13576=CARTESIAN_POINT('Ctrl Pts',(-35.5537704365291,1.54757844631576,311.536313351547));
#13577=CARTESIAN_POINT('Ctrl Pts',(-35.5772895686174,1.5198314516041,311.538678107176));
#13578=CARTESIAN_POINT('Ctrl Pts',(-35.6149210354168,1.47330709005423,311.542611679588));
#13579=CARTESIAN_POINT('Ctrl Pts',(-35.6294094527706,1.45484082762781,311.544165125999));
#13580=CARTESIAN_POINT('Ctrl Pts',(-35.657375319916,1.41808636385474,311.547243666299));
#13581=CARTESIAN_POINT('Ctrl Pts',(-35.6708688087159,1.39981350674182,311.548767899338));
#13582=CARTESIAN_POINT('Ctrl Pts',(-35.7029329355317,1.35506114375053,311.552487425318));
#13583=CARTESIAN_POINT('Ctrl Pts',(-35.721227965454,1.32839078211471,311.554692955811));
#13584=CARTESIAN_POINT('Ctrl Pts',(-35.7917645191564,1.22091595110344,311.563541629351));
#13585=CARTESIAN_POINT('Ctrl Pts',(-35.8396073329563,1.137348394133,311.570341235822));
#13586=CARTESIAN_POINT('Ctrl Pts',(-35.9640172724249,0.885702064154583,
311.590544314634));
#13587=CARTESIAN_POINT('Ctrl Pts',(-36.0262080375081,0.711320133444521,
311.604257744596));
#13588=CARTESIAN_POINT('Ctrl Pts',(-36.0760279630006,0.494658036375356,
311.620044419309));
#13589=CARTESIAN_POINT('Ctrl Pts',(-36.0836175175372,0.457619193461639,
311.622698352683));
#13590=CARTESIAN_POINT('Ctrl Pts',(-36.0931971584312,0.404431606899662,
311.62643121419));
#13591=CARTESIAN_POINT('Ctrl Pts',(-36.0959113741356,0.388421125193596,
311.62754482376));
#13592=CARTESIAN_POINT('Ctrl Pts',(-36.1004261515361,0.360022666108016,
311.629500821265));
#13593=CARTESIAN_POINT('Ctrl Pts',(-36.1022933905915,0.347646548247032,
311.630346701726));
#13594=CARTESIAN_POINT('Ctrl Pts',(-36.10576382888,0.323341589605107,311.631995019574));
#13595=CARTESIAN_POINT('Ctrl Pts',(-36.107374296921,0.31141479668319,311.632797931021));
#13596=CARTESIAN_POINT('Ctrl Pts',(-36.1108662962818,0.283980671111723,
311.634632231051));
#13597=CARTESIAN_POINT('Ctrl Pts',(-36.1126855749867,0.268465804968367,
311.635660384521));
#13598=CARTESIAN_POINT('Ctrl Pts',(-36.1175734049914,0.222894162164295,
311.638656400295));
#13599=CARTESIAN_POINT('Ctrl Pts',(-36.1202212125426,0.192794368185148,
311.640604738208));
#13600=CARTESIAN_POINT('Ctrl Pts',(-36.1259712436791,0.109145623039551,
311.645955056815));
#13601=CARTESIAN_POINT('Ctrl Pts',(-36.1278334709158,0.0555286738497468,
311.649311870199));
#13602=CARTESIAN_POINT('Ctrl Pts',(-36.1278762701717,0.00189255109243725,
311.652636760053));
#13603=CARTESIAN_POINT('Ctrl Pts',(-36.1278763296291,0.00181651129381628,
311.651410108134));
#13604=CARTESIAN_POINT('Ctrl Pts',(-36.1279360242218,-0.0761244347127474,
311.65665745587));
#13605=CARTESIAN_POINT('Ctrl Pts',(-36.1241495396959,-0.154209488219651,
311.661904803605));
#13606=CARTESIAN_POINT('Ctrl Pts',(-36.1165007931509,-0.232020986854782,
311.667152151341));
#13607=CARTESIAN_POINT('Ctrl Pts',(-36.1088615680256,-0.309735623091775,
311.672392967));
#13608=CARTESIAN_POINT('Ctrl Pts',(-36.0973696750115,-0.387176902131175,
311.677633782659));
#13609=CARTESIAN_POINT('Ctrl Pts',(-36.0820610669041,-0.463927684461548,
311.682874598318));
#13610=CARTESIAN_POINT('Ctrl Pts',(-36.0667627704861,-0.540626768412813,
311.688111883828));
#13611=CARTESIAN_POINT('Ctrl Pts',(-36.0476529513995,-0.616635804913145,
311.693349169338));
#13612=CARTESIAN_POINT('Ctrl Pts',(-36.0248191594953,-0.691544693095099,
311.698586454848));
#13613=CARTESIAN_POINT('Ctrl Pts',(-36.0019931453665,-0.766428065387754,
311.703821956404));
#13614=CARTESIAN_POINT('Ctrl Pts',(-35.975445816364,-0.840211570422187,
311.709057457961));
#13615=CARTESIAN_POINT('Ctrl Pts',(-35.9453149843139,-0.912498845162449,
311.714292959517));
#13616=CARTESIAN_POINT('Ctrl Pts',(-35.9151843840198,-0.984785563893851,
311.719528420804));
#13617=CARTESIAN_POINT('Ctrl Pts',(-35.8814705237313,-1.05557562941191,
311.724763882091));
#13618=CARTESIAN_POINT('Ctrl Pts',(-35.8443592521434,-1.12449287640938,
311.729999343377));
#13619=CARTESIAN_POINT('Ctrl Pts',(-35.807211913622,-1.19347710127281,311.735239892796));
#13620=CARTESIAN_POINT('Ctrl Pts',(-35.766660803185,-1.26058444773637,311.740480442214));
#13621=CARTESIAN_POINT('Ctrl Pts',(-35.7229371941708,-1.32546437974002,
311.745720991632));
#13622=CARTESIAN_POINT('Ctrl Pts',(-35.6791906631924,-1.39037832484348,
311.750964288392));
#13623=CARTESIAN_POINT('Ctrl Pts',(-35.632268615843,-1.45306214577811,311.756207585152));
#13624=CARTESIAN_POINT('Ctrl Pts',(-35.582443414649,-1.51319744525969,311.761450881912));
#13625=CARTESIAN_POINT('Ctrl Pts',(-35.5325342744983,-1.57343405279763,
311.76670301189));
#13626=CARTESIAN_POINT('Ctrl Pts',(-35.4797125464819,-1.63111321409497,
311.771955141867));
#13627=CARTESIAN_POINT('Ctrl Pts',(-35.4242878302129,-1.68595302167966,
311.777207271845));
#13628=CARTESIAN_POINT('Ctrl Pts',(-35.3910604008471,-1.71882979499703,
311.780355953329));
#13629=CARTESIAN_POINT('Ctrl Pts',(-35.3568981046379,-1.75068684193181,
311.783504634813));
#13630=CARTESIAN_POINT('Ctrl Pts',(-35.3218729594151,-1.78147066553713,
311.786653316296));
#13631=CARTESIAN_POINT('Ctrl Pts',(-35.262562423286,-1.83359907415669,311.791985199596));
#13632=CARTESIAN_POINT('Ctrl Pts',(-35.2005333909952,-1.88286108117392,
311.797317082897));
#13633=CARTESIAN_POINT('Ctrl Pts',(-35.1360943489985,-1.92896040599787,
311.802648966197));
#13634=CARTESIAN_POINT('Ctrl Pts',(-35.0717485172144,-1.97499304876486,
311.807973136999));
#13635=CARTESIAN_POINT('Ctrl Pts',(-35.004999976621,-2.01787182371846,311.813297307801));
#13636=CARTESIAN_POINT('Ctrl Pts',(-34.9361916222065,-2.05733944927128,
311.818621478603));
#13637=CARTESIAN_POINT('Ctrl Pts',(-34.8674634457484,-2.09676108573469,
311.823939445491));
#13638=CARTESIAN_POINT('Ctrl Pts',(-34.796680629712,-2.13277923951948,311.829257412379));
#13639=CARTESIAN_POINT('Ctrl Pts',(-34.7242152333153,-2.16517973478409,
311.834575379267));
#13640=CARTESIAN_POINT('Ctrl Pts',(-34.6517960792214,-2.1975595543388,311.839889952604));
#13641=CARTESIAN_POINT('Ctrl Pts',(-34.5776969027343,-2.22632610655882,
311.845204525941));
#13642=CARTESIAN_POINT('Ctrl Pts',(-34.5023134833563,-2.25131158044595,
311.850519099277));
#13643=CARTESIAN_POINT('Ctrl Pts',(-34.4269546807666,-2.27628889521632,
311.855831937117));
#13644=CARTESIAN_POINT('Ctrl Pts',(-34.3503129127364,-2.29748743606748,
311.861144774956));
#13645=CARTESIAN_POINT('Ctrl Pts',(-34.2728016154043,-2.31478842022262,
311.866457612795));
#13646=CARTESIAN_POINT('Ctrl Pts',(-34.1952914796619,-2.33208914510403,
311.871770371016));
#13647=CARTESIAN_POINT('Ctrl Pts',(-34.1169122983884,-2.34549232855847,
311.877083129237));
#13648=CARTESIAN_POINT('Ctrl Pts',(-34.0380888041827,-2.35493006641926,
311.882395887457));
#13649=CARTESIAN_POINT('Ctrl Pts',(-33.9591866428774,-2.36437722329236,
311.887713947895));
#13650=CARTESIAN_POINT('Ctrl Pts',(-33.8798397494492,-2.36985097290238,
311.893032008333));
#13651=CARTESIAN_POINT('Ctrl Pts',(-33.8004785106302,-2.3713352795936,311.898350068771));
#13652=CARTESIAN_POINT('Ctrl Pts',(-33.721079266264,-2.37282029710901,311.903670675991));
#13653=CARTESIAN_POINT('Ctrl Pts',(-33.6416661320715,-2.3703120804766,311.908991283211));
#13654=CARTESIAN_POINT('Ctrl Pts',(-33.5626674490636,-2.36384674944863,
311.914311890431));
#13655=CARTESIAN_POINT('Ctrl Pts',(-33.4835246576759,-2.35736962444709,
311.919642203435));
#13656=CARTESIAN_POINT('Ctrl Pts',(-33.4047982942091,-2.34692102251696,
311.924972516438));
#13657=CARTESIAN_POINT('Ctrl Pts',(-33.3269093570692,-2.33258874553894,
311.930302829441));
#13658=CARTESIAN_POINT('Ctrl Pts',(-33.2525720247612,-2.31890999634082,
311.935390089116));
#13659=CARTESIAN_POINT('Ctrl Pts',(-33.1789977522611,-2.30169415298837,
311.940477348791));
#13660=CARTESIAN_POINT('Ctrl Pts',(-33.1065386255153,-2.28105961636696,
311.945564608466));
#13661=CARTESIAN_POINT('Ctrl Pts',(-33.030595253178,-2.25943285424569,311.950896492426));
#13662=CARTESIAN_POINT('Ctrl Pts',(-32.9555891915697,-2.23396839258137,
311.956228376386));
#13663=CARTESIAN_POINT('Ctrl Pts',(-32.8819365800715,-2.20476509588785,
311.961560260346));
#13664=CARTESIAN_POINT('Ctrl Pts',(-32.8083905058681,-2.17560404128413,
311.966884431824));
#13665=CARTESIAN_POINT('Ctrl Pts',(-32.7361944261268,-2.142715062857,311.972208603301));
#13666=CARTESIAN_POINT('Ctrl Pts',(-32.6657503312906,-2.10624707186824,
311.977532774779));
#13667=CARTESIAN_POINT('Ctrl Pts',(-32.5953883201663,-2.06982157454872,
311.982850742361));
#13668=CARTESIAN_POINT('Ctrl Pts',(-32.5267746513005,-2.02982556655169,
311.988168709944));
#13669=CARTESIAN_POINT('Ctrl Pts',(-32.4602908736375,-1.98645582147061,
311.993486677527));
#13670=CARTESIAN_POINT('Ctrl Pts',(-32.3938495210811,-1.9431137518033,311.99880125157));
#13671=CARTESIAN_POINT('Ctrl Pts',(-32.3295357536859,-1.89640247359618,
312.004115825612));
#13672=CARTESIAN_POINT('Ctrl Pts',(-32.2677049907753,-1.84656381145296,
312.009430399655));
#13673=CARTESIAN_POINT('Ctrl Pts',(-32.2058944188493,-1.79674142424491,
312.014743238211));
#13674=CARTESIAN_POINT('Ctrl Pts',(-32.1465656060824,-1.74379397501524,
312.020056076767));
#13675=CARTESIAN_POINT('Ctrl Pts',(-32.0900423192198,-1.68800468447423,
312.025368915323));
#13676=CARTESIAN_POINT('Ctrl Pts',(-32.0335198793195,-1.63221622989706,
312.03068167427));
#13677=CARTESIAN_POINT('Ctrl Pts',(-31.9798032145028,-1.57358634894655,
312.035994433216));
#13678=CARTESIAN_POINT('Ctrl Pts',(-31.9291794388162,-1.51243531395428,
312.041307192163));
#13679=CARTESIAN_POINT('Ctrl Pts',(-31.8785051397142,-1.45122324915724,
312.046625253336));
#13680=CARTESIAN_POINT('Ctrl Pts',(-31.8309301956454,-1.3874853659602,312.05194331451));
#13681=CARTESIAN_POINT('Ctrl Pts',(-31.7867011799799,-1.3215747812562,312.057261375683));
#13682=CARTESIAN_POINT('Ctrl Pts',(-31.7424509832956,-1.25563263235569,
312.062581983645));
#13683=CARTESIAN_POINT('Ctrl Pts',(-31.7015501488218,-1.18751611161875,
312.067902591607));
#13684=CARTESIAN_POINT('Ctrl Pts',(-31.6642002979126,-1.11760486305292,
312.073223199569));
#13685=CARTESIAN_POINT('Ctrl Pts',(-31.6267823138835,-1.0475660832824,312.078553513315));
#13686=CARTESIAN_POINT('Ctrl Pts',(-31.5929284577645,-0.975726458808749,
312.083883827062));
#13687=CARTESIAN_POINT('Ctrl Pts',(-31.5627929280154,-0.90248745164398,
312.089214140809));
#13688=CARTESIAN_POINT('Ctrl Pts',(-31.5340315680465,-0.832588117987969,
312.094301394084));
#13689=CARTESIAN_POINT('Ctrl Pts',(-31.5086568979712,-0.761414594229492,
312.09938864736));
#13690=CARTESIAN_POINT('Ctrl Pts',(-31.4867600707703,-0.689326982194133,
312.104475900635));
#13691=CARTESIAN_POINT('Ctrl Pts',(-31.4638103195706,-0.613772987745216,
312.109807777984));
#13692=CARTESIAN_POINT('Ctrl Pts',(-31.4445943310761,-0.536928478462323,
312.115139655332));
#13693=CARTESIAN_POINT('Ctrl Pts',(-31.4292543726937,-0.459196821907729,
312.120471532681));
#13694=CARTESIAN_POINT('Ctrl Pts',(-31.4139366033829,-0.381577603291414,
312.125795697531));
#13695=CARTESIAN_POINT('Ctrl Pts',(-31.4024838202053,-0.303074241846239,
312.131119862381));
#13696=CARTESIAN_POINT('Ctrl Pts',(-31.3949885562303,-0.224105315821012,
312.13644402723));
#13697=CARTESIAN_POINT('Ctrl Pts',(-31.3875020259773,-0.145228406921945,
312.141761988193));
#13698=CARTESIAN_POINT('Ctrl Pts',(-31.3839638950802,-0.0658874758163853,
312.147079949155));
#13699=CARTESIAN_POINT('Ctrl Pts',(-31.3844153905843,0.0134901614254798,
312.152397910117));
#13700=CARTESIAN_POINT('Ctrl Pts',(-31.384866597977,0.0928171456831942,
312.157712477547));
#13701=CARTESIAN_POINT('Ctrl Pts',(-31.3893023759705,0.172180322016819,
312.163027044977));
#13702=CARTESIAN_POINT('Ctrl Pts',(-31.3977119282638,0.251149940815805,
312.168341612406));
#13703=CARTESIAN_POINT('Ctrl Pts',(-31.4061187344199,0.330093772104531,
312.173654444365));
#13704=CARTESIAN_POINT('Ctrl Pts',(-31.4184966885462,0.408643835201987,
312.178967276324));
#13705=CARTESIAN_POINT('Ctrl Pts',(-31.4347830522822,0.486374569268121,
312.184280108283));
#13706=CARTESIAN_POINT('Ctrl Pts',(-31.4510691720554,0.564104138960999,
312.189592860658));
#13707=CARTESIAN_POINT('Ctrl Pts',(-31.4712634876137,0.641013945416478,
312.194905613033));
#13708=CARTESIAN_POINT('Ctrl Pts',(-31.495252262682,0.716689172827941,312.200218365408));
#13709=CARTESIAN_POINT('Ctrl Pts',(-31.5192649793855,0.792439926758653,
312.205536420096));
#13710=CARTESIAN_POINT('Ctrl Pts',(-31.5470795786416,0.866953192264275,
312.210854474783));
#13711=CARTESIAN_POINT('Ctrl Pts',(-31.5785327572063,0.939830445479384,
312.216172529471));
#13712=CARTESIAN_POINT('Ctrl Pts',(-31.6100009987479,1.01274259972627,312.221493130983));
#13713=CARTESIAN_POINT('Ctrl Pts',(-31.6451110835093,1.08401675969073,312.226813732495));
#13714=CARTESIAN_POINT('Ctrl Pts',(-31.6836530628696,1.15327782330353,312.232134334007));
#13715=CARTESIAN_POINT('Ctrl Pts',(-31.7222653511026,1.22266523401594,312.237464641443));
#13716=CARTESIAN_POINT('Ctrl Pts',(-31.7643217950518,1.29003181142169,312.242794948878));
#13717=CARTESIAN_POINT('Ctrl Pts',(-31.8095684211962,1.35503050277643,312.248125256314));
#13718=CARTESIAN_POINT('Ctrl Pts',(-31.8527523677748,1.41706606773059,312.253212568477));
#13719=CARTESIAN_POINT('Ctrl Pts',(-31.8988417181438,1.47694467569995,312.258299880641));
#13720=CARTESIAN_POINT('Ctrl Pts',(-31.9475831132455,1.53439466266794,312.263387192804));
#13721=CARTESIAN_POINT('Ctrl Pts',(-31.9986528195241,1.59458895858519,312.268717519058));
#13722=CARTESIAN_POINT('Ctrl Pts',(-32.0528277432143,1.65234484218041,312.274047845311));
#13723=CARTESIAN_POINT('Ctrl Pts',(-32.1098460819132,1.7073245497213,312.279378171564));
#13724=CARTESIAN_POINT('Ctrl Pts',(-32.1667924423372,1.76223485249541,312.284701768971));
#13725=CARTESIAN_POINT('Ctrl Pts',(-32.2265747624877,1.81437560954772,312.290025366377));
#13726=CARTESIAN_POINT('Ctrl Pts',(-32.2888913929784,1.86344242247249,312.295348963783));
#13727=CARTESIAN_POINT('Ctrl Pts',(-32.3511417192024,1.91245702880295,312.300666896935));
#13728=CARTESIAN_POINT('Ctrl Pts',(-32.4159206342127,1.95840389809495,312.305984830087));
#13729=CARTESIAN_POINT('Ctrl Pts',(-32.482891265758,2.00101693227009,312.31130276324));
#13730=CARTESIAN_POINT('Ctrl Pts',(-32.5435379039074,2.03960604520561,312.316118527406));
#13731=CARTESIAN_POINT('Ctrl Pts',(-32.6059812320803,2.07546152952587,312.320934291572));
#13732=CARTESIAN_POINT('Ctrl Pts',(-32.6699490794746,2.10841540797695,312.325750055738));
#13733=CARTESIAN_POINT('Origin',(-33.7561270252576,0.,302.151410108095));
#13734=CARTESIAN_POINT('',(-32.6699490794746,2.10841540797695,313.522886073942));
#13735=CARTESIAN_POINT('',(-32.669949079475,2.10841540797714,313.324578124683));
#13736=CARTESIAN_POINT('',(-32.6699490794746,2.10841540797695,302.151410108095));
#13737=CARTESIAN_POINT('',(-36.1278760162702,-0.0021877227769147,312.848589891943));
#13738=CARTESIAN_POINT('Ctrl Pts',(-36.1278760162702,-0.00218772277689684,
312.848589891943));
#13739=CARTESIAN_POINT('Ctrl Pts',(-36.1277803864196,-0.105861736697777,
312.85554583238));
#13740=CARTESIAN_POINT('Ctrl Pts',(-36.1208833294905,-0.209232213304625,
312.862501772816));
#13741=CARTESIAN_POINT('Ctrl Pts',(-36.1073257787753,-0.31154852584567,
312.869457713252));
#13742=CARTESIAN_POINT('Ctrl Pts',(-36.0955253581672,-0.400604104425696,
312.875512127106));
#13743=CARTESIAN_POINT('Ctrl Pts',(-36.078679841791,-0.488861716537749,
312.88156654096));
#13744=CARTESIAN_POINT('Ctrl Pts',(-36.0569106229126,-0.575841036451612,
312.887620954814));
#13745=CARTESIAN_POINT('Ctrl Pts',(-36.0377363360177,-0.652452257243405,
312.892953671108));
#13746=CARTESIAN_POINT('Ctrl Pts',(-36.0146951003667,-0.72824970273293,
312.898286387402));
#13747=CARTESIAN_POINT('Ctrl Pts',(-35.9878724107818,-0.80281417320027,
312.903619103696));
#13748=CARTESIAN_POINT('Ctrl Pts',(-35.9610885250329,-0.877270772774612,
312.908944105258));
#13749=CARTESIAN_POINT('Ctrl Pts',(-35.9305342065032,-0.950497502270844,
312.914269106821));
#13750=CARTESIAN_POINT('Ctrl Pts',(-35.8963454245516,-1.0220876996732,312.919594108383));
#13751=CARTESIAN_POINT('Ctrl Pts',(-35.8621965206471,-1.09359439374219,
312.924912898824));
#13752=CARTESIAN_POINT('Ctrl Pts',(-35.8244217786945,-1.16346792834909,
312.930231689266));
#13753=CARTESIAN_POINT('Ctrl Pts',(-35.7832056612843,-1.23132053741675,
312.935550479707));
#13754=CARTESIAN_POINT('Ctrl Pts',(-35.742015877669,-1.29912979410644,312.940865871868));
#13755=CARTESIAN_POINT('Ctrl Pts',(-35.6973893254698,-1.36492028861939,
312.946181264028));
#13756=CARTESIAN_POINT('Ctrl Pts',(-35.6495563344201,-1.42832892349921,
312.951496656189));
#13757=CARTESIAN_POINT('Ctrl Pts',(-35.6017390133426,-1.49171678586353,
312.95681030704));
#13758=CARTESIAN_POINT('Ctrl Pts',(-35.5507176213022,-1.55272396416407,
312.962123957891));
#13759=CARTESIAN_POINT('Ctrl Pts',(-35.4967648808627,-1.61101766537006,
312.967437608742));
#13760=CARTESIAN_POINT('Ctrl Pts',(-35.4428130188985,-1.66931041741987,
312.972751173075));
#13761=CARTESIAN_POINT('Ctrl Pts',(-35.3859302227345,-1.72488943713238,
312.978064737407));
#13762=CARTESIAN_POINT('Ctrl Pts',(-35.3264274278707,-1.77745737165566,
312.98337830174));
#13763=CARTESIAN_POINT('Ctrl Pts',(-35.2668654415753,-1.83007759903868,
312.988697151832));
#13764=CARTESIAN_POINT('Ctrl Pts',(-35.2046786022178,-1.87968044658249,
312.994016001924));
#13765=CARTESIAN_POINT('Ctrl Pts',(-35.1402119786694,-1.92600802289063,
312.999334852016));
#13766=CARTESIAN_POINT('Ctrl Pts',(-35.0757145801997,-1.97235771494546,
313.004656241208));
#13767=CARTESIAN_POINT('Ctrl Pts',(-35.0089356237967,-2.01542876648465,
313.009977630401));
#13768=CARTESIAN_POINT('Ctrl Pts',(-34.940248143378,-2.05500735768059,313.015299019593));
#13769=CARTESIAN_POINT('Ctrl Pts',(-34.8714356706571,-2.09465797101505,
313.020630092248));
#13770=CARTESIAN_POINT('Ctrl Pts',(-34.8007081524456,-2.13080321061484,
313.025961164903));
#13771=CARTESIAN_POINT('Ctrl Pts',(-34.7284619600125,-2.16327595030203,
313.031292237559));
#13772=CARTESIAN_POINT('Ctrl Pts',(-34.6596182378814,-2.19421937019132,
313.0363722407));
#13773=CARTESIAN_POINT('Ctrl Pts',(-34.5893960069771,-2.22182831486617,
313.041452243842));
#13774=CARTESIAN_POINT('Ctrl Pts',(-34.5181506453613,-2.24600045968474,
313.046532246984));
#13775=CARTESIAN_POINT('Ctrl Pts',(-34.4433707229326,-2.27137181121518,
313.051864274673));
#13776=CARTESIAN_POINT('Ctrl Pts',(-34.3671808330306,-2.29305242269349,
313.057196302363));
#13777=CARTESIAN_POINT('Ctrl Pts',(-34.2899796105284,-2.31088716290944,
313.062528330052));
#13778=CARTESIAN_POINT('Ctrl Pts',(-34.2128899123519,-2.32869613918914,
313.067852655133));
#13779=CARTESIAN_POINT('Ctrl Pts',(-34.1347922357811,-2.34267017248802,
313.073176980214));
#13780=CARTESIAN_POINT('Ctrl Pts',(-34.0561020108446,-2.35270335370231,
313.078501305295));
#13781=CARTESIAN_POINT('Ctrl Pts',(-33.9775032689726,-2.36272487061947,
313.083819440464));
#13782=CARTESIAN_POINT('Ctrl Pts',(-33.8983138103218,-2.36881458095319,
313.089137575632));
#13783=CARTESIAN_POINT('Ctrl Pts',(-33.8189594424695,-2.37091757550686,
313.094455710801));
#13784=CARTESIAN_POINT('Ctrl Pts',(-33.7396555858598,-2.37301923144652,
313.09977046083));
#13785=CARTESIAN_POINT('Ctrl Pts',(-33.6601874957708,-2.37113919603529,
313.10508521086));
#13786=CARTESIAN_POINT('Ctrl Pts',(-33.5809850785911,-2.36527447900193,
313.110399960889));
#13787=CARTESIAN_POINT('Ctrl Pts',(-33.5018084038412,-2.35941166812337,
313.115712983514));
#13788=CARTESIAN_POINT('Ctrl Pts',(-33.4228976977028,-2.34956678191858,
313.121026006139));
#13789=CARTESIAN_POINT('Ctrl Pts',(-33.3446803444295,-2.3357888798724,313.126339028764));
#13790=CARTESIAN_POINT('Ctrl Pts',(-33.2664640487071,-2.32201116411265,
313.131651979553));
#13791=CARTESIAN_POINT('Ctrl Pts',(-33.1889415486718,-2.30430062086182,
313.136964930343));
#13792=CARTESIAN_POINT('Ctrl Pts',(-33.1125311238695,-2.28275762581497,
313.142277881132));
#13793=CARTESIAN_POINT('Ctrl Pts',(-33.0360442884017,-2.26119308770524,
313.147596144889));
#13794=CARTESIAN_POINT('Ctrl Pts',(-32.96067220197,-2.23578856947746,313.152914408646));
#13795=CARTESIAN_POINT('Ctrl Pts',(-32.8868184508175,-2.2066945110062,313.158232672403));
#13796=CARTESIAN_POINT('Ctrl Pts',(-32.8129292469554,-2.17758648624088,
313.163553489136));
#13797=CARTESIAN_POINT('Ctrl Pts',(-32.7405602579407,-2.14478558668956,
313.168874305869));
#13798=CARTESIAN_POINT('Ctrl Pts',(-32.6700931563666,-2.10848962485513,
313.174195122602));
#13799=CARTESIAN_POINT('Ctrl Pts',(-32.5994974099785,-2.07212740107497,
313.179525653024));
#13800=CARTESIAN_POINT('Ctrl Pts',(-32.5308108956193,-2.03225760100031,
313.184856183446));
#13801=CARTESIAN_POINT('Ctrl Pts',(-32.4643886639911,-1.989122939522,313.190186713867));
#13802=CARTESIAN_POINT('Ctrl Pts',(-32.4010183360325,-1.9479701872392,313.195272322296));
#13803=CARTESIAN_POINT('Ctrl Pts',(-32.3397090541619,-1.90384624575719,
313.200357930725));
#13804=CARTESIAN_POINT('Ctrl Pts',(-32.280740185164,-1.85699535125395,313.205443539153));
#13805=CARTESIAN_POINT('Ctrl Pts',(-32.2189629243854,-1.80791318338083,
313.210771349631));
#13806=CARTESIAN_POINT('Ctrl Pts',(-32.1595194065857,-1.75565099827935,
313.216099160109));
#13807=CARTESIAN_POINT('Ctrl Pts',(-32.1027557233654,-1.70045917345262,
313.221426970587));
#13808=CARTESIAN_POINT('Ctrl Pts',(-32.0460743470137,-1.64534737631299,
313.226747055783));
#13809=CARTESIAN_POINT('Ctrl Pts',(-31.9920654229078,-1.58731469948817,
313.23206714098));
#13810=CARTESIAN_POINT('Ctrl Pts',(-31.9410428092489,-1.52665233478226,
313.237387226177));
#13811=CARTESIAN_POINT('Ctrl Pts',(-31.8900796960507,-1.46606071201581,
313.242701107311));
#13812=CARTESIAN_POINT('Ctrl Pts',(-31.8420962738445,-1.40284585266758,
313.248014988445));
#13813=CARTESIAN_POINT('Ctrl Pts',(-31.797369184335,-1.33733532934864,313.253328869578));
#13814=CARTESIAN_POINT('Ctrl Pts',(-31.7526706448738,-1.27186662249119,
313.258639358773));
#13815=CARTESIAN_POINT('Ctrl Pts',(-31.7112245768274,-1.20410554679715,
313.263949847968));
#13816=CARTESIAN_POINT('Ctrl Pts',(-31.6732662206456,-1.13441127070882,
313.269260337162));
#13817=CARTESIAN_POINT('Ctrl Pts',(-31.635320218597,-1.06473967769885,313.274569097976));
#13818=CARTESIAN_POINT('Ctrl Pts',(-31.6008598989647,-0.993136545736397,
313.27987785879));
#13819=CARTESIAN_POINT('Ctrl Pts',(-31.570075395045,-0.919987137162623,
313.285186619604));
#13820=CARTESIAN_POINT('Ctrl Pts',(-31.5392912796118,-0.846838651701281,
313.290495313423));
#13821=CARTESIAN_POINT('Ctrl Pts',(-31.512183068623,-0.772144361806512,
313.295804007243));
#13822=CARTESIAN_POINT('Ctrl Pts',(-31.4888928321102,-0.696309683921922,
313.301112701063));
#13823=CARTESIAN_POINT('Ctrl Pts',(-31.4655791217774,-0.620398573598213,
313.306426745422));
#13824=CARTESIAN_POINT('Ctrl Pts',(-31.4460912110809,-0.543345229299718,
313.311740789781));
#13825=CARTESIAN_POINT('Ctrl Pts',(-31.4305211288046,-0.465569841036638,
313.31705483414));
#13826=CARTESIAN_POINT('Ctrl Pts',(-31.4149435268195,-0.387756890463096,
313.322371444963));
#13827=CARTESIAN_POINT('Ctrl Pts',(-31.4032875914132,-0.309221666466385,
313.327688055787));
#13828=CARTESIAN_POINT('Ctrl Pts',(-31.3955936577933,-0.230391587493498,
313.33300466661));
#13829=CARTESIAN_POINT('Ctrl Pts',(-31.3878855610137,-0.151416396402887,
313.338331064366));
#13830=CARTESIAN_POINT('Ctrl Pts',(-31.3841540618197,-0.0721457361033145,
313.343657462122));
#13831=CARTESIAN_POINT('Ctrl Pts',(-31.3843873287825,0.00699104172302907,
313.348983859878));
#13832=CARTESIAN_POINT('Ctrl Pts',(-31.3846117168204,0.0831156076991083,
313.354107517027));
#13833=CARTESIAN_POINT('Ctrl Pts',(-31.3885044163401,0.159115927399626,
313.359231174175));
#13834=CARTESIAN_POINT('Ctrl Pts',(-31.3960098112352,0.234616279433132,
313.364354831323));
#13835=CARTESIAN_POINT('Ctrl Pts',(-31.4038328626931,0.313312090553255,
313.369695340927));
#13836=CARTESIAN_POINT('Ctrl Pts',(-31.4156108517525,0.391763030641342,
313.375035850532));
#13837=CARTESIAN_POINT('Ctrl Pts',(-31.4313196407786,0.469540932796829,
313.380376360136));
#13838=CARTESIAN_POINT('Ctrl Pts',(-31.4470056964146,0.547206276601627,
313.385709141081));
#13839=CARTESIAN_POINT('Ctrl Pts',(-31.4666111625597,0.624200062725887,
313.391041922025));
#13840=CARTESIAN_POINT('Ctrl Pts',(-31.4900601455345,0.700099249479816,
313.39637470297));
#13841=CARTESIAN_POINT('Ctrl Pts',(-31.513481539297,0.775909136037327,313.40170120956));
#13842=CARTESIAN_POINT('Ctrl Pts',(-31.5407373250942,0.850626538719343,
313.40702771615));
#13843=CARTESIAN_POINT('Ctrl Pts',(-31.571700895418,0.923840108338071,313.412354222741));
#13844=CARTESIAN_POINT('Ctrl Pts',(-31.6026444800451,0.997006421642888,
313.417677291292));
#13845=CARTESIAN_POINT('Ctrl Pts',(-31.6372909170154,1.06867039958483,313.423000359844));
#13846=CARTESIAN_POINT('Ctrl Pts',(-31.6754646407872,1.13843844996113,313.428323428396));
#13847=CARTESIAN_POINT('Ctrl Pts',(-31.7136255167986,1.20818301918062,313.433644705414));
#13848=CARTESIAN_POINT('Ctrl Pts',(-31.7553110979245,1.27603251853521,313.438965982433));
#13849=CARTESIAN_POINT('Ctrl Pts',(-31.8002994718418,1.34161717483033,313.444287259451));
#13850=CARTESIAN_POINT('Ctrl Pts',(-31.8452866008212,1.40720001623811,313.449608389216));
#13851=CARTESIAN_POINT('Ctrl Pts',(-31.8935760755625,1.47051775466638,313.454929518982));
#13852=CARTESIAN_POINT('Ctrl Pts',(-31.9449030141891,1.53123010819042,313.460250648747));
#13853=CARTESIAN_POINT('Ctrl Pts',(-31.9962791591546,1.59200066570493,313.465576879797));
#13854=CARTESIAN_POINT('Ctrl Pts',(-32.0506982828648,1.65016049104283,313.470903110847));
#13855=CARTESIAN_POINT('Ctrl Pts',(-32.1078559892727,1.70540337000759,313.476229341897));
#13856=CARTESIAN_POINT('Ctrl Pts',(-32.165040217359,1.76067188215399,313.481558044365));
#13857=CARTESIAN_POINT('Ctrl Pts',(-32.2249652078903,1.8130204431315,313.486886746833));
#13858=CARTESIAN_POINT('Ctrl Pts',(-32.2872924442793,1.86218233162658,313.492215449301));
#13859=CARTESIAN_POINT('Ctrl Pts',(-32.3497294374532,1.91143079304122,313.497553535488));
#13860=CARTESIAN_POINT('Ctrl Pts',(-32.4145767478216,1.95748109725601,313.502891621675));
#13861=CARTESIAN_POINT('Ctrl Pts',(-32.4814659584981,2.00010930386008,313.508229707861));
#13862=CARTESIAN_POINT('Ctrl Pts',(-32.5426834513249,2.0391229490445,313.513115163222));
#13863=CARTESIAN_POINT('Ctrl Pts',(-32.6056106806806,2.07527063509553,313.518000618582));
#13864=CARTESIAN_POINT('Ctrl Pts',(-32.6699490794746,2.10841540797695,313.522886073942));
#13865=CARTESIAN_POINT('Ctrl Pts',(-32.6699490794746,2.10841540797695,312.522795280203));
#13866=CARTESIAN_POINT('Ctrl Pts',(-32.7405450600518,2.14478385646856,312.528116002019));
#13867=CARTESIAN_POINT('Ctrl Pts',(-32.8129152355776,2.17757481367262,312.533436723835));
#13868=CARTESIAN_POINT('Ctrl Pts',(-32.8866592463607,2.20663178712718,312.538757445651));
#13869=CARTESIAN_POINT('Ctrl Pts',(-32.9605374302371,2.2357416281159,312.544087848221));
#13870=CARTESIAN_POINT('Ctrl Pts',(-33.035793998677,2.26110375999759,312.549418250792));
#13871=CARTESIAN_POINT('Ctrl Pts',(-33.1120124034452,2.28261131524128,312.554748653363));
#13872=CARTESIAN_POINT('Ctrl Pts',(-33.1837434103354,2.30285260208094,312.559765225734));
#13873=CARTESIAN_POINT('Ctrl Pts',(-33.2563258906175,2.31968023219454,312.564781798105));
#13874=CARTESIAN_POINT('Ctrl Pts',(-33.3294068249702,2.33304692048117,312.569798370476));
#13875=CARTESIAN_POINT('Ctrl Pts',(-33.4070818752241,2.34725388422061,312.575130301635));
#13876=CARTESIAN_POINT('Ctrl Pts',(-33.4856143465868,2.35760442458897,312.580462232795));
#13877=CARTESIAN_POINT('Ctrl Pts',(-33.5645872962858,2.36400308686884,312.585794163954));
#13878=CARTESIAN_POINT('Ctrl Pts',(-33.6434460292288,2.37039249491102,312.591118383664));
#13879=CARTESIAN_POINT('Ctrl Pts',(-33.7227435120484,2.37284133753259,312.596442603375));
#13880=CARTESIAN_POINT('Ctrl Pts',(-33.8020533484656,2.37130530200913,312.601766823085));
#13881=CARTESIAN_POINT('Ctrl Pts',(-33.8812707909413,2.36977105592796,312.607084840215));
#13882=CARTESIAN_POINT('Ctrl Pts',(-33.9605000921013,2.36426116596706,312.612402857344));
#13883=CARTESIAN_POINT('Ctrl Pts',(-34.0393120115705,2.35478328642509,312.617720874474));
#13884=CARTESIAN_POINT('Ctrl Pts',(-34.1180736509638,2.34531145353833,312.623035498839));
#13885=CARTESIAN_POINT('Ctrl Pts',(-34.1964179729635,2.33187671144784,312.628350123204));
#13886=CARTESIAN_POINT('Ctrl Pts',(-34.2739192380045,2.31453867691137,312.633664747569));
#13887=CARTESIAN_POINT('Ctrl Pts',(-34.351395205256,2.29720630181735,312.638977637146));
#13888=CARTESIAN_POINT('Ctrl Pts',(-34.4280282048192,2.27597326655007,312.644290526723));
#13889=CARTESIAN_POINT('Ctrl Pts',(-34.5034025678486,2.25095031618765,312.6496034163));
#13890=CARTESIAN_POINT('Ctrl Pts',(-34.5787758103104,2.22592773783379,312.654916226893));
#13891=CARTESIAN_POINT('Ctrl Pts',(-34.6528900089037,2.19711550536241,312.660229037485));
#13892=CARTESIAN_POINT('Ctrl Pts',(-34.725345971637,2.16467380833216,312.665541848077));
#13893=CARTESIAN_POINT('Ctrl Pts',(-34.7978742542544,2.13219973053319,312.670859961501));
#13894=CARTESIAN_POINT('Ctrl Pts',(-34.8687405657672,2.09608914348932,312.676178074926));
#13895=CARTESIAN_POINT('Ctrl Pts',(-34.9375675389942,2.056549628626,312.681496188351));
#13896=CARTESIAN_POINT('Ctrl Pts',(-35.0064274781194,2.01699117561153,312.68681684898));
#13897=CARTESIAN_POINT('Ctrl Pts',(-35.0732457382495,1.97400077698668,312.69213750961));
#13898=CARTESIAN_POINT('Ctrl Pts',(-35.1376735281126,1.92782969241295,312.697458170239));
#13899=CARTESIAN_POINT('Ctrl Pts',(-35.2022188459847,1.88157438338188,312.702788536721));
#13900=CARTESIAN_POINT('Ctrl Pts',(-35.2643646120948,1.83212708694795,312.708118903203));
#13901=CARTESIAN_POINT('Ctrl Pts',(-35.3237949104075,1.77977961117932,312.713449269686));
#13902=CARTESIAN_POINT('Ctrl Pts',(-35.3805095665181,1.72982413104941,312.718536067339));
#13903=CARTESIAN_POINT('Ctrl Pts',(-35.4347512701437,1.67722800610831,312.723622864992));
#13904=CARTESIAN_POINT('Ctrl Pts',(-35.486279014651,1.62227376114459,312.728709662645));
#13905=CARTESIAN_POINT('Ctrl Pts',(-35.5396271593962,1.56537806266751,312.733976169458));
#13906=CARTESIAN_POINT('Ctrl Pts',(-35.5902789241322,1.50572711898534,312.739242676271));
#13907=CARTESIAN_POINT('Ctrl Pts',(-35.6379314395801,1.44361013044951,312.744509183083));
#13908=CARTESIAN_POINT('Ctrl Pts',(-35.6855211242083,1.38157504443795,312.749768745899));
#13909=CARTESIAN_POINT('Ctrl Pts',(-35.7301191118534,1.31708073912948,312.755028308714));
#13910=CARTESIAN_POINT('Ctrl Pts',(-35.7714598544099,1.25045257816565,312.76028787153));
#13911=CARTESIAN_POINT('Ctrl Pts',(-35.8127597196738,1.18389029842842,312.765542233744));
#13912=CARTESIAN_POINT('Ctrl Pts',(-35.8508084769252,1.1151987550711,312.770796595959));
#13913=CARTESIAN_POINT('Ctrl Pts',(-35.8853823420327,1.04473434828417,312.776050958174));
#13914=CARTESIAN_POINT('Ctrl Pts',(-35.9199334147536,0.974316394273128,
312.781301856517));
#13915=CARTESIAN_POINT('Ctrl Pts',(-35.9510139310135,0.902128327428168,
312.786552754859));
#13916=CARTESIAN_POINT('Ctrl Pts',(-35.9784455896821,0.828551905866046,
312.791803653202));
#13917=CARTESIAN_POINT('Ctrl Pts',(-36.0058765309656,0.75497740845396,312.797054414224));
#13918=CARTESIAN_POINT('Ctrl Pts',(-36.0296586205228,0.680015073258473,
312.802305175247));
#13919=CARTESIAN_POINT('Ctrl Pts',(-36.0496618558139,0.604066257562219,
312.807555936269));
#13920=CARTESIAN_POINT('Ctrl Pts',(-36.069664292838,0.528120472747102,312.81280648775));
#13921=CARTESIAN_POINT('Ctrl Pts',(-36.0858880609003,0.451188753325259,
312.818057039231));
#13922=CARTESIAN_POINT('Ctrl Pts',(-36.0982537172768,0.373685189740282,
312.823307590712));
#13923=CARTESIAN_POINT('Ctrl Pts',(-36.1106293976277,0.296118799427103,
312.828562398448));
#13924=CARTESIAN_POINT('Ctrl Pts',(-36.1191406563015,0.217980116654933,
312.833817206185));
#13925=CARTESIAN_POINT('Ctrl Pts',(-36.1237597639975,0.139689931444203,
312.839072013921));
#13926=CARTESIAN_POINT('Ctrl Pts',(-36.1265485817589,0.0924216983950322,
312.842244639916));
#13927=CARTESIAN_POINT('Ctrl Pts',(-36.1279196333306,0.0450983169026677,
312.84541726591));
#13928=CARTESIAN_POINT('Ctrl Pts',(-36.1278760162707,-0.00218772220706814,
312.848589891905));
#13929=CARTESIAN_POINT('',(-36.1278769078432,0.000746294306655331,312.651410108059));
#13930=CARTESIAN_POINT('Ctrl Pts',(-32.6699490794746,2.10841540797695,312.325750055738));
#13931=CARTESIAN_POINT('Ctrl Pts',(-32.7405208763421,2.1447713979122,312.331062992539));
#13932=CARTESIAN_POINT('Ctrl Pts',(-32.812948244602,2.1775948627673,312.33637592934));
#13933=CARTESIAN_POINT('Ctrl Pts',(-32.8868415286018,2.20670360216407,312.341688866141));
#13934=CARTESIAN_POINT('Ctrl Pts',(-32.9607315335957,2.2358110498639,312.347001567181));
#13935=CARTESIAN_POINT('Ctrl Pts',(-33.0360868884612,2.26120392885337,312.352314268221));
#13936=CARTESIAN_POINT('Ctrl Pts',(-33.1124987676385,2.28274850311949,312.357626969261));
#13937=CARTESIAN_POINT('Ctrl Pts',(-33.1900122585412,2.30460368034269,312.363016262237));
#13938=CARTESIAN_POINT('Ctrl Pts',(-33.2686125083594,2.32249855389248,312.368405555214));
#13939=CARTESIAN_POINT('Ctrl Pts',(-33.3478596159751,2.33634667483612,312.37379484819));
#13940=CARTESIAN_POINT('Ctrl Pts',(-33.4260929774439,2.3500176476204,312.379115200164));
#13941=CARTESIAN_POINT('Ctrl Pts',(-33.5049562627513,2.3597448119232,312.384435552138));
#13942=CARTESIAN_POINT('Ctrl Pts',(-33.5840206401277,2.3654972954323,312.389755904112));
#13943=CARTESIAN_POINT('Ctrl Pts',(-33.6646217891527,2.37136158977024,312.395179667589));
#13944=CARTESIAN_POINT('Ctrl Pts',(-33.7454314176383,2.37309504518618,312.400603431066));
#13945=CARTESIAN_POINT('Ctrl Pts',(-33.8259968514571,2.37072062248736,312.406027194543));
#13946=CARTESIAN_POINT('Ctrl Pts',(-33.9065622852758,2.36834619978854,312.41145095802));
#13947=CARTESIAN_POINT('Ctrl Pts',(-33.9868830226482,2.36186400685828,312.416874721497));
#13948=CARTESIAN_POINT('Ctrl Pts',(-34.0665156523982,2.35135215623729,312.422298484974));
#13949=CARTESIAN_POINT('Ctrl Pts',(-34.144799397919,2.34101836415295,312.427630376199));
#13950=CARTESIAN_POINT('Ctrl Pts',(-34.2227148445178,2.32675126035608,312.432962267424));
#13951=CARTESIAN_POINT('Ctrl Pts',(-34.2998358892453,2.30858803897994,312.438294158649));
#13952=CARTESIAN_POINT('Ctrl Pts',(-34.3768453811961,2.29045109004065,312.443618337488));
#13953=CARTESIAN_POINT('Ctrl Pts',(-34.4530623006692,2.26842932159174,312.448942516327));
#13954=CARTESIAN_POINT('Ctrl Pts',(-34.5280672528151,2.24261150170475,312.454266695166));
#13955=CARTESIAN_POINT('Ctrl Pts',(-34.6029848084572,2.21682376499404,312.45958467022));
#13956=CARTESIAN_POINT('Ctrl Pts',(-34.6766927621011,2.18724891850967,312.464902645273));
#13957=CARTESIAN_POINT('Ctrl Pts',(-34.748784970606,2.15402605973946,312.470220620327));
#13958=CARTESIAN_POINT('Ctrl Pts',(-34.8208311760328,2.12082440095462,312.475535201904));
#13959=CARTESIAN_POINT('Ctrl Pts',(-34.8912632580845,2.08397954595495,312.480849783481));
#13960=CARTESIAN_POINT('Ctrl Pts',(-34.9596943622761,2.0436789688604,312.486164365058));
#13961=CARTESIAN_POINT('Ctrl Pts',(-35.0281031208306,2.00339155160127,312.491477211201));
#13962=CARTESIAN_POINT('Ctrl Pts',(-35.0945117953117,1.95965089073064,312.496790057343));
#13963=CARTESIAN_POINT('Ctrl Pts',(-35.1585588163074,1.91269002557991,312.502102903486));
#13964=CARTESIAN_POINT('Ctrl Pts',(-35.2226048781042,1.86572986373761,312.507415670061));
#13965=CARTESIAN_POINT('Ctrl Pts',(-35.2842889794171,1.8155498717802,312.512728436635));
#13966=CARTESIAN_POINT('Ctrl Pts',(-35.3432804155137,1.76242508445002,312.51804120321));
#13967=CARTESIAN_POINT('Ctrl Pts',(-35.40233072613,1.70924727762161,312.523359272022));
#13968=CARTESIAN_POINT('Ctrl Pts',(-35.458682654007,1.65311911893993,312.528677340834));
#13969=CARTESIAN_POINT('Ctrl Pts',(-35.5120408184047,1.59435404271937,312.533995409645));
#13970=CARTESIAN_POINT('Ctrl Pts',(-35.5654245358643,1.53556082408343,312.539316025264));
#13971=CARTESIAN_POINT('Ctrl Pts',(-35.6158113359467,1.47412853518857,312.544636640883));
#13972=CARTESIAN_POINT('Ctrl Pts',(-35.6629464464039,1.4104034024489,312.549957256502));
#13973=CARTESIAN_POINT('Ctrl Pts',(-35.7101675394602,1.34656202403813,312.555287577844));
#13974=CARTESIAN_POINT('Ctrl Pts',(-35.7541248298147,1.28041983552675,312.560617899187));
#13975=CARTESIAN_POINT('Ctrl Pts',(-35.7946072841821,1.2123515564699,312.565948220529));
#13976=CARTESIAN_POINT('Ctrl Pts',(-35.8332431830649,1.14738812508074,312.571035406067));
#13977=CARTESIAN_POINT('Ctrl Pts',(-35.8687142033516,1.08067082032187,312.576122591605));
#13978=CARTESIAN_POINT('Ctrl Pts',(-35.9008777155876,1.01254261087078,312.581209777143));
#13979=CARTESIAN_POINT('Ctrl Pts',(-35.9378642638722,0.934198327761406,
312.587059804719));
#13980=CARTESIAN_POINT('Ctrl Pts',(-35.9706015859964,0.853724764581502,
312.592909832296));
#13981=CARTESIAN_POINT('Ctrl Pts',(-35.9988607118803,0.771585169237672,
312.598759859872));
#13982=CARTESIAN_POINT('Ctrl Pts',(-36.0266549611423,0.690796810933859,
312.604513651597));
#13983=CARTESIAN_POINT('Ctrl Pts',(-36.0501170642415,0.608397144709793,
312.610267443321));
#13984=CARTESIAN_POINT('Ctrl Pts',(-36.0690751867648,0.524851278630692,
312.616021235045));
#13985=CARTESIAN_POINT('Ctrl Pts',(-36.0885089394018,0.439209375365859,
312.621919380548));
#13986=CARTESIAN_POINT('Ctrl Pts',(-36.103209476303,0.352363287906919,312.62781752605));
#13987=CARTESIAN_POINT('Ctrl Pts',(-36.1130445591917,0.26483542197729,312.633715671552));
#13988=CARTESIAN_POINT('Ctrl Pts',(-36.1228796420805,0.177307556047662,
312.639613817055));
#13989=CARTESIAN_POINT('Ctrl Pts',(-36.1278491070246,0.0890982858603586,
312.645511962557));
#13990=CARTESIAN_POINT('Ctrl Pts',(-36.1278769078432,0.000746294306655331,
312.651410108059));
#13991=CARTESIAN_POINT('Ctrl Pts',(-32.6699490794749,2.10841540797709,313.324578124683));
#13992=CARTESIAN_POINT('Ctrl Pts',(-32.6586890743879,2.10261466816627,313.323667641728));
#13993=CARTESIAN_POINT('Ctrl Pts',(-32.64747558103,2.09672374956396,313.322759165335));
#13994=CARTESIAN_POINT('Ctrl Pts',(-32.5641501948446,2.05209406353605,313.315996031982));
#13995=CARTESIAN_POINT('Ctrl Pts',(-32.4940336030402,2.00973173904113,313.310238156099));
#13996=CARTESIAN_POINT('Ctrl Pts',(-32.4000804743237,1.94610740862244,313.302435513491));
#13997=CARTESIAN_POINT('Ctrl Pts',(-32.3742753537587,1.92786991792475,313.300282354887));
#13998=CARTESIAN_POINT('Ctrl Pts',(-32.3308335463775,1.89584731471528,313.296638242202));
#13999=CARTESIAN_POINT('Ctrl Pts',(-32.3130140708035,1.88231867700841,313.295137674329));
#14000=CARTESIAN_POINT('Ctrl Pts',(-32.2767628222872,1.85397910602036,313.292071651396));
#14001=CARTESIAN_POINT('Ctrl Pts',(-32.2583557110656,1.83914059527149,313.290507520255));
#14002=CARTESIAN_POINT('Ctrl Pts',(-32.2115654420805,1.80025310881025,313.286509959624));
#14003=CARTESIAN_POINT('Ctrl Pts',(-32.1835200342395,1.775806644272,313.284092927292));
#14004=CARTESIAN_POINT('Ctrl Pts',(-32.1230854388463,1.72057223386636,313.278826282586));
#14005=CARTESIAN_POINT('Ctrl Pts',(-32.0909675731802,1.68950820967722,313.275988443552));
#14006=CARTESIAN_POINT('Ctrl Pts',(-31.9906577164792,1.5868485972456,313.266959944821));
#14007=CARTESIAN_POINT('Ctrl Pts',(-31.9260557342601,1.51188991338232,313.260890162012));
#14008=CARTESIAN_POINT('Ctrl Pts',(-31.7779476675745,1.31658400306205,313.245867885478));
#14009=CARTESIAN_POINT('Ctrl Pts',(-31.7005563976988,1.19214319748892,313.236966747008));
#14010=CARTESIAN_POINT('Ctrl Pts',(-31.6237939728056,1.03874678103291,313.225836437172));
#14011=CARTESIAN_POINT('Ctrl Pts',(-31.6128271783569,1.01592556875727,313.224176310468));
#14012=CARTESIAN_POINT('Ctrl Pts',(-31.5963208983471,0.980119721610386,
313.221558303073));
#14013=CARTESIAN_POINT('Ctrl Pts',(-31.5905281116862,0.967253066444005,
313.220614897917));
#14014=CARTESIAN_POINT('Ctrl Pts',(-31.5796868526516,0.942587359769649,
313.218799911641));
#14015=CARTESIAN_POINT('Ctrl Pts',(-31.5746187869785,0.930797791944203,
313.217929491182));
#14016=CARTESIAN_POINT('Ctrl Pts',(-31.5622502811555,0.901369685125223,
313.215750462696));
#14017=CARTESIAN_POINT('Ctrl Pts',(-31.5550667574463,0.883683266699383,
313.214435278246));
#14018=CARTESIAN_POINT('Ctrl Pts',(-31.5267975709807,0.811598421728999,
313.209057933878));
#14019=CARTESIAN_POINT('Ctrl Pts',(-31.5075104808776,0.756521156086602,
313.204910681697));
#14020=CARTESIAN_POINT('Ctrl Pts',(-31.4549511171713,0.586582893429965,
313.192106923249));
#14021=CARTESIAN_POINT('Ctrl Pts',(-31.4283136954704,0.46986656769488,313.183311939748));
#14022=CARTESIAN_POINT('Ctrl Pts',(-31.3914779407305,0.224162454293398,
313.165246867116));
#14023=CARTESIAN_POINT('Ctrl Pts',(-31.3827881848785,0.0953216489531737,
313.156026874364));
#14024=CARTESIAN_POINT('Ctrl Pts',(-31.3851067672275,-0.0683014395058179,
313.144730280878));
#14025=CARTESIAN_POINT('Ctrl Pts',(-31.3863598271791,-0.102984465040225,
313.142358043477));
#14026=CARTESIAN_POINT('Ctrl Pts',(-31.3897163209358,-0.160729126179656,
313.138443483193));
#14027=CARTESIAN_POINT('Ctrl Pts',(-31.3913970544757,-0.18380888131378,
313.136888218864));
#14028=CARTESIAN_POINT('Ctrl Pts',(-31.3954169147684,-0.229722647026887,
313.133811526557));
#14029=CARTESIAN_POINT('Ctrl Pts',(-31.3977502638263,-0.252554616421627,
313.132290091853));
#14030=CARTESIAN_POINT('Ctrl Pts',(-31.4043259979175,-0.308812280624378,
313.128560253025));
#14031=CARTESIAN_POINT('Ctrl Pts',(-31.4089499869474,-0.342188886350895,
313.126364032423));
#14032=CARTESIAN_POINT('Ctrl Pts',(-31.4323680839719,-0.488254890763436,
313.116810055559));
#14033=CARTESIAN_POINT('Ctrl Pts',(-31.4585791967774,-0.599605620174556,
313.109686669187));
#14034=CARTESIAN_POINT('Ctrl Pts',(-31.5374058476634,-0.85137789562294,
313.093441540655));
#14035=CARTESIAN_POINT('Ctrl Pts',(-31.5954912572841,-0.989552596102437,
313.08442514723));
#14036=CARTESIAN_POINT('Ctrl Pts',(-31.688513148751,-1.16292721019981,313.071968754634));
#14037=CARTESIAN_POINT('Ctrl Pts',(-31.7120687128626,-1.2038487342366,313.068936080935));
#14038=CARTESIAN_POINT('Ctrl Pts',(-31.7463994266074,-1.25957375859849,
313.064637241868));
#14039=CARTESIAN_POINT('Ctrl Pts',(-31.7561498619814,-1.27499896823074,
313.063428715757));
#14040=CARTESIAN_POINT('Ctrl Pts',(-31.7729835603744,-1.30096165563062,
313.061360132739));
#14041=CARTESIAN_POINT('Ctrl Pts',(-31.7799751384848,-1.3115574500516,313.060505952081));
#14042=CARTESIAN_POINT('Ctrl Pts',(-31.7951161363673,-1.33410780992833,
313.058665781108));
#14043=CARTESIAN_POINT('Ctrl Pts',(-31.8032899797416,-1.34604413039435,
313.057678329311));
#14044=CARTESIAN_POINT('Ctrl Pts',(-31.8270767350198,-1.38010738589654,
313.05482334377));
#14045=CARTESIAN_POINT('Ctrl Pts',(-31.8429595640473,-1.40204191412584,
313.052939436539));
#14046=CARTESIAN_POINT('Ctrl Pts',(-31.9206918008067,-1.50561112080414,
313.043842121119));
#14047=CARTESIAN_POINT('Ctrl Pts',(-31.9874059696796,-1.58344859361498,
313.036397732682));
#14048=CARTESIAN_POINT('Ctrl Pts',(-32.1876948424848,-1.78862993823934,
313.01546527657));
#14049=CARTESIAN_POINT('Ctrl Pts',(-32.3314196618491,-1.90510089161966,
313.002029900501));
#14050=CARTESIAN_POINT('Ctrl Pts',(-32.5186387929183,-2.02366132015657,
312.986688797455));
#14051=CARTESIAN_POINT('Ctrl Pts',(-32.5505365166754,-2.04282502010893,
312.984139608101));
#14052=CARTESIAN_POINT('Ctrl Pts',(-32.6034157070038,-2.07292387120959,
312.98001538703));
#14053=CARTESIAN_POINT('Ctrl Pts',(-32.624132116142,-2.08430908342133,312.978424385611));
#14054=CARTESIAN_POINT('Ctrl Pts',(-32.664996126768,-2.10597789239471,312.975332731625));
#14055=CARTESIAN_POINT('Ctrl Pts',(-32.6851273992073,-2.11628669659473,
312.973831309742));
#14056=CARTESIAN_POINT('Ctrl Pts',(-32.7338717369575,-2.14037392016344,
312.970245593641));
#14057=CARTESIAN_POINT('Ctrl Pts',(-32.7626205123395,-2.15386892794943,
312.968171289395));
#14058=CARTESIAN_POINT('Ctrl Pts',(-32.8738900317796,-2.20339802535053,
312.960285482809));
#14059=CARTESIAN_POINT('Ctrl Pts',(-32.9581707669326,-2.23530163228674,
312.954612079052));
#14060=CARTESIAN_POINT('Ctrl Pts',(-33.2404921192669,-2.32416064156935,
312.936239573021));
#14061=CARTESIAN_POINT('Ctrl Pts',(-33.4440992494008,-2.36013097937297,
312.924032558544));
#14062=CARTESIAN_POINT('Ctrl Pts',(-33.6783814193257,-2.37064854638675,
312.90888509538));
#14063=CARTESIAN_POINT('Ctrl Pts',(-33.7070224163962,-2.37141465570959,
312.907013524308));
#14064=CARTESIAN_POINT('Ctrl Pts',(-33.7504479594286,-2.37178925161856,
312.904136335765));
#14065=CARTESIAN_POINT('Ctrl Pts',(-33.7652276194867,-2.37177858497555,
312.903150162358));
#14066=CARTESIAN_POINT('Ctrl Pts',(-33.7926274681729,-2.37150271026286,
312.901307439557));
#14067=CARTESIAN_POINT('Ctrl Pts',(-33.805247108981,-2.37127488386425,312.900452899957));
#14068=CARTESIAN_POINT('Ctrl Pts',(-33.8355317541939,-2.37048630267468,
312.898388638559));
#14069=CARTESIAN_POINT('Ctrl Pts',(-33.8531931023898,-2.36982880204653,
312.897173867065));
#14070=CARTESIAN_POINT('Ctrl Pts',(-33.9171279475226,-2.36673275251141,
312.892740617524));
#14071=CARTESIAN_POINT('Ctrl Pts',(-33.9633320795099,-2.36313576121074,
312.889469112301));
#14072=CARTESIAN_POINT('Ctrl Pts',(-34.0879321045611,-2.34975366435724,
312.880512707947));
#14073=CARTESIAN_POINT('Ctrl Pts',(-34.1659924381588,-2.33740154073621,
312.874758580285));
#14074=CARTESIAN_POINT('Ctrl Pts',(-34.4173974806705,-2.28463767752996,
312.85599965948));
#14075=CARTESIAN_POINT('Ctrl Pts',(-34.5868761986164,-2.22861509838322,
312.843049912591));
#14076=CARTESIAN_POINT('Ctrl Pts',(-34.7830805105049,-2.13822662378613,
312.82808124603));
#14077=CARTESIAN_POINT('Ctrl Pts',(-34.8172611237326,-2.12147148762995,
312.825471632893));
#14078=CARTESIAN_POINT('Ctrl Pts',(-34.8721417230487,-2.09291087143466,
312.82127606372));
#14079=CARTESIAN_POINT('Ctrl Pts',(-34.8930919882881,-2.08160406088059,
312.819673048284));
#14080=CARTESIAN_POINT('Ctrl Pts',(-34.933526371461,-2.05898910203936,312.816575127921));
#14081=CARTESIAN_POINT('Ctrl Pts',(-34.9530265324101,-2.0477150612715,312.81507921302));
#14082=CARTESIAN_POINT('Ctrl Pts',(-34.999151587765,-2.02016375979472,312.811534373709));
#14083=CARTESIAN_POINT('Ctrl Pts',(-35.025622048016,-2.00363525033919,312.809494840846));
#14084=CARTESIAN_POINT('Ctrl Pts',(-35.1227875307324,-1.94026491931808,
312.801978451707));
#14085=CARTESIAN_POINT('Ctrl Pts',(-35.1912844645948,-1.89016249864544,
312.796622455246));
#14086=CARTESIAN_POINT('Ctrl Pts',(-35.3889896387542,-1.72859284842388,
312.780737267705));
#14087=CARTESIAN_POINT('Ctrl Pts',(-35.5089926288937,-1.60677619342329,
312.770525829199));
#14088=CARTESIAN_POINT('Ctrl Pts',(-35.6511765411855,-1.42737442731966,
312.756153350141));
#14089=CARTESIAN_POINT('Ctrl Pts',(-35.6857530430412,-1.38027267808487,
312.752428972949));
#14090=CARTESIAN_POINT('Ctrl Pts',(-35.7295581294675,-1.31573241103249,
312.747319462395));
#14091=CARTESIAN_POINT('Ctrl Pts',(-35.7403616777977,-1.29938250008593,
312.74602454274));
#14092=CARTESIAN_POINT('Ctrl Pts',(-35.7578834600322,-1.27213718797955,
312.743862490469));
#14093=CARTESIAN_POINT('Ctrl Pts',(-35.7647186044117,-1.26131744956902,
312.743002797603));
#14094=CARTESIAN_POINT('Ctrl Pts',(-35.778783017391,-1.23864983781866,312.741198372929));
#14095=CARTESIAN_POINT('Ctrl Pts',(-35.7859963560826,-1.22679303813002,
312.740252761793));
#14096=CARTESIAN_POINT('Ctrl Pts',(-35.8055102361105,-1.19407413592374,
312.737639971577));
#14097=CARTESIAN_POINT('Ctrl Pts',(-35.8175955757306,-1.17308647941892,
312.735960274613));
#14098=CARTESIAN_POINT('Ctrl Pts',(-35.8886373006526,-1.04522515852139,
312.725721445401));
#14099=CARTESIAN_POINT('Ctrl Pts',(-35.9395879214242,-0.934124607467737,
312.716810603119));
#14100=CARTESIAN_POINT('Ctrl Pts',(-35.9978169286636,-0.77600491013887,
312.70450224756));
#14101=CARTESIAN_POINT('Ctrl Pts',(-36.0125899120188,-0.731937566093798,
312.701108704179));
#14102=CARTESIAN_POINT('Ctrl Pts',(-36.0469688574708,-0.618422027908436,
312.692486011683));
#14103=CARTESIAN_POINT('Ctrl Pts',(-36.0647191292152,-0.548457765586274,
312.68728383032));
#14104=CARTESIAN_POINT('Ctrl Pts',(-36.0929210759187,-0.411332955030435,
312.677344522685));
#14105=CARTESIAN_POINT('Ctrl Pts',(-36.1037319952619,-0.344316284979759,
312.672602533189));
#14106=CARTESIAN_POINT('Ctrl Pts',(-36.115080144577,-0.247787789815633,
312.665937125438));
#14107=CARTESIAN_POINT('Ctrl Pts',(-36.1179645736235,-0.218591257846128,
312.663942234706));
#14108=CARTESIAN_POINT('Ctrl Pts',(-36.1220531485902,-0.16754160781995,
312.660489400263));
#14109=CARTESIAN_POINT('Ctrl Pts',(-36.1234978656349,-0.145711945608564,
312.659024092762));
#14110=CARTESIAN_POINT('Ctrl Pts',(-36.1257396777691,-0.102844534490654,
312.656167350096));
#14111=CARTESIAN_POINT('Ctrl Pts',(-36.1265591135728,-0.0818100484010116,
312.654775347735));
#14112=CARTESIAN_POINT('Ctrl Pts',(-36.1276227136054,-0.0403110232039128,
312.652046917201));
#14113=CARTESIAN_POINT('Ctrl Pts',(-36.1278822476091,-0.0198488686738843,
312.650710146788));
#14114=CARTESIAN_POINT('Ctrl Pts',(-36.1278769456495,0.000614508638078176,
312.64938106027));
#14115=CARTESIAN_POINT('Origin',(-33.7561270252576,0.,307.));
#14116=CARTESIAN_POINT('',(-36.6981270252576,-3.60291088309151E-16,294.));
#14117=CARTESIAN_POINT('Origin',(-33.7561270252576,0.,294.));
#14118=CARTESIAN_POINT('',(-32.4165951196292,2.61935455290104,304.));
#14119=CARTESIAN_POINT('',(-35.045048879311,2.64462557919708,304.));
#14120=CARTESIAN_POINT('Origin',(-33.7561270252576,0.,304.));
#14121=CARTESIAN_POINT('',(-36.6984067016598,0.0019070081496421,304.17782388291));
#14122=CARTESIAN_POINT('Ctrl Pts',(-35.045048879311,2.64462557919709,304.));
#14123=CARTESIAN_POINT('Ctrl Pts',(-35.9252411831751,2.21564269967566,304.052970430723));
#14124=CARTESIAN_POINT('Ctrl Pts',(-36.642667118141,1.20804330944867,304.11224505836));
#14125=CARTESIAN_POINT('Ctrl Pts',(-36.7013903832366,0.117973363423384,
304.171519685997));
#14126=CARTESIAN_POINT('Ctrl Pts',(-36.7004990485223,0.00190836428262659,
304.17782388291));
#14127=CARTESIAN_POINT('',(-36.6981267041397,0.00137457535740912,305.17782388288));
#14128=CARTESIAN_POINT('Ctrl Pts',(-36.6981264073127,0.00190682647975922,
304.17782388291));
#14129=CARTESIAN_POINT('Ctrl Pts',(-36.6981854606991,-0.0892053056498797,
304.182776755507));
#14130=CARTESIAN_POINT('Ctrl Pts',(-36.6940077850111,-0.180500285875559,
304.187729628104));
#14131=CARTESIAN_POINT('Ctrl Pts',(-36.6855688210284,-0.271541461274618,
304.192682500701));
#14132=CARTESIAN_POINT('Ctrl Pts',(-36.6771404656152,-0.362468189374255,
304.197629147072));
#14133=CARTESIAN_POINT('Ctrl Pts',(-36.6644614994644,-0.453141289439652,
304.202575793443));
#14134=CARTESIAN_POINT('Ctrl Pts',(-36.6475593849915,-0.543123290868441,
304.207522439814));
#14135=CARTESIAN_POINT('Ctrl Pts',(-36.6306729670744,-0.633021728343676,
304.212464492363));
#14136=CARTESIAN_POINT('Ctrl Pts',(-36.6095712754905,-0.722229889458937,
304.217406544912));
#14137=CARTESIAN_POINT('Ctrl Pts',(-36.5843335276798,-0.810315975195248,
304.222348597461));
#14138=CARTESIAN_POINT('Ctrl Pts',(-36.55910798703,-0.898359454871054,304.227288259606));
#14139=CARTESIAN_POINT('Ctrl Pts',(-36.5297504869776,-0.985281492292477,
304.23222792175));
#14140=CARTESIAN_POINT('Ctrl Pts',(-36.4963909571031,-1.07066221742735,
304.237167583894));
#14141=CARTESIAN_POINT('Ctrl Pts',(-36.4630374409516,-1.15602755097755,
304.242106355565));
#14142=CARTESIAN_POINT('Ctrl Pts',(-36.4256834960837,-1.23985169331863,
304.247045127237));
#14143=CARTESIAN_POINT('Ctrl Pts',(-36.384507891906,-1.32173296086493,304.251983898908));
#14144=CARTESIAN_POINT('Ctrl Pts',(-36.3433272170591,-1.40362431187755,
304.256923278776));
#14145=CARTESIAN_POINT('Ctrl Pts',(-36.2983241585483,-1.48357190095865,
304.261862658644));
#14146=CARTESIAN_POINT('Ctrl Pts',(-36.2497236632193,-1.56119819598473,
304.266802038513));
#14147=CARTESIAN_POINT('Ctrl Pts',(-36.2010727089338,-1.63890508570063,
304.27174654664));
#14148=CARTESIAN_POINT('Ctrl Pts',(-36.1488171115561,-1.71428548023768,
304.276691054768));
#14149=CARTESIAN_POINT('Ctrl Pts',(-36.0932250918958,-1.78699094203527,
304.281635562896));
#14150=CARTESIAN_POINT('Ctrl Pts',(-36.037600203778,-1.8597393905131,304.286582994435));
#14151=CARTESIAN_POINT('Ctrl Pts',(-35.9786352690852,-1.92980940885522,
304.291530425975));
#14152=CARTESIAN_POINT('Ctrl Pts',(-35.9166371470862,-1.99688758158193,
304.296477857514));
#14153=CARTESIAN_POINT('Ctrl Pts',(-35.854540124742,-2.06407275842786,304.301433181271));
#14154=CARTESIAN_POINT('Ctrl Pts',(-35.7894005919193,-2.1282562461531,304.306388505029));
#14155=CARTESIAN_POINT('Ctrl Pts',(-35.7215600172065,-2.18916357409825,
304.311343828786));
#14156=CARTESIAN_POINT('Ctrl Pts',(-35.6919943405294,-2.21570766475376,
304.31350341397));
#14157=CARTESIAN_POINT('Ctrl Pts',(-35.6619160432118,-2.2416300539507,304.315662999154));
#14158=CARTESIAN_POINT('Ctrl Pts',(-35.6313550759192,-2.2669106197669,304.317822584338));
#14159=CARTESIAN_POINT('Ctrl Pts',(-35.5598720168902,-2.32604265447061,
304.322873921677));
#14160=CARTESIAN_POINT('Ctrl Pts',(-35.4854586911232,-2.38189825448609,
304.327925259016));
#14161=CARTESIAN_POINT('Ctrl Pts',(-35.4084480715605,-2.43417319842788,
304.332976596355));
#14162=CARTESIAN_POINT('Ctrl Pts',(-35.3315455516945,-2.48637476410539,
304.338020843139));
#14163=CARTESIAN_POINT('Ctrl Pts',(-35.2520533470419,-2.53500541361462,
304.343065089923));
#14164=CARTESIAN_POINT('Ctrl Pts',(-35.170338012154,-2.5798006288358,304.348109336707));
#14165=CARTESIAN_POINT('Ctrl Pts',(-35.0887120906379,-2.62454682888449,
304.353148064049));
#14166=CARTESIAN_POINT('Ctrl Pts',(-35.004868261466,-2.66546572358029,304.35818679139));
#14167=CARTESIAN_POINT('Ctrl Pts',(-34.919201690894,-2.70233627110963,304.363225518731));
#14168=CARTESIAN_POINT('Ctrl Pts',(-34.8335998302158,-2.73917896776087,
304.368260439973));
#14169=CARTESIAN_POINT('Ctrl Pts',(-34.7461783720883,-2.77197922066161,
304.373295361214));
#14170=CARTESIAN_POINT('Ctrl Pts',(-34.6573557382733,-2.80056258755918,
304.378330282456));
#14171=CARTESIAN_POINT('Ctrl Pts',(-34.5685672970876,-2.82913495117493,
304.383363265484));
#14172=CARTESIAN_POINT('Ctrl Pts',(-34.4783791744485,-2.85349351759961,
304.388396248512));
#14173=CARTESIAN_POINT('Ctrl Pts',(-34.3872273957038,-2.8735128888562,304.393429231541));
#14174=CARTESIAN_POINT('Ctrl Pts',(-34.296085166436,-2.89353016279196,304.398461687291));
#14175=CARTESIAN_POINT('Ctrl Pts',(-34.2039799159809,-2.90920905013263,
304.403494143041));
#14176=CARTESIAN_POINT('Ctrl Pts',(-34.1113592482792,-2.92047497296709,
304.408526598791));
#14177=CARTESIAN_POINT('Ctrl Pts',(-34.0187223329283,-2.93174287208575,
304.413559937341));
#14178=CARTESIAN_POINT('Ctrl Pts',(-33.9255702621046,-2.9385962161771,304.418593275892));
#14179=CARTESIAN_POINT('Ctrl Pts',(-33.832356019879,-2.94101226457473,304.423626614443));
#14180=CARTESIAN_POINT('Ctrl Pts',(-33.7390420287663,-2.94343089839423,
304.428665339186));
#14181=CARTESIAN_POINT('Ctrl Pts',(-33.6456661785347,-2.94140274649516,
304.43370406393));
#14182=CARTESIAN_POINT('Ctrl Pts',(-33.5526813899142,-2.93495721833551,
304.438742788674));
#14183=CARTESIAN_POINT('Ctrl Pts',(-33.4596410362822,-2.92850783851526,
304.443784524414));
#14184=CARTESIAN_POINT('Ctrl Pts',(-33.3669926507445,-2.91763587886526,
304.448826260153));
#14185=CARTESIAN_POINT('Ctrl Pts',(-33.2751817983903,-2.90242238289909,
304.453867995893));
#14186=CARTESIAN_POINT('Ctrl Pts',(-33.1832243190797,-2.88718459014716,
304.45891778356));
#14187=CARTESIAN_POINT('Ctrl Pts',(-33.0921074774406,-2.86759151198321,
304.463967571227));
#14188=CARTESIAN_POINT('Ctrl Pts',(-33.002264267968,-2.84377477012013,304.469017358895));
#14189=CARTESIAN_POINT('Ctrl Pts',(-32.956501504991,-2.83164341462688,304.471589531433));
#14190=CARTESIAN_POINT('Ctrl Pts',(-32.9110689104682,-2.81841702045556,
304.47416170397));
#14191=CARTESIAN_POINT('Ctrl Pts',(-32.8660217096371,-2.80411778053349,
304.476733876508));
#14192=CARTESIAN_POINT('Ctrl Pts',(-32.7774092731068,-2.77598971782041,
304.481793602119));
#14193=CARTESIAN_POINT('Ctrl Pts',(-32.6899775587321,-2.74360836087013,
304.48685332773));
#14194=CARTESIAN_POINT('Ctrl Pts',(-32.6041635777236,-2.70709146789421,
304.491913053341));
#14195=CARTESIAN_POINT('Ctrl Pts',(-32.5184654773731,-2.67062388624883,
304.496965946448));
#14196=CARTESIAN_POINT('Ctrl Pts',(-32.4343811730132,-2.63003203869568,
304.502018839556));
#14197=CARTESIAN_POINT('Ctrl Pts',(-32.3523321918021,-2.58548333306629,
304.507071732663));
#14198=CARTESIAN_POINT('Ctrl Pts',(-32.270368876532,-2.54098113998017,304.512119350131));
#14199=CARTESIAN_POINT('Ctrl Pts',(-32.1904370472337,-2.49253051133187,
304.517166967599));
#14200=CARTESIAN_POINT('Ctrl Pts',(-32.1129369193408,-2.4403463434146,304.522214585067));
#14201=CARTESIAN_POINT('Ctrl Pts',(-32.0354902433746,-2.38819816697764,
304.527258721187));
#14202=CARTESIAN_POINT('Ctrl Pts',(-31.960472301415,-2.33232181619026,304.532302857307));
#14203=CARTESIAN_POINT('Ctrl Pts',(-31.8882565289755,-2.27297686066506,
304.537346993428));
#14204=CARTESIAN_POINT('Ctrl Pts',(-31.8160656728214,-2.2136523806648,304.542389389192));
#14205=CARTESIAN_POINT('Ctrl Pts',(-31.7466754070349,-2.15086195445824,
304.547431784957));
#14206=CARTESIAN_POINT('Ctrl Pts',(-31.6804272817949,-2.08490637079679,
304.552474180722));
#14207=CARTESIAN_POINT('Ctrl Pts',(-31.6141836406136,-2.01895525139302,
304.557516235187));
#14208=CARTESIAN_POINT('Ctrl Pts',(-31.5510820306443,-1.94983971306171,
304.562558289653));
#14209=CARTESIAN_POINT('Ctrl Pts',(-31.4914273986124,-1.87789765457896,
304.567600344119));
#14210=CARTESIAN_POINT('Ctrl Pts',(-31.4317602600743,-1.8059405135491,304.572643455645));
#14211=CARTESIAN_POINT('Ctrl Pts',(-31.3755418171684,-1.7311560163198,304.57768656717));
#14212=CARTESIAN_POINT('Ctrl Pts',(-31.3230362369419,-1.65391451284924,
304.582729678695));
#14213=CARTESIAN_POINT('Ctrl Pts',(-31.2704724489103,-1.57658737927302,
304.587778381025));
#14214=CARTESIAN_POINT('Ctrl Pts',(-31.221629989032,-1.49679816901213,304.592827083355));
#14215=CARTESIAN_POINT('Ctrl Pts',(-31.1767290702231,-1.41494529560819,
304.597875785685));
#14216=CARTESIAN_POINT('Ctrl Pts',(-31.1318002081743,-1.33304148261251,
304.60292762998));
#14217=CARTESIAN_POINT('Ctrl Pts',(-31.0908179649267,-1.24907184707223,
304.607979474275));
#14218=CARTESIAN_POINT('Ctrl Pts',(-31.0539551055439,-1.16345645226235,
304.613031318569));
#14219=CARTESIAN_POINT('Ctrl Pts',(-31.0170327261524,-1.07770281996536,
304.618091319741));
#14220=CARTESIAN_POINT('Ctrl Pts',(-30.9842431645956,-0.990298537332545,
304.623151320913));
#14221=CARTESIAN_POINT('Ctrl Pts',(-30.9557098242559,-0.901680375927937,
304.628211322085));
#14222=CARTESIAN_POINT('Ctrl Pts',(-30.9417366736823,-0.858282901320502,
304.630689270949));
#14223=CARTESIAN_POINT('Ctrl Pts',(-30.9287834717208,-0.814594498065602,
304.633167219813));
#14224=CARTESIAN_POINT('Ctrl Pts',(-30.9168602232918,-0.770667261050437,
304.635645168677));
#14225=CARTESIAN_POINT('Ctrl Pts',(-30.8925677055117,-0.681169571508969,
304.640693760694));
#14226=CARTESIAN_POINT('Ctrl Pts',(-30.8724667729455,-0.590359276240205,
304.645742352711));
#14227=CARTESIAN_POINT('Ctrl Pts',(-30.8566965402011,-0.498665080314254,
304.650790944728));
#14228=CARTESIAN_POINT('Ctrl Pts',(-30.8409482211076,-0.40709829877985,
304.655832521434));
#14229=CARTESIAN_POINT('Ctrl Pts',(-30.8295187190975,-0.314650491811056,
304.66087409814));
#14230=CARTESIAN_POINT('Ctrl Pts',(-30.8224971057688,-0.221764504553785,
304.665915674846));
#14231=CARTESIAN_POINT('Ctrl Pts',(-30.8154830707788,-0.128978767971246,
304.670951810242));
#14232=CARTESIAN_POINT('Ctrl Pts',(-30.8128675022509,-0.0357562323716657,
304.675987945638));
#14233=CARTESIAN_POINT('Ctrl Pts',(-30.8146880502506,0.0574522089200695,
304.681024081034));
#14234=CARTESIAN_POINT('Ctrl Pts',(-30.8165072681548,0.150592551962246,
304.686056537021));
#14235=CARTESIAN_POINT('Ctrl Pts',(-30.8227561520802,0.243718377546381,
304.691088993008));
#14236=CARTESIAN_POINT('Ctrl Pts',(-30.8334203043104,0.336376906653812,
304.696121448994));
#14237=CARTESIAN_POINT('Ctrl Pts',(-30.8440805176586,0.429001211661709,
304.701152046207));
#14238=CARTESIAN_POINT('Ctrl Pts',(-30.8591527088614,0.521158121429664,
304.70618264342));
#14239=CARTESIAN_POINT('Ctrl Pts',(-30.8785705473647,0.612399148053428,
304.711213240632));
#14240=CARTESIAN_POINT('Ctrl Pts',(-30.8979866680719,0.703632103053712,
304.716243392814));
#14241=CARTESIAN_POINT('Ctrl Pts',(-30.921747578977,0.793948900766828,304.721273544995));
#14242=CARTESIAN_POINT('Ctrl Pts',(-30.9497358979465,0.882911570062178,
304.726303697177));
#14243=CARTESIAN_POINT('Ctrl Pts',(-30.9777296025736,0.971891358016018,
304.731334817287));
#14244=CARTESIAN_POINT('Ctrl Pts',(-31.0099521968002,1.05951607572889,304.736365937396));
#14245=CARTESIAN_POINT('Ctrl Pts',(-31.0462368920462,1.14536433763394,304.741397057506));
#14246=CARTESIAN_POINT('Ctrl Pts',(-31.0825614605805,1.23130693828065,304.746433706318));
#14247=CARTESIAN_POINT('Ctrl Pts',(-31.122956866943,1.31546877587347,304.751470355131));
#14248=CARTESIAN_POINT('Ctrl Pts',(-31.1672088839136,1.39745012698849,304.756507003943));
#14249=CARTESIAN_POINT('Ctrl Pts',(-31.2114880394619,1.47948175507192,304.761546741598));
#14250=CARTESIAN_POINT('Ctrl Pts',(-31.2596282843582,1.55932985381511,304.766586479252));
#14251=CARTESIAN_POINT('Ctrl Pts',(-31.3113714564842,1.63662280594869,304.771626216907));
#14252=CARTESIAN_POINT('Ctrl Pts',(-31.3631987410459,1.71404140361594,304.776674147036));
#14253=CARTESIAN_POINT('Ctrl Pts',(-31.4186403806381,1.78889620548035,304.781722077164));
#14254=CARTESIAN_POINT('Ctrl Pts',(-31.4773973968817,1.86084800044545,304.786770007293));
#14255=CARTESIAN_POINT('Ctrl Pts',(-31.5076083788235,1.89784331636418,304.789365491811));
#14256=CARTESIAN_POINT('Ctrl Pts',(-31.5386952293429,1.9340717539159,304.791960976329));
#14257=CARTESIAN_POINT('Ctrl Pts',(-31.5706136604705,1.96949113537912,304.794556460846));
#14258=CARTESIAN_POINT('Ctrl Pts',(-31.6327474971313,2.03844007756441,304.799608946366));
#14259=CARTESIAN_POINT('Ctrl Pts',(-31.6982589083538,2.10456961592866,304.804661431885));
#14260=CARTESIAN_POINT('Ctrl Pts',(-31.766861969177,2.16753051573831,304.809713917405));
#14261=CARTESIAN_POINT('Ctrl Pts',(-31.8353703396491,2.23040451286983,304.814759429159));
#14262=CARTESIAN_POINT('Ctrl Pts',(-31.9069615556201,2.29011826452337,304.819804940914));
#14263=CARTESIAN_POINT('Ctrl Pts',(-31.981310754738,2.34635700734113,304.824850452668));
#14264=CARTESIAN_POINT('Ctrl Pts',(-32.0555802999834,2.4025354988892,304.829890558923));
#14265=CARTESIAN_POINT('Ctrl Pts',(-32.1326016029631,2.45524611498477,304.834930665178));
#14266=CARTESIAN_POINT('Ctrl Pts',(-32.2120152378283,2.50421300769759,304.839970771433));
#14267=CARTESIAN_POINT('Ctrl Pts',(-32.2913714757742,2.553144509148,304.845007234906));
#14268=CARTESIAN_POINT('Ctrl Pts',(-32.373116231767,2.59833743295884,304.850043698379));
#14269=CARTESIAN_POINT('Ctrl Pts',(-32.4568603529284,2.63955869686101,304.855080161852));
#14270=CARTESIAN_POINT('Ctrl Pts',(-32.5405739207141,2.68076492151328,304.860114787811));
#14271=CARTESIAN_POINT('Ctrl Pts',(-32.6262850063833,2.71800216893644,304.865149413771));
#14272=CARTESIAN_POINT('Ctrl Pts',(-32.7135799813971,2.75108336139379,304.87018403973));
#14273=CARTESIAN_POINT('Ctrl Pts',(-32.8008675225753,2.78416173673429,304.875218236952));
#14274=CARTESIAN_POINT('Ctrl Pts',(-32.8897382694725,2.81308460353882,304.880252434175));
#14275=CARTESIAN_POINT('Ctrl Pts',(-32.979759821264,2.83771350995184,304.885286631397));
#14276=CARTESIAN_POINT('Ctrl Pts',(-33.0697988843359,2.86234720725854,304.890321807888));
#14277=CARTESIAN_POINT('Ctrl Pts',(-33.1609887683415,2.88268516846175,304.895356984378));
#14278=CARTESIAN_POINT('Ctrl Pts',(-33.2528842838104,2.89863946415913,304.900392160869));
#14279=CARTESIAN_POINT('Ctrl Pts',(-33.3448805646758,2.91461125408268,304.905432858538));
#14280=CARTESIAN_POINT('Ctrl Pts',(-33.437583583138,2.92618970747071,304.910473556207));
#14281=CARTESIAN_POINT('Ctrl Pts',(-33.5305406876089,2.93333850829839,304.915514253876));
#14282=CARTESIAN_POINT('Ctrl Pts',(-33.6235547875403,2.94049169232194,304.920558042184));
#14283=CARTESIAN_POINT('Ctrl Pts',(-33.716822839926,2.94320980382093,304.925601830493));
#14284=CARTESIAN_POINT('Ctrl Pts',(-33.8098920317969,2.94150868162442,304.930645618801));
#14285=CARTESIAN_POINT('Ctrl Pts',(-33.9031117125039,2.93980480878729,304.935697562696));
#14286=CARTESIAN_POINT('Ctrl Pts',(-33.9961314480596,2.93366746590286,304.940749506591));
#14287=CARTESIAN_POINT('Ctrl Pts',(-34.0885035655184,2.92316435314271,304.945801450486));
#14288=CARTESIAN_POINT('Ctrl Pts',(-34.1352283255008,2.91785154407991,304.948356884663));
#14289=CARTESIAN_POINT('Ctrl Pts',(-34.1817875400494,2.91142249892789,304.950912318839));
#14290=CARTESIAN_POINT('Ctrl Pts',(-34.2281245246065,2.90389090025923,304.953467753016));
#14291=CARTESIAN_POINT('Ctrl Pts',(-34.3197490134596,2.88899828510833,304.958520743677));
#14292=CARTESIAN_POINT('Ctrl Pts',(-34.4108318991177,2.86973832589534,304.963573734339));
#14293=CARTESIAN_POINT('Ctrl Pts',(-34.5009246691104,2.8461624109863,304.968626725));
#14294=CARTESIAN_POINT('Ctrl Pts',(-34.5908934455138,2.82261894332369,304.973672761291));
#14295=CARTESIAN_POINT('Ctrl Pts',(-34.6798743881723,2.7947714350649,304.978718797583));
#14296=CARTESIAN_POINT('Ctrl Pts',(-34.7674268960541,2.76272267361873,304.983764833874));
#14297=CARTESIAN_POINT('Ctrl Pts',(-34.8548859364688,2.73070812611603,304.988805483224));
#14298=CARTESIAN_POINT('Ctrl Pts',(-34.9409191583632,2.69450139213777,304.993846132574));
#14299=CARTESIAN_POINT('Ctrl Pts',(-35.025099974914,2.6542553857985,304.998886781924));
#14300=CARTESIAN_POINT('Ctrl Pts',(-35.1092203804635,2.61403826135463,305.003923813933));
#14301=CARTESIAN_POINT('Ctrl Pts',(-35.1914906234124,2.56978781717587,305.008960845943));
#14302=CARTESIAN_POINT('Ctrl Pts',(-35.2715039831891,2.52170511269069,305.013997877952));
#14303=CARTESIAN_POINT('Ctrl Pts',(-35.3514884017069,2.47363979997609,305.019033088041));
#14304=CARTESIAN_POINT('Ctrl Pts',(-35.429217178504,2.42174520923741,305.024068298129));
#14305=CARTESIAN_POINT('Ctrl Pts',(-35.5043090261056,2.36626788253385,305.029103508217));
#14306=CARTESIAN_POINT('Ctrl Pts',(-35.5793947021467,2.31079511533554,305.034138304477));
#14307=CARTESIAN_POINT('Ctrl Pts',(-35.6518435228012,2.25174046167026,305.039173100737));
#14308=CARTESIAN_POINT('Ctrl Pts',(-35.7213049238018,2.18939257034307,305.044207896998));
#14309=CARTESIAN_POINT('Ctrl Pts',(-35.7907800314854,2.12703237602788,305.049243686764));
#14310=CARTESIAN_POINT('Ctrl Pts',(-35.8572662185125,2.06137795033843,305.054279476531));
#14311=CARTESIAN_POINT('Ctrl Pts',(-35.9204484764443,1.99275604526325,305.059315266298));
#14312=CARTESIAN_POINT('Ctrl Pts',(-35.9837002323473,1.92405865882124,305.064356595233));
#14313=CARTESIAN_POINT('Ctrl Pts',(-36.0436405035994,1.85238760466307,305.069397924169));
#14314=CARTESIAN_POINT('Ctrl Pts',(-36.0999936365512,1.77810385199042,305.074439253104));
#14315=CARTESIAN_POINT('Ctrl Pts',(-36.1563814422621,1.70377439426943,305.07948368385));
#14316=CARTESIAN_POINT('Ctrl Pts',(-36.2091774646966,1.62682940365229,305.084528114597));
#14317=CARTESIAN_POINT('Ctrl Pts',(-36.2581498129686,1.54765822124098,305.089572545344));
#14318=CARTESIAN_POINT('Ctrl Pts',(-36.3072014459971,1.46835886307041,305.094625142872));
#14319=CARTESIAN_POINT('Ctrl Pts',(-36.3524168313347,1.3868265057755,305.099677740399));
#14320=CARTESIAN_POINT('Ctrl Pts',(-36.3936104632933,1.30347424757353,305.104730337927));
#14321=CARTESIAN_POINT('Ctrl Pts',(-36.4143970013056,1.26141423001381,305.107279907013));
#14322=CARTESIAN_POINT('Ctrl Pts',(-36.4341602616885,1.21889112438577,305.109829476099));
#14323=CARTESIAN_POINT('Ctrl Pts',(-36.452881187343,1.1759596035897,305.112379045185));
#14324=CARTESIAN_POINT('Ctrl Pts',(-36.4937574003875,1.08222075633557,305.117945902885));
#14325=CARTESIAN_POINT('Ctrl Pts',(-36.5297871600594,0.986245715449588,
305.123512760585));
#14326=CARTESIAN_POINT('Ctrl Pts',(-36.5607450233516,0.888527931337765,
305.129079618284));
#14327=CARTESIAN_POINT('Ctrl Pts',(-36.5916177368753,0.791078920513456,
305.134631164312));
#14328=CARTESIAN_POINT('Ctrl Pts',(-36.617446262904,0.69189698993402,305.14018271034));
#14329=CARTESIAN_POINT('Ctrl Pts',(-36.6380530834695,0.591494881633886,
305.145734256368));
#14330=CARTESIAN_POINT('Ctrl Pts',(-36.6585600993455,0.491579049283951,
305.15125891468));
#14331=CARTESIAN_POINT('Ctrl Pts',(-36.6738957476405,0.390455097248779,
305.156783572993));
#14332=CARTESIAN_POINT('Ctrl Pts',(-36.6839327803678,0.288647640461142,
305.162308231305));
#14333=CARTESIAN_POINT('Ctrl Pts',(-36.6933289030985,0.193341050867358,
305.167480115163));
#14334=CARTESIAN_POINT('Ctrl Pts',(-36.6980818219432,0.0974358112860457,
305.172651999022));
#14335=CARTESIAN_POINT('Ctrl Pts',(-36.6981267041397,0.00137457535742581,
305.17782388288));
#14336=CARTESIAN_POINT('',(-36.6981259159627,-0.00255481704953209,306.177823882956));
#14337=CARTESIAN_POINT('Ctrl Pts',(-36.69812670414,0.00137457480061522,
305.17782388291));
#14338=CARTESIAN_POINT('Ctrl Pts',(-36.6981711145098,-0.0936768503563982,
305.182941399114));
#14339=CARTESIAN_POINT('Ctrl Pts',(-36.6936047326977,-0.188714855235633,
305.188058915319));
#14340=CARTESIAN_POINT('Ctrl Pts',(-36.6844578460534,-0.2832712551197,305.193176431524));
#14341=CARTESIAN_POINT('Ctrl Pts',(-36.6753071449356,-0.377867087315354,
305.198296081856));
#14342=CARTESIAN_POINT('Ctrl Pts',(-36.6615721793269,-0.471980493434233,
305.203415732189));
#14343=CARTESIAN_POINT('Ctrl Pts',(-36.6433349537333,-0.565149871934047,
305.208535382522));
#14344=CARTESIAN_POINT('Ctrl Pts',(-36.6247061380591,-0.660319785232445,
305.213764962092));
#14345=CARTESIAN_POINT('Ctrl Pts',(-36.6013795804879,-0.754504207632462,
305.218994541661));
#14346=CARTESIAN_POINT('Ctrl Pts',(-36.5734968599925,-0.847225598247542,
305.22422412123));
#14347=CARTESIAN_POINT('Ctrl Pts',(-36.54613897342,-0.938201702523416,305.229355264897));
#14348=CARTESIAN_POINT('Ctrl Pts',(-36.5143951653034,-1.02776899639892,
305.234486408564));
#14349=CARTESIAN_POINT('Ctrl Pts',(-36.4784481532836,-1.11549615683031,
305.23961755223));
#14350=CARTESIAN_POINT('Ctrl Pts',(-36.4414667295986,-1.20574775512201,
305.244896349751));
#14351=CARTESIAN_POINT('Ctrl Pts',(-36.4000367303914,-1.29405126427797,
305.250175147272));
#14352=CARTESIAN_POINT('Ctrl Pts',(-36.3544073594601,-1.37996496509757,
305.255453944793));
#14353=CARTESIAN_POINT('Ctrl Pts',(-36.3087779885287,-1.46587866591718,
305.260732742313));
#14354=CARTESIAN_POINT('Ctrl Pts',(-36.2589495538321,-1.54940218336193,
305.266011539834));
#14355=CARTESIAN_POINT('Ctrl Pts',(-36.2052180200171,-1.63012800092138,
305.271290337355));
#14356=CARTESIAN_POINT('Ctrl Pts',(-36.1537916608698,-1.70739054288728,
305.276342665437));
#14357=CARTESIAN_POINT('Ctrl Pts',(-36.0986132638484,-1.78235581499684,
305.281394993518));
#14358=CARTESIAN_POINT('Ctrl Pts',(-36.0399148375032,-1.85463668373043,
305.2864473216));
#14359=CARTESIAN_POINT('Ctrl Pts',(-35.9812973679311,-1.92681786280866,
305.291492681519));
#14360=CARTESIAN_POINT('Ctrl Pts',(-35.9191697938031,-1.9963216536412,305.296538041438));
#14361=CARTESIAN_POINT('Ctrl Pts',(-35.853807665721,-2.0627893568237,305.301583401357));
#14362=CARTESIAN_POINT('Ctrl Pts',(-35.7885154902605,-2.12918592416307,
305.306623361572));
#14363=CARTESIAN_POINT('Ctrl Pts',(-35.7199959513547,-2.19255254731278,
305.311663321787));
#14364=CARTESIAN_POINT('Ctrl Pts',(-35.6485644612311,-2.25256399485696,
305.316703282002));
#14365=CARTESIAN_POINT('Ctrl Pts',(-35.5771844683521,-2.3125321782303,305.321739608749));
#14366=CARTESIAN_POINT('Ctrl Pts',(-35.5028970361107,-2.36914970887272,
305.326775935495));
#14367=CARTESIAN_POINT('Ctrl Pts',(-35.4260532144577,-2.4221293364772,305.331812262242));
#14368=CARTESIAN_POINT('Ctrl Pts',(-35.3492373402543,-2.47508969583817,
305.336846757319));
#14369=CARTESIAN_POINT('Ctrl Pts',(-35.2698672890388,-2.52441452868439,
305.341881252396));
#14370=CARTESIAN_POINT('Ctrl Pts',(-35.1883250236095,-2.56985853570132,
305.346915747473));
#14371=CARTESIAN_POINT('Ctrl Pts',(-35.1067896045841,-2.61529872717515,
305.351949819846));
#14372=CARTESIAN_POINT('Ctrl Pts',(-35.0230827221049,-2.65685852456116,
305.35698389222));
#14373=CARTESIAN_POINT('Ctrl Pts',(-34.9376119904645,-2.6943380034788,305.362017964594));
#14374=CARTESIAN_POINT('Ctrl Pts',(-34.8521245266221,-2.73182481957722,
305.367053022464));
#14375=CARTESIAN_POINT('Ctrl Pts',(-34.7648729348238,-2.76522955276159,
305.372088080334));
#14376=CARTESIAN_POINT('Ctrl Pts',(-34.6762848366658,-2.79440040117814,
305.377123138204));
#14377=CARTESIAN_POINT('Ctrl Pts',(-34.5875994170297,-2.82360329622559,
305.382163727509));
#14378=CARTESIAN_POINT('Ctrl Pts',(-34.4975749828143,-2.84856288283961,
305.387204316814));
#14379=CARTESIAN_POINT('Ctrl Pts',(-34.4066540525099,-2.86917733624367,
305.392244906119));
#14380=CARTESIAN_POINT('Ctrl Pts',(-34.315677271657,-2.88980445261239,305.397288591737));
#14381=CARTESIAN_POINT('Ctrl Pts',(-34.2238033354969,-2.90608104464846,
305.402332277355));
#14382=CARTESIAN_POINT('Ctrl Pts',(-34.1314825136292,-2.91795686351757,
305.407375962973));
#14383=CARTESIAN_POINT('Ctrl Pts',(-34.0390122288789,-2.92985190875497,
305.412427814071));
#14384=CARTESIAN_POINT('Ctrl Pts',(-33.9460940563293,-2.93733192175819,
305.417479665169));
#14385=CARTESIAN_POINT('Ctrl Pts',(-33.8531807296274,-2.94039871079895,
305.422531516266));
#14386=CARTESIAN_POINT('Ctrl Pts',(-33.8061579832348,-2.94195079001537,
305.425088220685));
#14387=CARTESIAN_POINT('Ctrl Pts',(-33.7591364404184,-2.94237334174126,
305.427644925105));
#14388=CARTESIAN_POINT('Ctrl Pts',(-33.7121742597644,-2.94167165985694,
305.430201629524));
#14389=CARTESIAN_POINT('Ctrl Pts',(-33.6193715853836,-2.94028505568902,
305.435253971736));
#14390=CARTESIAN_POINT('Ctrl Pts',(-33.5264680640071,-2.93450010510437,
305.440306313949));
#14391=CARTESIAN_POINT('Ctrl Pts',(-33.4339147939597,-2.9243021865057,305.445358656161));
#14392=CARTESIAN_POINT('Ctrl Pts',(-33.3414891459972,-2.91411832985895,
305.450404031678));
#14393=CARTESIAN_POINT('Ctrl Pts',(-33.2494132273939,-2.89953364522624,
305.455449407195));
#14394=CARTESIAN_POINT('Ctrl Pts',(-33.1581378141286,-2.88058551398379,
305.460494782712));
#14395=CARTESIAN_POINT('Ctrl Pts',(-33.0669600603847,-2.86165765616839,
305.465534759963));
#14396=CARTESIAN_POINT('Ctrl Pts',(-32.9765815421969,-2.8383757211902,305.470574737214));
#14397=CARTESIAN_POINT('Ctrl Pts',(-32.8874464882813,-2.81082872560364,
305.475614714464));
#14398=CARTESIAN_POINT('Ctrl Pts',(-32.7983756576732,-2.78330157809133,
305.480651060327));
#14399=CARTESIAN_POINT('Ctrl Pts',(-32.7105469337537,-2.7515156088772,305.485687406189));
#14400=CARTESIAN_POINT('Ctrl Pts',(-32.6243919166768,-2.71561036306861,
305.490723752052));
#14401=CARTESIAN_POINT('Ctrl Pts',(-32.5382682113436,-2.679718166481,305.49575826753));
#14402=CARTESIAN_POINT('Ctrl Pts',(-32.4538174140773,-2.63970983814811,
305.500792783009));
#14403=CARTESIAN_POINT('Ctrl Pts',(-32.3714526001545,-2.59577362966524,
305.505827298487));
#14404=CARTESIAN_POINT('Ctrl Pts',(-32.2890946809843,-2.55184109907919,
305.510861392526));
#14405=CARTESIAN_POINT('Ctrl Pts',(-32.2088227898532,-2.50398155132848,
305.515895486566));
#14406=CARTESIAN_POINT('Ctrl Pts',(-32.1310257494574,-2.45242937582157,
305.520929580605));
#14407=CARTESIAN_POINT('Ctrl Pts',(-32.0532134599363,-2.4008670954883,305.525964661386));
#14408=CARTESIAN_POINT('Ctrl Pts',(-31.9778773546524,-2.34561099561574,
305.530999742166));
#14409=CARTESIAN_POINT('Ctrl Pts',(-31.9053766372575,-2.28693834663676,
305.536034822947));
#14410=CARTESIAN_POINT('Ctrl Pts',(-31.8327962467274,-2.22820122058678,
305.541075436923));
#14411=CARTESIAN_POINT('Ctrl Pts',(-31.7630578096342,-2.16604033081065,
305.546116050899));
#14412=CARTESIAN_POINT('Ctrl Pts',(-31.6964865840428,-2.10077253716643,
305.551156664876));
#14413=CARTESIAN_POINT('Ctrl Pts',(-31.6298744518257,-2.03546463782815,
305.556200376204));
#14414=CARTESIAN_POINT('Ctrl Pts',(-31.5664337074163,-1.96704635943276,
305.561244087532));
#14415=CARTESIAN_POINT('Ctrl Pts',(-31.5064504491303,-1.89586900993298,
305.56628779886));
#14416=CARTESIAN_POINT('Ctrl Pts',(-31.446370065043,-1.82457640898968,305.571339677042));
#14417=CARTESIAN_POINT('Ctrl Pts',(-31.3897586130749,-1.75051617056496,
305.576391555224));
#14418=CARTESIAN_POINT('Ctrl Pts',(-31.3368597640667,-1.6740698668006,305.581443433406));
#14419=CARTESIAN_POINT('Ctrl Pts',(-31.3100903733426,-1.63538431856568,
305.583999929502));
#14420=CARTESIAN_POINT('Ctrl Pts',(-31.2842710071267,-1.59608815225124,
305.586556425598));
#14421=CARTESIAN_POINT('Ctrl Pts',(-31.2594287056429,-1.55623311262589,
305.589112921693));
#14422=CARTESIAN_POINT('Ctrl Pts',(-31.2103345269535,-1.47747026376844,
305.594165153919));
#14423=CARTESIAN_POINT('Ctrl Pts',(-31.1648829387026,-1.39624058813763,
305.599217386146));
#14424=CARTESIAN_POINT('Ctrl Pts',(-31.1233305500467,-1.3129153514667,305.604269618372));
#14425=CARTESIAN_POINT('Ctrl Pts',(-31.0818354756799,-1.22970504745927,
305.609314881923));
#14426=CARTESIAN_POINT('Ctrl Pts',(-31.0442291101545,-1.14440532024443,
305.614360145474));
#14427=CARTESIAN_POINT('Ctrl Pts',(-31.0107241737315,-1.05741533128288,
305.619405409025));
#14428=CARTESIAN_POINT('Ctrl Pts',(-30.9772550985143,-0.970518449971734,
305.624445272499));
#14429=CARTESIAN_POINT('Ctrl Pts',(-30.947878885703,-0.881935315182517,
305.629485135974));
#14430=CARTESIAN_POINT('Ctrl Pts',(-30.9227613040443,-0.792087551886581,
305.634524999448));
#14431=CARTESIAN_POINT('Ctrl Pts',(-30.8976618315003,-0.702304566460958,
305.639561229313));
#14432=CARTESIAN_POINT('Ctrl Pts',(-30.8768150066068,-0.611259191416344,
305.644597459178));
#14433=CARTESIAN_POINT('Ctrl Pts',(-30.8603372828654,-0.519389803381136,
305.649633689044));
#14434=CARTESIAN_POINT('Ctrl Pts',(-30.84386555221,-0.427553829011225,305.65466808719));
#14435=CARTESIAN_POINT('Ctrl Pts',(-30.831759844188,-0.334894873883701,
305.659702485337));
#14436=CARTESIAN_POINT('Ctrl Pts',(-30.8240856351023,-0.241862122739805,
305.664736883483));
#14437=CARTESIAN_POINT('Ctrl Pts',(-30.8164120702546,-0.148837181552168,
305.669770859));
#14438=CARTESIAN_POINT('Ctrl Pts',(-30.8131693010271,-0.0554389495150576,
305.674804834516));
#14439=CARTESIAN_POINT('Ctrl Pts',(-30.8143708835112,0.0378787869061924,
305.679838810033));
#14440=CARTESIAN_POINT('Ctrl Pts',(-30.8155727012748,0.131214795689443,
305.684873771242));
#14441=CARTESIAN_POINT('Ctrl Pts',(-30.8212205929581,0.224469833356506,
305.689908732451));
#14442=CARTESIAN_POINT('Ctrl Pts',(-30.8312760256051,0.317191787144155,
305.69494369366));
#14443=CARTESIAN_POINT('Ctrl Pts',(-30.8413425069902,0.410015622235569,
305.699984187199));
#14444=CARTESIAN_POINT('Ctrl Pts',(-30.8558261484302,0.502304761874496,
305.705024680738));
#14445=CARTESIAN_POINT('Ctrl Pts',(-30.8746367516526,0.593614187094206,
305.710065174277));
#14446=CARTESIAN_POINT('Ctrl Pts',(-30.8934589113658,0.684979709214852,
305.715108764496));
#14447=CARTESIAN_POINT('Ctrl Pts',(-30.9166132148726,0.77536388860677,305.720152354715));
#14448=CARTESIAN_POINT('Ctrl Pts',(-30.9439592965877,0.864335968144081,
305.725195944934));
#14449=CARTESIAN_POINT('Ctrl Pts',(-30.9713496592894,0.953452118466536,
305.730247702142));
#14450=CARTESIAN_POINT('Ctrl Pts',(-31.0029452005464,1.04115118660185,305.73529945935));
#14451=CARTESIAN_POINT('Ctrl Pts',(-31.0385571348216,1.12702169038389,305.740351216558));
#14452=CARTESIAN_POINT('Ctrl Pts',(-31.056587182879,1.1704972651151,305.742908882326));
#14453=CARTESIAN_POINT('Ctrl Pts',(-31.0756460196631,1.21350449811005,305.745466548094));
#14454=CARTESIAN_POINT('Ctrl Pts',(-31.0957047499967,1.2559925625956,305.748024213862));
#14455=CARTESIAN_POINT('Ctrl Pts',(-31.1353277645684,1.33992136418171,305.753076499142));
#14456=CARTESIAN_POINT('Ctrl Pts',(-31.1789973687618,1.42212398259354,305.758128784422));
#14457=CARTESIAN_POINT('Ctrl Pts',(-31.2265404258993,1.5021836227129,305.763181069703));
#14458=CARTESIAN_POINT('Ctrl Pts',(-31.274017912798,1.58213284650578,305.768226386993));
#14459=CARTESIAN_POINT('Ctrl Pts',(-31.3253580121973,1.6599445863842,305.773271704283));
#14460=CARTESIAN_POINT('Ctrl Pts',(-31.3803403677703,1.73522383515941,305.778317021573));
#14461=CARTESIAN_POINT('Ctrl Pts',(-31.4352638815194,1.81042252048378,305.783356939391));
#14462=CARTESIAN_POINT('Ctrl Pts',(-31.4938216431132,1.8830937449263,305.788396857209));
#14463=CARTESIAN_POINT('Ctrl Pts',(-31.5557489845037,1.95286980563684,305.793436775028));
#14464=CARTESIAN_POINT('Ctrl Pts',(-31.6176316866468,2.02259556948712,305.798473059909));
#14465=CARTESIAN_POINT('Ctrl Pts',(-31.6828788467583,2.08942998635647,305.80350934479));
#14466=CARTESIAN_POINT('Ctrl Pts',(-31.7511850065142,2.15303773805229,305.808545629671));
#14467=CARTESIAN_POINT('Ctrl Pts',(-31.8194663283909,2.21662236033099,305.813580083229));
#14468=CARTESIAN_POINT('Ctrl Pts',(-31.8908041153576,2.27698234586884,305.818614536788));
#14469=CARTESIAN_POINT('Ctrl Pts',(-31.9648562151284,2.33381937706824,305.823648990346));
#14470=CARTESIAN_POINT('Ctrl Pts',(-32.0389021032213,2.39065164063333,305.828683021601));
#14471=CARTESIAN_POINT('Ctrl Pts',(-32.1156614989019,2.44396126706701,305.833717052857));
#14472=CARTESIAN_POINT('Ctrl Pts',(-32.1947602624996,2.49349109325755,305.838751084113));
#14473=CARTESIAN_POINT('Ctrl Pts',(-32.2738745181639,2.54303062022381,305.84378610132));
#14474=CARTESIAN_POINT('Ctrl Pts',(-32.3553286749949,2.58878864126048,305.848821118527));
#14475=CARTESIAN_POINT('Ctrl Pts',(-32.4387217898061,2.63055268823968,305.853856135734));
#14476=CARTESIAN_POINT('Ctrl Pts',(-32.5222065353734,2.67236262475317,305.858896685321));
#14477=CARTESIAN_POINT('Ctrl Pts',(-32.6076340937918,2.71016962799671,305.863937234909));
#14478=CARTESIAN_POINT('Ctrl Pts',(-32.6945815041307,2.74380850399137,305.868977784496));
#14479=CARTESIAN_POINT('Ctrl Pts',(-32.7815823328632,2.77746804690081,305.874021430876));
#14480=CARTESIAN_POINT('Ctrl Pts',(-32.8701044512753,2.8069542242249,305.879065077255));
#14481=CARTESIAN_POINT('Ctrl Pts',(-32.9597097176111,2.83215173888708,305.884108723635));
#14482=CARTESIAN_POINT('Ctrl Pts',(-33.0494600717647,2.85739005307551,305.889160536629));
#14483=CARTESIAN_POINT('Ctrl Pts',(-33.1402966427661,2.8783257418025,305.894212349623));
#14484=CARTESIAN_POINT('Ctrl Pts',(-33.2317712685927,2.89489465101105,305.899264162617));
#14485=CARTESIAN_POINT('Ctrl Pts',(-33.2780736732506,2.90328146136399,305.901821277089));
#14486=CARTESIAN_POINT('Ctrl Pts',(-33.3245394738246,2.91055026116043,305.90437839156));
#14487=CARTESIAN_POINT('Ctrl Pts',(-33.3711103324178,2.91669781537868,305.906935506032));
#14488=CARTESIAN_POINT('Ctrl Pts',(-33.463123866918,2.92884399883414,305.911987788678));
#14489=CARTESIAN_POINT('Ctrl Pts',(-33.5558778885821,2.93665356560635,305.917040071324));
#14490=CARTESIAN_POINT('Ctrl Pts',(-33.6489282527769,2.94004633010751,305.922092353969));
#14491=CARTESIAN_POINT('Ctrl Pts',(-33.7418502857503,2.94343441544792,305.927137668715));
#14492=CARTESIAN_POINT('Ctrl Pts',(-33.8350674090016,2.94241778699734,305.932182983462));
#14493=CARTESIAN_POINT('Ctrl Pts',(-33.9281282201202,2.93696775415833,305.937228298208));
#14494=CARTESIAN_POINT('Ctrl Pts',(-34.021089439732,2.93152355381719,305.942268213576));
#14495=CARTESIAN_POINT('Ctrl Pts',(-34.113894238596,2.9216554053822,305.947308128944));
#14496=CARTESIAN_POINT('Ctrl Pts',(-34.2060901687657,2.90738665634351,305.952348044312));
#14497=CARTESIAN_POINT('Ctrl Pts',(-34.2982196438287,2.89312819226249,305.957384326893));
#14498=CARTESIAN_POINT('Ctrl Pts',(-34.3897406847555,2.87447550005484,305.962420609475));
#14499=CARTESIAN_POINT('Ctrl Pts',(-34.4802059759686,2.85150375646556,305.967456892057));
#14500=CARTESIAN_POINT('Ctrl Pts',(-34.5706383733567,2.82854036556609,305.97249134341));
#14501=CARTESIAN_POINT('Ctrl Pts',(-34.6600153534899,2.80126115235585,305.977525794764));
#14502=CARTESIAN_POINT('Ctrl Pts',(-34.7479008320584,2.76979217923366,305.982560246117));
#14503=CARTESIAN_POINT('Ctrl Pts',(-34.8357789402739,2.73832584519863,305.987594275266));
#14504=CARTESIAN_POINT('Ctrl Pts',(-34.9221653774275,2.702670599785,305.992628304414));
#14505=CARTESIAN_POINT('Ctrl Pts',(-35.0066413314548,2.66300168418949,305.997662333563));
#14506=CARTESIAN_POINT('Ctrl Pts',(-35.0911338324131,2.62332499834962,306.002697348764));
#14507=CARTESIAN_POINT('Ctrl Pts',(-35.1737147050978,2.57963327011389,306.007732363965));
#14508=CARTESIAN_POINT('Ctrl Pts',(-35.2539881935179,2.53214847918087,306.012767379166));
#14509=CARTESIAN_POINT('Ctrl Pts',(-35.3343498876031,2.48461151127571,306.017807926914));
#14510=CARTESIAN_POINT('Ctrl Pts',(-35.412398753533,2.43327338764073,306.022848474663));
#14511=CARTESIAN_POINT('Ctrl Pts',(-35.4877668514603,2.37840020019946,306.027889022411));
#14512=CARTESIAN_POINT('Ctrl Pts',(-35.5631812551253,2.32349329897871,306.032932667044));
#14513=CARTESIAN_POINT('Ctrl Pts',(-35.6359112657968,2.2650472881556,306.037976311676));
#14514=CARTESIAN_POINT('Ctrl Pts',(-35.7056226673916,2.20336804490324,306.043019956309));
#14515=CARTESIAN_POINT('Ctrl Pts',(-35.7754469471574,2.14158892931992,306.048071767717));
#14516=CARTESIAN_POINT('Ctrl Pts',(-35.8422425420291,2.07656643913191,306.053123579126));
#14517=CARTESIAN_POINT('Ctrl Pts',(-35.9057128021194,2.00864257345936,306.058175390534));
#14518=CARTESIAN_POINT('Ctrl Pts',(-35.9378403038885,1.97426073680938,306.060732526423));
#14519=CARTESIAN_POINT('Ctrl Pts',(-35.9691164376634,1.93913602754469,306.063289662312));
#14520=CARTESIAN_POINT('Ctrl Pts',(-35.999506887958,1.90331573619042,306.065846798201));
#14521=CARTESIAN_POINT('Ctrl Pts',(-36.0591447921124,1.83302236831168,306.070864895122));
#14522=CARTESIAN_POINT('Ctrl Pts',(-36.1155911972667,1.7597869486787,306.075882992043));
#14523=CARTESIAN_POINT('Ctrl Pts',(-36.1685392712908,1.68393323952848,306.080901088964));
#14524=CARTESIAN_POINT('Ctrl Pts',(-36.2214185594307,1.6081780734235,306.085912666777));
#14525=CARTESIAN_POINT('Ctrl Pts',(-36.2708082843961,1.52981173657589,306.09092424459));
#14526=CARTESIAN_POINT('Ctrl Pts',(-36.316440565194,1.44919238792459,306.095935822403));
#14527=CARTESIAN_POINT('Ctrl Pts',(-36.3620267530452,1.36865447248823,306.100942338045));
#14528=CARTESIAN_POINT('Ctrl Pts',(-36.403862813887,1.28586845454363,306.105948853687));
#14529=CARTESIAN_POINT('Ctrl Pts',(-36.4417237757902,1.20122191685325,306.110955369329));
#14530=CARTESIAN_POINT('Ctrl Pts',(-36.479557433727,1.11663642320685,306.115958274452));
#14531=CARTESIAN_POINT('Ctrl Pts',(-36.5134215051908,1.0301934856244,306.120961179575));
#14532=CARTESIAN_POINT('Ctrl Pts',(-36.5431372321584,0.942304678238938,
306.125964084698));
#14533=CARTESIAN_POINT('Ctrl Pts',(-36.5728451955578,0.854438832793723,
306.130965682756));
#14534=CARTESIAN_POINT('Ctrl Pts',(-36.5984068163879,0.765128291939525,
306.135967280813));
#14535=CARTESIAN_POINT('Ctrl Pts',(-36.6196920864541,0.67480303814878,306.140968878871));
#14536=CARTESIAN_POINT('Ctrl Pts',(-36.6409740365617,0.584491872790789,
306.145969696807));
#14537=CARTESIAN_POINT('Ctrl Pts',(-36.6579808638972,0.493166748923216,
306.150970514743));
#14538=CARTESIAN_POINT('Ctrl Pts',(-36.6706332603493,0.40126974170949,306.155971332679));
#14539=CARTESIAN_POINT('Ctrl Pts',(-36.6832914889933,0.30933037406389,306.160974455769));
#14540=CARTESIAN_POINT('Ctrl Pts',(-36.6915912226164,0.216819044003163,
306.16597757886));
#14541=CARTESIAN_POINT('Ctrl Pts',(-36.6955049036665,0.124184088836673,
306.170980701951));
#14542=CARTESIAN_POINT('Ctrl Pts',(-36.6972892576362,0.0819492853693997,
306.17326176227));
#14543=CARTESIAN_POINT('Ctrl Pts',(-36.6981626001127,0.0396888201570203,
306.17554282259));
#14544=CARTESIAN_POINT('Ctrl Pts',(-36.6981259159634,-0.00255481619919655,
306.17782388291));
#14545=CARTESIAN_POINT('',(-36.6981270248952,-4.61744834887231E-5,307.177823883003));
#14546=CARTESIAN_POINT('Ctrl Pts',(-36.6981259159627,-0.00255481704952955,
306.177823882956));
#14547=CARTESIAN_POINT('Ctrl Pts',(-36.6980278861538,-0.115441017225031,
306.183919481112));
#14548=CARTESIAN_POINT('Ctrl Pts',(-36.6914288167197,-0.228042423400951,
306.190015079268));
#14549=CARTESIAN_POINT('Ctrl Pts',(-36.678449336265,-0.33970032468089,306.196110677424));
#14550=CARTESIAN_POINT('Ctrl Pts',(-36.66528380746,-0.452958734425924,306.202293650108));
#14551=CARTESIAN_POINT('Ctrl Pts',(-36.6455537081551,-0.565246414805456,
306.208476622792));
#14552=CARTESIAN_POINT('Ctrl Pts',(-36.6194337914689,-0.675898189499465,
306.214659595477));
#14553=CARTESIAN_POINT('Ctrl Pts',(-36.6052134555697,-0.736139783027078,
306.218025760441));
#14554=CARTESIAN_POINT('Ctrl Pts',(-36.5891000237347,-0.795896879811981,
306.221391925406));
#14555=CARTESIAN_POINT('Ctrl Pts',(-36.5711275860838,-0.855064817746686,
306.22475809037));
#14556=CARTESIAN_POINT('Ctrl Pts',(-36.544152748426,-0.943869995505168,
306.229810368487));
#14557=CARTESIAN_POINT('Ctrl Pts',(-36.5129230489886,-1.03155685598148,
306.234862646604));
#14558=CARTESIAN_POINT('Ctrl Pts',(-36.4775490641029,-1.1176878305175,306.23991492472));
#14559=CARTESIAN_POINT('Ctrl Pts',(-36.442223866422,-1.20370001466287,306.24496023482));
#14560=CARTESIAN_POINT('Ctrl Pts',(-36.4027659084823,-1.28816016956632,
306.25000554492));
#14561=CARTESIAN_POINT('Ctrl Pts',(-36.3593356563898,-1.3706454037419,306.25505085502));
#14562=CARTESIAN_POINT('Ctrl Pts',(-36.3159518833297,-1.45304236226443,
306.260090765631));
#14563=CARTESIAN_POINT('Ctrl Pts',(-36.2686044717746,-1.53346821009158,
306.265130676243));
#14564=CARTESIAN_POINT('Ctrl Pts',(-36.2175017042479,-1.61152061408643,
306.270170586854));
#14565=CARTESIAN_POINT('Ctrl Pts',(-36.1664357732496,-1.68951675538271,
306.275206864535));
#14566=CARTESIAN_POINT('Ctrl Pts',(-36.1116201094323,-1.76514248279957,
306.280243142216));
#14567=CARTESIAN_POINT('Ctrl Pts',(-36.0533080678788,-1.83802156065203,
306.285279419897));
#14568=CARTESIAN_POINT('Ctrl Pts',(-35.995017230037,-1.91087413785538,306.290313866262));
#14569=CARTESIAN_POINT('Ctrl Pts',(-35.933232817441,-1.98098170308195,306.295348312627));
#14570=CARTESIAN_POINT('Ctrl Pts',(-35.8682498774875,-2.0479992815156,306.300382758992));
#14571=CARTESIAN_POINT('Ctrl Pts',(-35.8032723882692,-2.11501123854948,
306.30541678307));
#14572=CARTESIAN_POINT('Ctrl Pts',(-35.7350972145074,-2.17893340530029,
306.310450807148));
#14573=CARTESIAN_POINT('Ctrl Pts',(-35.6640570446037,-2.23945686300899,
306.315484831226));
#14574=CARTESIAN_POINT('Ctrl Pts',(-35.5930029605927,-2.29999217499513,
306.320519841281));
#14575=CARTESIAN_POINT('Ctrl Pts',(-35.5190831043916,-2.35712716808914,
306.325554851336));
#14576=CARTESIAN_POINT('Ctrl Pts',(-35.4426631925446,-2.41059323744859,
306.33058986139));
#14577=CARTESIAN_POINT('Ctrl Pts',(-35.3661593105919,-2.46411805525971,
306.335630403908));
#14578=CARTESIAN_POINT('Ctrl Pts',(-35.2871502541142,-2.5139656470969,306.340670946426));
#14579=CARTESIAN_POINT('Ctrl Pts',(-35.2060304087611,-2.55991097081618,
306.345711488944));
#14580=CARTESIAN_POINT('Ctrl Pts',(-35.1248607246741,-2.6058845226066,306.35075512829));
#14581=CARTESIAN_POINT('Ctrl Pts',(-35.0415780662161,-2.64795083319799,
306.355798767636));
#14582=CARTESIAN_POINT('Ctrl Pts',(-34.9565991061602,-2.68593201384052,
306.360842406982));
#14583=CARTESIAN_POINT('Ctrl Pts',(-34.8714825468343,-2.72397469420872,
306.365894213069));
#14584=CARTESIAN_POINT('Ctrl Pts',(-34.7846646157423,-2.75791887761006,
306.370946019155));
#14585=CARTESIAN_POINT('Ctrl Pts',(-34.6965793487808,-2.78763581322592,
306.375997825242));
#14586=CARTESIAN_POINT('Ctrl Pts',(-34.6519912575088,-2.8026782997083,306.378555011008));
#14587=CARTESIAN_POINT('Ctrl Pts',(-34.6070786392107,-2.81663844150935,
306.381112196774));
#14588=CARTESIAN_POINT('Ctrl Pts',(-34.561898743212,-2.82950453941054,306.38366938254));
#14589=CARTESIAN_POINT('Ctrl Pts',(-34.4726360188751,-2.85492431793941,
306.388721659954));
#14590=CARTESIAN_POINT('Ctrl Pts',(-34.3820090100032,-2.87616160923423,
306.393773937368));
#14591=CARTESIAN_POINT('Ctrl Pts',(-34.2904454424642,-2.89307238572315,
306.398826214782));
#14592=CARTESIAN_POINT('Ctrl Pts',(-34.1990081578266,-2.90995983915926,
306.403871524181));
#14593=CARTESIAN_POINT('Ctrl Pts',(-34.1066373143415,-2.92253255510016,
306.408916833581));
#14594=CARTESIAN_POINT('Ctrl Pts',(-34.0137753194199,-2.93069639446246,
306.41396214298));
#14595=CARTESIAN_POINT('Ctrl Pts',(-33.9210127053026,-2.9388514968929,306.419002052895));
#14596=CARTESIAN_POINT('Ctrl Pts',(-33.8277604246888,-2.94260706252909,
306.42404196281));
#14597=CARTESIAN_POINT('Ctrl Pts',(-33.734469499653,-2.94192028300984,306.429081872725));
#14598=CARTESIAN_POINT('Ctrl Pts',(-33.6412458215886,-2.94123399854241,
306.434118149718));
#14599=CARTESIAN_POINT('Ctrl Pts',(-33.5479839974368,-2.93611173695885,
306.43915442671));
#14600=CARTESIAN_POINT('Ctrl Pts',(-33.4551375214818,-2.9265627139388,306.444190703703));
#14601=CARTESIAN_POINT('Ctrl Pts',(-33.3623248067228,-2.91701716317156,
306.449225149385));
#14602=CARTESIAN_POINT('Ctrl Pts',(-33.2699275816022,-2.9030480941656,306.454259595067));
#14603=CARTESIAN_POINT('Ctrl Pts',(-33.1783956413144,-2.88471670151629,
306.45929404075));
#14604=CARTESIAN_POINT('Ctrl Pts',(-33.0868713785632,-2.86638684647166,
306.464328064151));
#14605=CARTESIAN_POINT('Ctrl Pts',(-32.9962126919121,-2.84369548270597,
306.469362087553));
#14606=CARTESIAN_POINT('Ctrl Pts',(-32.9068594522753,-2.81675497505209,
306.474396110955));
#14607=CARTESIAN_POINT('Ctrl Pts',(-32.8174887115554,-2.7898091907226,306.47943112034));
#14608=CARTESIAN_POINT('Ctrl Pts',(-32.7294243508627,-2.75861273823514,
306.484466129726));
#14609=CARTESIAN_POINT('Ctrl Pts',(-32.6430902392105,-2.72332758090282,
306.489501139112));
#14610=CARTESIAN_POINT('Ctrl Pts',(-32.556661263468,-2.68800365217077,306.494541680976));
#14611=CARTESIAN_POINT('Ctrl Pts',(-32.4719667436607,-2.64858221901239,
306.49958222284));
#14612=CARTESIAN_POINT('Ctrl Pts',(-32.3894094550258,-2.6052729383348,306.504622764703));
#14613=CARTESIAN_POINT('Ctrl Pts',(-32.3068014443821,-2.5619370490591,306.509666403404));
#14614=CARTESIAN_POINT('Ctrl Pts',(-32.2263336618595,-2.51470878166137,
306.514710042104));
#14615=CARTESIAN_POINT('Ctrl Pts',(-32.1483813140059,-2.46384206635727,
306.519753680804));
#14616=CARTESIAN_POINT('Ctrl Pts',(-32.0703027441829,-2.41289298667088,
306.524805486263));
#14617=CARTESIAN_POINT('Ctrl Pts',(-31.994748099982,-2.35829395741093,306.529857291721));
#14618=CARTESIAN_POINT('Ctrl Pts',(-31.9220606841871,-2.30034011758097,
306.53490909718));
#14619=CARTESIAN_POINT('Ctrl Pts',(-31.8852667663045,-2.27100424423385,
306.53746628969));
#14620=CARTESIAN_POINT('Ctrl Pts',(-31.8492069570012,-2.24080936811905,
306.540023482199));
#14621=CARTESIAN_POINT('Ctrl Pts',(-31.8139220971151,-2.20979727963877,
306.542580674709));
#14622=CARTESIAN_POINT('Ctrl Pts',(-31.744209368765,-2.14852631790696,306.547632951162));
#14623=CARTESIAN_POINT('Ctrl Pts',(-31.6772737338398,-2.08384328835132,
306.552685227615));
#14624=CARTESIAN_POINT('Ctrl Pts',(-31.6134679200877,-2.01602975152468,
306.557737504069));
#14625=CARTESIAN_POINT('Ctrl Pts',(-31.5497501064817,-1.94830974224348,
306.562782812488));
#14626=CARTESIAN_POINT('Ctrl Pts',(-31.4891538381885,-1.87746812596406,
306.567828120907));
#14627=CARTESIAN_POINT('Ctrl Pts',(-31.4319978559518,-1.80382582429177,
306.572873429327));
#14628=CARTESIAN_POINT('Ctrl Pts',(-31.3749030421993,-1.7302623348067,306.577913338244));
#14629=CARTESIAN_POINT('Ctrl Pts',(-31.3212414672872,-1.65390446658554,
306.582953247161));
#14630=CARTESIAN_POINT('Ctrl Pts',(-31.2712933867857,-1.57510818330629,
306.587993156078));
#14631=CARTESIAN_POINT('Ctrl Pts',(-31.2213813106296,-1.49636869917867,
306.59302943205));
#14632=CARTESIAN_POINT('Ctrl Pts',(-31.175177645499,-1.41519466780222,306.598065708022));
#14633=CARTESIAN_POINT('Ctrl Pts',(-31.1329202522621,-1.33197230681066,
306.603101983994));
#14634=CARTESIAN_POINT('Ctrl Pts',(-31.0906782249401,-1.24878020768858,
306.608136428642));
#14635=CARTESIAN_POINT('Ctrl Pts',(-31.0523798197239,-1.1635416543478,306.61317087329));
#14636=CARTESIAN_POINT('Ctrl Pts',(-31.0182171983976,-1.0766679060804,306.618205317938));
#14637=CARTESIAN_POINT('Ctrl Pts',(-30.984057442656,-0.989801444843948,
306.623239340293));
#14638=CARTESIAN_POINT('Ctrl Pts',(-30.9540329434734,-0.901300474894601,
306.628273362648));
#14639=CARTESIAN_POINT('Ctrl Pts',(-30.9282874718564,-0.811595626047812,
306.633307385003));
#14640=CARTESIAN_POINT('Ctrl Pts',(-30.9025369576843,-0.721873207445191,
306.638342393331));
#14641=CARTESIAN_POINT('Ctrl Pts',(-30.8810672577357,-0.630946868751912,
306.643377401659));
#14642=CARTESIAN_POINT('Ctrl Pts',(-30.8639717819456,-0.539260649948624,
306.648412409987));
#14643=CARTESIAN_POINT('Ctrl Pts',(-30.8468575216451,-0.447473686319338,
306.653452950783));
#14644=CARTESIAN_POINT('Ctrl Pts',(-30.8341271612002,-0.354925613313889,
306.658493491578));
#14645=CARTESIAN_POINT('Ctrl Pts',(-30.825822593093,-0.26206856895959,306.663534032374));
#14646=CARTESIAN_POINT('Ctrl Pts',(-30.8175129227902,-0.169154474702264,
306.668577669998));
#14647=CARTESIAN_POINT('Ctrl Pts',(-30.813634476547,-0.0759314747314025,
306.673621307622));
#14648=CARTESIAN_POINT('Ctrl Pts',(-30.8141769978822,0.0171474903620899,
306.678664945247));
#14649=CARTESIAN_POINT('Ctrl Pts',(-30.8147203976786,0.11037717074817,306.683716749628));
#14650=CARTESIAN_POINT('Ctrl Pts',(-30.8196990324575,0.203461907586567,
306.68876855401));
#14651=CARTESIAN_POINT('Ctrl Pts',(-30.8290507251081,0.295953261687169,
306.693820358392));
#14652=CARTESIAN_POINT('Ctrl Pts',(-30.833784513888,0.342772008906082,306.696377561221));
#14653=CARTESIAN_POINT('Ctrl Pts',(-30.8396380121032,0.389438859133182,
306.698934764049));
#14654=CARTESIAN_POINT('Ctrl Pts',(-30.8465982077714,0.435896845844663,
306.701491966878));
#14655=CARTESIAN_POINT('Ctrl Pts',(-30.8603494975764,0.527684098601365,
306.706544243979));
#14656=CARTESIAN_POINT('Ctrl Pts',(-30.8784731646952,0.618984748438965,
306.711596521079));
#14657=CARTESIAN_POINT('Ctrl Pts',(-30.9009235509167,0.709349786855151,
306.71664879818));
#14658=CARTESIAN_POINT('Ctrl Pts',(-30.9233429739038,0.799590195172318,
306.721694107256));
#14659=CARTESIAN_POINT('Ctrl Pts',(-30.950077151935,0.888897128811458,306.726739416332));
#14660=CARTESIAN_POINT('Ctrl Pts',(-30.9810289311959,0.97682883266996,306.731784725408));
#14661=CARTESIAN_POINT('Ctrl Pts',(-31.011947585836,1.06466643194327,306.73682463499));
#14662=CARTESIAN_POINT('Ctrl Pts',(-31.0470747233719,1.15113131000311,306.741864544572));
#14663=CARTESIAN_POINT('Ctrl Pts',(-31.0862628889441,1.23579508561368,306.746904454154));
#14664=CARTESIAN_POINT('Ctrl Pts',(-31.1254228063775,1.32039783274682,306.7519407308));
#14665=CARTESIAN_POINT('Ctrl Pts',(-31.1686377473062,1.40320165596974,306.756977007447));
#14666=CARTESIAN_POINT('Ctrl Pts',(-31.2157118635612,1.48379742762378,306.762013284094));
#14667=CARTESIAN_POINT('Ctrl Pts',(-31.2627688624683,1.56436389260216,306.767047729422));
#14668=CARTESIAN_POINT('Ctrl Pts',(-31.3136820250735,1.64272351783683,306.77208217475));
#14669=CARTESIAN_POINT('Ctrl Pts',(-31.36820970196,1.71849202997719,306.777116620079));
#14670=CARTESIAN_POINT('Ctrl Pts',(-31.4227328050804,1.79425418667629,306.782150643119));
#14671=CARTESIAN_POINT('Ctrl Pts',(-31.4808695600314,1.86742530192697,306.78718466616));
#14672=CARTESIAN_POINT('Ctrl Pts',(-31.5423358257536,1.937651290867,306.7922186892));
#14673=CARTESIAN_POINT('Ctrl Pts',(-31.6038141304191,2.00789103445263,306.797253698217));
#14674=CARTESIAN_POINT('Ctrl Pts',(-31.6686229481257,2.0751841720915,306.802288707235));
#14675=CARTESIAN_POINT('Ctrl Pts',(-31.7364395896121,2.13921169179105,306.807323716252));
#14676=CARTESIAN_POINT('Ctrl Pts',(-31.8043307480469,2.20330956495084,306.812364257739));
#14677=CARTESIAN_POINT('Ctrl Pts',(-31.8752360038975,2.26413435212009,306.817404799226));
#14678=CARTESIAN_POINT('Ctrl Pts',(-31.9487979590096,2.32140596326777,306.822445340713));
#14679=CARTESIAN_POINT('Ctrl Pts',(-32.0224051094515,2.37871276120936,306.827488979031));
#14680=CARTESIAN_POINT('Ctrl Pts',(-32.0986718457472,2.43246178144004,306.832532617349));
#14681=CARTESIAN_POINT('Ctrl Pts',(-32.1772118517246,2.48241633792307,306.837576255666));
#14682=CARTESIAN_POINT('Ctrl Pts',(-32.255879031155,2.53245178176226,306.842628060738));
#14683=CARTESIAN_POINT('Ctrl Pts',(-32.3368264434786,2.5786802759391,306.84767986581));
#14684=CARTESIAN_POINT('Ctrl Pts',(-32.4196434369083,2.62091121903678,306.852731670882));
#14685=CARTESIAN_POINT('Ctrl Pts',(-32.4615649453431,2.64228829110816,306.855288866937));
#14686=CARTESIAN_POINT('Ctrl Pts',(-32.5039651833339,2.6626418269809,306.857846062993));
#14687=CARTESIAN_POINT('Ctrl Pts',(-32.5467892156698,2.68195191274964,306.860403259048));
#14688=CARTESIAN_POINT('Ctrl Pts',(-32.6313970706085,2.72010303599651,306.865455536032));
#14689=CARTESIAN_POINT('Ctrl Pts',(-32.7179639015626,2.75431501252238,306.870507813015));
#14690=CARTESIAN_POINT('Ctrl Pts',(-32.8060875247434,2.78438304610961,306.875560089999));
#14691=CARTESIAN_POINT('Ctrl Pts',(-32.8940896091405,2.81440961031446,306.880605398957));
#14692=CARTESIAN_POINT('Ctrl Pts',(-32.983643802389,2.84030344631984,306.885650707916));
#14693=CARTESIAN_POINT('Ctrl Pts',(-33.0743261287194,2.86190697568591,306.890696016875));
#14694=CARTESIAN_POINT('Ctrl Pts',(-33.1649114067385,2.88348738493448,306.895735926339));
#14695=CARTESIAN_POINT('Ctrl Pts',(-33.256621988251,2.90078651142073,306.900775835803));
#14696=CARTESIAN_POINT('Ctrl Pts',(-33.3490178975942,2.91369630506907,306.905815745267));
#14697=CARTESIAN_POINT('Ctrl Pts',(-33.4413472048798,2.92659679290694,306.910852021796));
#14698=CARTESIAN_POINT('Ctrl Pts',(-33.5343604193706,2.9351141754558,306.915888298325));
#14699=CARTESIAN_POINT('Ctrl Pts',(-33.6276075414581,2.93919151167186,306.920924574855));
#14700=CARTESIAN_POINT('Ctrl Pts',(-33.7208207565177,2.94326736526465,306.925959020065));
#14701=CARTESIAN_POINT('Ctrl Pts',(-33.8142672668187,2.94290636054046,306.930993465276));
#14702=CARTESIAN_POINT('Ctrl Pts',(-33.9074931608555,2.9381035197886,306.936027910487));
#14703=CARTESIAN_POINT('Ctrl Pts',(-34.0007112351353,2.93330108189743,306.94106193341));
#14704=CARTESIAN_POINT('Ctrl Pts',(-34.0937082862849,2.92405757179393,306.946095956333));
#14705=CARTESIAN_POINT('Ctrl Pts',(-34.1860327674912,2.91042008184293,306.951129979256));
#14706=CARTESIAN_POINT('Ctrl Pts',(-34.278375331619,2.89677992081641,306.956164988157));
#14707=CARTESIAN_POINT('Ctrl Pts',(-34.3700446247773,2.87874413603468,306.961199997057));
#14708=CARTESIAN_POINT('Ctrl Pts',(-34.4605977065936,2.85641122024437,306.966235005958));
#14709=CARTESIAN_POINT('Ctrl Pts',(-34.5512502881931,2.83405376503216,306.971275547329));
#14710=CARTESIAN_POINT('Ctrl Pts',(-34.6407837782241,2.80738986030109,306.9763160887));
#14711=CARTESIAN_POINT('Ctrl Pts',(-34.7287691577975,2.77656825632078,306.981356630072));
#14712=CARTESIAN_POINT('Ctrl Pts',(-34.8168085942416,2.74572771601869,306.986400268275));
#14713=CARTESIAN_POINT('Ctrl Pts',(-34.9032976151997,2.71072455764508,306.991443906477));
#14714=CARTESIAN_POINT('Ctrl Pts',(-34.9878280273348,2.67175534835848,306.99648754468));
#14715=CARTESIAN_POINT('Ctrl Pts',(-35.0724953127383,2.63272303937902,307.001539349639));
#14716=CARTESIAN_POINT('Ctrl Pts',(-35.1551972643274,2.58971206366467,307.006591154598));
#14717=CARTESIAN_POINT('Ctrl Pts',(-35.2355512495486,2.54296440489852,307.011642959557));
#14718=CARTESIAN_POINT('Ctrl Pts',(-35.2762260161533,2.51930098479069,307.014200156777));
#14719=CARTESIAN_POINT('Ctrl Pts',(-35.3162996289194,2.49468078638073,307.016757353997));
#14720=CARTESIAN_POINT('Ctrl Pts',(-35.3557255949467,2.46913920544158,307.019314551217));
#14721=CARTESIAN_POINT('Ctrl Pts',(-35.4335843309677,2.41869947223314,307.02436452623));
#14722=CARTESIAN_POINT('Ctrl Pts',(-35.5091953622117,2.364482524689,307.029414501244));
#14723=CARTESIAN_POINT('Ctrl Pts',(-35.5821689169263,2.30671519912427,307.034464476257));
#14724=CARTESIAN_POINT('Ctrl Pts',(-35.6550418028966,2.24902756495117,307.03950748471));
#14725=CARTESIAN_POINT('Ctrl Pts',(-35.7252840966099,2.18779955876853,307.044550493164));
#14726=CARTESIAN_POINT('Ctrl Pts',(-35.7925338978758,2.12330192133702,307.049593501617));
#14727=CARTESIAN_POINT('Ctrl Pts',(-35.8597117582939,2.05887328061074,307.054631115284));
#14728=CARTESIAN_POINT('Ctrl Pts',(-35.9239031698351,1.99118226687543,307.059668728952));
#14729=CARTESIAN_POINT('Ctrl Pts',(-35.9847791895293,1.92053990603867,307.064706342619));
#14730=CARTESIAN_POINT('Ctrl Pts',(-36.0456114286456,1.84994834949884,307.069740333355));
#14731=CARTESIAN_POINT('Ctrl Pts',(-36.1031327255531,1.7764100005162,307.07477432409));
#14732=CARTESIAN_POINT('Ctrl Pts',(-36.1570516650408,1.70027200002884,307.079808314826));
#14733=CARTESIAN_POINT('Ctrl Pts',(-36.2109510990481,1.62416154289233,307.084840484487));
#14734=CARTESIAN_POINT('Ctrl Pts',(-36.2612505077187,1.54545366506143,307.089872654149));
#14735=CARTESIAN_POINT('Ctrl Pts',(-36.3077000371575,1.46452694237562,307.09490482381));
#14736=CARTESIAN_POINT('Ctrl Pts',(-36.3541457898697,1.38360679969419,307.099936584315));
#14737=CARTESIAN_POINT('Ctrl Pts',(-36.3967420645186,1.30046855666009,307.104968344819));
#14738=CARTESIAN_POINT('Ctrl Pts',(-36.4352840609986,1.21551700022649,307.110000105324));
#14739=CARTESIAN_POINT('Ctrl Pts',(-36.4738337325948,1.13054852684173,307.115032867836));
#14740=CARTESIAN_POINT('Ctrl Pts',(-36.5083273392784,1.04376642805243,307.120065630348));
#14741=CARTESIAN_POINT('Ctrl Pts',(-36.5386079542234,0.955596086190086,
307.125098392859));
#14742=CARTESIAN_POINT('Ctrl Pts',(-36.5689218711038,0.86732877657978,307.130136690289));
#14743=CARTESIAN_POINT('Ctrl Pts',(-36.5950134032165,0.777670597661236,
307.135174987719));
#14744=CARTESIAN_POINT('Ctrl Pts',(-36.616775416527,0.6870624291343,307.140213285149));
#14745=CARTESIAN_POINT('Ctrl Pts',(-36.6385508920485,0.596398209438501,
307.145254699323));
#14746=CARTESIAN_POINT('Ctrl Pts',(-36.655991433999,0.50478326675529,307.150296113497));
#14747=CARTESIAN_POINT('Ctrl Pts',(-36.6690413856439,0.412666849959389,
307.155337527671));
#14748=CARTESIAN_POINT('Ctrl Pts',(-36.6821123812078,0.32040188928585,307.160387071462));
#14749=CARTESIAN_POINT('Ctrl Pts',(-36.6907786114471,0.227634282353497,
307.165436615253));
#14750=CARTESIAN_POINT('Ctrl Pts',(-36.6950364409153,0.134816343810574,
307.170486159045));
#14751=CARTESIAN_POINT('Ctrl Pts',(-36.6970988567292,0.0898570081459208,
307.172932067));
#14752=CARTESIAN_POINT('Ctrl Pts',(-36.698127730074,0.0448858346111718,
307.175377974955));
#14753=CARTESIAN_POINT('Ctrl Pts',(-36.6981270248953,-4.61727831956564E-5,
307.17782388291));
#14754=CARTESIAN_POINT('',(-36.6981258930304,0.00258108961789129,308.177823882867));
#14755=CARTESIAN_POINT('Ctrl Pts',(-36.6981270248952,-4.61761837817898E-5,
307.177823883095));
#14756=CARTESIAN_POINT('Ctrl Pts',(-36.6981269862627,-0.00250755018580523,
307.177957869859));
#14757=CARTESIAN_POINT('Ctrl Pts',(-36.6981238587313,-0.00496892131678009,
307.178091856623));
#14758=CARTESIAN_POINT('Ctrl Pts',(-36.6981176423178,-0.00743028464312453,
307.178225843386));
#14759=CARTESIAN_POINT('Ctrl Pts',(-36.6978832382483,-0.100241611014921,
307.183278120355));
#14760=CARTESIAN_POINT('Ctrl Pts',(-36.6932522120412,-0.193208428131717,
307.188330397323));
#14761=CARTESIAN_POINT('Ctrl Pts',(-36.6842043299577,-0.285879865852879,
307.193382674291));
#14762=CARTESIAN_POINT('Ctrl Pts',(-36.6751689265795,-0.378423492497563,
307.198427983234));
#14763=CARTESIAN_POINT('Ctrl Pts',(-36.661728815025,-0.470672110951617,
307.203473292176));
#14764=CARTESIAN_POINT('Ctrl Pts',(-36.6439157644718,-0.562174525986155,
307.208518601119));
#14765=CARTESIAN_POINT('Ctrl Pts',(-36.6261217774649,-0.653579015035336,
307.213558510567));
#14766=CARTESIAN_POINT('Ctrl Pts',(-36.603964237949,-0.744238454251292,
307.218598420014));
#14767=CARTESIAN_POINT('Ctrl Pts',(-36.5775266277404,-0.833707552508677,
307.223638329461));
#14768=CARTESIAN_POINT('Ctrl Pts',(-36.55110807465,-0.923112158432051,307.228674605973));
#14769=CARTESIAN_POINT('Ctrl Pts',(-36.520415708702,-1.01132770404676,307.233710882484));
#14770=CARTESIAN_POINT('Ctrl Pts',(-36.4855836934334,-1.09792089721922,
307.238747158995));
#14771=CARTESIAN_POINT('Ctrl Pts',(-36.4507643439771,-1.18448260289011,
307.243781604188));
#14772=CARTESIAN_POINT('Ctrl Pts',(-36.411808501228,-1.26942271632916,307.24881604938));
#14773=CARTESIAN_POINT('Ctrl Pts',(-36.3688992618611,-1.35232586296131,
307.253850494572));
#14774=CARTESIAN_POINT('Ctrl Pts',(-36.3259936217126,-1.4352220556942,307.258884517476));
#14775=CARTESIAN_POINT('Ctrl Pts',(-36.2791354486352,-1.51608122687307,
307.26391854038));
#14776=CARTESIAN_POINT('Ctrl Pts',(-36.2285542751424,-1.59451167886186,
307.268952563284));
#14777=CARTESIAN_POINT('Ctrl Pts',(-36.1779631946911,-1.67295749244054,
307.273987572165));
#14778=CARTESIAN_POINT('Ctrl Pts',(-36.1236479067135,-1.74897326897108,
307.279022581046));
#14779=CARTESIAN_POINT('Ctrl Pts',(-36.0658811896667,-1.82219639446329,
307.284057589926));
#14780=CARTESIAN_POINT('Ctrl Pts',(-36.0080509985243,-1.8954999775598,307.289098131277));
#14781=CARTESIAN_POINT('Ctrl Pts',(-35.9467620837555,-1.96600443507194,
307.294138672628));
#14782=CARTESIAN_POINT('Ctrl Pts',(-35.8823272320804,-2.03338060394674,
307.299179213979));
#14783=CARTESIAN_POINT('Ctrl Pts',(-35.8178527926249,-2.10079816770187,
307.30422285216));
#14784=CARTESIAN_POINT('Ctrl Pts',(-35.7502288901532,-2.16508331068846,
307.309266490342));
#14785=CARTESIAN_POINT('Ctrl Pts',(-35.6798032434156,-2.22594559854757,
307.314310128524));
#14786=CARTESIAN_POINT('Ctrl Pts',(-35.6092635621247,-2.28690643578653,
307.319361933461));
#14787=CARTESIAN_POINT('Ctrl Pts',(-35.535913428861,-2.34443307945525,307.324413738398));
#14788=CARTESIAN_POINT('Ctrl Pts',(-35.4601313513528,-2.39827714341962,
307.329465543335));
#14789=CARTESIAN_POINT('Ctrl Pts',(-35.4217708575259,-2.42553272879326,
307.332022740742));
#14790=CARTESIAN_POINT('Ctrl Pts',(-35.3827876459725,-2.45184542834557,
307.334579938149));
#14791=CARTESIAN_POINT('Ctrl Pts',(-35.3432331652808,-2.47718753837912,
307.337137135556));
#14792=CARTESIAN_POINT('Ctrl Pts',(-35.2650850369469,-2.52725616353908,
307.342189412508));
#14793=CARTESIAN_POINT('Ctrl Pts',(-35.1844250303688,-2.57371301198807,
307.34724168946));
#14794=CARTESIAN_POINT('Ctrl Pts',(-35.101621207914,-2.61629688767116,307.352293966412));
#14795=CARTESIAN_POINT('Ctrl Pts',(-35.0189315872691,-2.65882203230136,
307.357339275338));
#14796=CARTESIAN_POINT('Ctrl Pts',(-34.9341044177683,-2.69748461708392,
307.362384584264));
#14797=CARTESIAN_POINT('Ctrl Pts',(-34.8475361993156,-2.73206698577871,
307.367429893189));
#14798=CARTESIAN_POINT('Ctrl Pts',(-34.7610606262675,-2.76661234438371,
307.37246980262));
#14799=CARTESIAN_POINT('Ctrl Pts',(-34.6728481181416,-2.79708600235726,
307.377509712051));
#14800=CARTESIAN_POINT('Ctrl Pts',(-34.5833182186416,-2.82331697292174,
307.382549621482));
#14801=CARTESIAN_POINT('Ctrl Pts',(-34.4938528553049,-2.84952903532027,
307.387585897976));
#14802=CARTESIAN_POINT('Ctrl Pts',(-34.4030724132053,-2.87150436450133,
307.39262217447));
#14803=CARTESIAN_POINT('Ctrl Pts',(-34.3114137978876,-2.88912107744591,
307.397658450965));
#14804=CARTESIAN_POINT('Ctrl Pts',(-34.2197885119895,-2.90673138450255,
307.40269289614));
#14805=CARTESIAN_POINT('Ctrl Pts',(-34.1272861230806,-2.91998614013724,
307.407727341315));
#14806=CARTESIAN_POINT('Ctrl Pts',(-34.034354976131,-2.9288143005921,307.412761786491));
#14807=CARTESIAN_POINT('Ctrl Pts',(-33.9414316242277,-2.9376417205426,307.417795809378));
#14808=CARTESIAN_POINT('Ctrl Pts',(-33.8480800280715,-2.94204324171661,
307.422829832265));
#14809=CARTESIAN_POINT('Ctrl Pts',(-33.7547537779637,-2.94199967950234,
307.427863855152));
#14810=CARTESIAN_POINT('Ctrl Pts',(-33.6614092487365,-2.94195610875587,
307.432898864016));
#14811=CARTESIAN_POINT('Ctrl Pts',(-33.5680905196465,-2.93746572613335,
307.437933872879));
#14812=CARTESIAN_POINT('Ctrl Pts',(-33.4752501536014,-2.92856145282434,
307.442968881743));
#14813=CARTESIAN_POINT('Ctrl Pts',(-33.3823077745167,-2.91964739549547,
307.448009423077));
#14814=CARTESIAN_POINT('Ctrl Pts',(-33.2898452505994,-2.90630980881408,
307.453049964411));
#14815=CARTESIAN_POINT('Ctrl Pts',(-33.1983086925367,-2.88863336331915,
307.458090505745));
#14816=CARTESIAN_POINT('Ctrl Pts',(-33.1067158958218,-2.87094605768821,
307.46313414391));
#14817=CARTESIAN_POINT('Ctrl Pts',(-33.0160506289026,-2.84891469112421,
307.468177782075));
#14818=CARTESIAN_POINT('Ctrl Pts',(-32.9267453643008,-2.82267427459644,
307.47322142024));
#14819=CARTESIAN_POINT('Ctrl Pts',(-32.8372954949032,-2.79639136908337,
307.47827322516));
#14820=CARTESIAN_POINT('Ctrl Pts',(-32.7492104433979,-2.76588595274889,
307.483325030081));
#14821=CARTESIAN_POINT('Ctrl Pts',(-32.6629040097661,-2.73134169198941,
307.488376835001));
#14822=CARTESIAN_POINT('Ctrl Pts',(-32.6192161385537,-2.71385556550174,
307.490934032576));
#14823=CARTESIAN_POINT('Ctrl Pts',(-32.5759836400009,-2.69533529825264,
307.49349123015));
#14824=CARTESIAN_POINT('Ctrl Pts',(-32.5332576670678,-2.6758091360933,307.496048427725));
#14825=CARTESIAN_POINT('Ctrl Pts',(-32.4488435998329,-2.6372311318443,307.50110070467));
#14826=CARTESIAN_POINT('Ctrl Pts',(-32.3661053390023,-2.59458543339677,
307.506152981615));
#14827=CARTESIAN_POINT('Ctrl Pts',(-32.2854617960258,-2.54803998860467,
307.511205258559));
#14828=CARTESIAN_POINT('Ctrl Pts',(-32.2049294754365,-2.50155873860477,
307.516250567478));
#14829=CARTESIAN_POINT('Ctrl Pts',(-32.1264865133108,-2.45118865011795,
307.521295876397));
#14830=CARTESIAN_POINT('Ctrl Pts',(-32.0505306211471,-2.3971451575333,307.526341185316));
#14831=CARTESIAN_POINT('Ctrl Pts',(-31.9746560170669,-2.34315950235686,
307.531381094739));
#14832=CARTESIAN_POINT('Ctrl Pts',(-31.9012635525235,-2.28550851326651,
307.536421004163));
#14833=CARTESIAN_POINT('Ctrl Pts',(-31.8307241869542,-2.22445227196567,
307.541460913586));
#14834=CARTESIAN_POINT('Ctrl Pts',(-31.7602356685354,-2.16344004205998,
307.546497190073));
#14835=CARTESIAN_POINT('Ctrl Pts',(-31.6925964962286,-2.09902772875402,
307.55153346656));
#14836=CARTESIAN_POINT('Ctrl Pts',(-31.6281457537451,-2.03151660295753,
307.556569743047));
#14837=CARTESIAN_POINT('Ctrl Pts',(-31.5637184472036,-1.96403002593684,
307.561604188215));
#14838=CARTESIAN_POINT('Ctrl Pts',(-31.5024775736843,-1.89344719596045,
307.566638633383));
#14839=CARTESIAN_POINT('Ctrl Pts',(-31.4447256747144,-1.82010653443884,
307.571673078551));
#14840=CARTESIAN_POINT('Ctrl Pts',(-31.3869786199636,-1.74677202471912,
307.57670710143));
#14841=CARTESIAN_POINT('Ctrl Pts',(-31.332720232598,-1.67068049253143,307.581741124309));
#14842=CARTESIAN_POINT('Ctrl Pts',(-31.2822122999425,-1.59220285512531,
307.586775147189));
#14843=CARTESIAN_POINT('Ctrl Pts',(-31.2316944746746,-1.51370984688898,
307.591810156045));
#14844=CARTESIAN_POINT('Ctrl Pts',(-31.1849288030875,-1.4328301790294,307.596845164901));
#14845=CARTESIAN_POINT('Ctrl Pts',(-31.1421327137115,-1.34996212510011,
307.601880173757));
#14846=CARTESIAN_POINT('Ctrl Pts',(-31.0992895999725,-1.2670030157144,307.606920715083));
#14847=CARTESIAN_POINT('Ctrl Pts',(-31.0604249792384,-1.18205155439716,
307.611961256409));
#14848=CARTESIAN_POINT('Ctrl Pts',(-31.0257092828616,-1.09552861761311,
307.617001797735));
#14849=CARTESIAN_POINT('Ctrl Pts',(-30.9909722576959,-1.00895252246989,
307.622045435892));
#14850=CARTESIAN_POINT('Ctrl Pts',(-30.9603893770265,-0.920803449160516,
307.627089074049));
#14851=CARTESIAN_POINT('Ctrl Pts',(-30.9340813675908,-0.831518073191303,
307.632132712206));
#14852=CARTESIAN_POINT('Ctrl Pts',(-30.9077307597221,-0.742088124630835,
307.637184517118));
#14853=CARTESIAN_POINT('Ctrl Pts',(-30.8856689469274,-0.651518631324878,
307.64223632203));
#14854=CARTESIAN_POINT('Ctrl Pts',(-30.8679656412477,-0.560256923129221,
307.647288126943));
#14855=CARTESIAN_POINT('Ctrl Pts',(-30.859004319013,-0.514060716068839,
307.649845324593));
#14856=CARTESIAN_POINT('Ctrl Pts',(-30.8511589651056,-0.467687234591618,
307.652402522244));
#14857=CARTESIAN_POINT('Ctrl Pts',(-30.8444335387786,-0.42119477774019,
307.654959719894));
#14858=CARTESIAN_POINT('Ctrl Pts',(-30.8311460572966,-0.329339238860322,
307.660011996846));
#14859=CARTESIAN_POINT('Ctrl Pts',(-30.8221856536612,-0.236689432625149,
307.665064273798));
#14860=CARTESIAN_POINT('Ctrl Pts',(-30.8176380219122,-0.143688472809013,
307.67011655075));
#14861=CARTESIAN_POINT('Ctrl Pts',(-30.8130966621898,-0.0508157785451592,
307.675161859676));
#14862=CARTESIAN_POINT('Ctrl Pts',(-30.8129560021499,0.0424066670474889,
307.680207168603));
#14863=CARTESIAN_POINT('Ctrl Pts',(-30.8172503349368,0.135527853555428,
307.685252477529));
#14864=CARTESIAN_POINT('Ctrl Pts',(-30.8215400719239,0.228549381663997,
307.69029238696));
#14865=CARTESIAN_POINT('Ctrl Pts',(-30.8302553473273,0.321469424684481,
307.695332296391));
#14866=CARTESIAN_POINT('Ctrl Pts',(-30.8433784332003,0.413835280598431,
307.700372205822));
#14867=CARTESIAN_POINT('Ctrl Pts',(-30.8564920595112,0.50613455609483,307.705408482316));
#14868=CARTESIAN_POINT('Ctrl Pts',(-30.8740071186566,0.597879999925961,
307.710444758811));
#14869=CARTESIAN_POINT('Ctrl Pts',(-30.8958539937072,0.68862339851713,307.715481035305));
#14870=CARTESIAN_POINT('Ctrl Pts',(-30.9176929246743,0.77933380048399,307.72051548048));
#14871=CARTESIAN_POINT('Ctrl Pts',(-30.9438604384449,0.869042449589275,
307.725549925656));
#14872=CARTESIAN_POINT('Ctrl Pts',(-30.9742358969099,0.957311730848763,
307.730584370831));
#14873=CARTESIAN_POINT('Ctrl Pts',(-31.0046088074872,1.04557360809749,307.735618393718));
#14874=CARTESIAN_POINT('Ctrl Pts',(-31.0391888162568,1.13239593752782,307.740652416605));
#14875=CARTESIAN_POINT('Ctrl Pts',(-31.0778058956517,1.21735776446638,307.745686439492));
#14876=CARTESIAN_POINT('Ctrl Pts',(-31.1164305386866,1.30233623224597,307.750721448356));
#14877=CARTESIAN_POINT('Ctrl Pts',(-31.1590936385486,1.38545306956626,307.75575645722));
#14878=CARTESIAN_POINT('Ctrl Pts',(-31.2055781465145,1.46630979576026,307.760791466084));
#14879=CARTESIAN_POINT('Ctrl Pts',(-31.2521137316798,1.54725536736323,307.765832007417));
#14880=CARTESIAN_POINT('Ctrl Pts',(-31.3024788848182,1.62593548491534,307.770872548751));
#14881=CARTESIAN_POINT('Ctrl Pts',(-31.356412103035,1.70197893408303,307.775913090085));
#14882=CARTESIAN_POINT('Ctrl Pts',(-31.4103784569904,1.77806910317456,307.78095672825));
#14883=CARTESIAN_POINT('Ctrl Pts',(-31.4679169664322,1.85151902945579,307.786000366414));
#14884=CARTESIAN_POINT('Ctrl Pts',(-31.5287259275976,1.92199072582133,307.791044004579));
#14885=CARTESIAN_POINT('Ctrl Pts',(-31.5896333517975,1.99257653130713,307.7960958095));
#14886=CARTESIAN_POINT('Ctrl Pts',(-31.6538214941681,2.06017415778127,307.80114761442));
#14887=CARTESIAN_POINT('Ctrl Pts',(-31.7209520654008,2.12448273298979,307.80619941934));
#14888=CARTESIAN_POINT('Ctrl Pts',(-31.754933214046,2.15703540181405,307.808756616914));
#14889=CARTESIAN_POINT('Ctrl Pts',(-31.7896677842723,2.18874594992559,307.811313814489));
#14890=CARTESIAN_POINT('Ctrl Pts',(-31.8251089117024,2.21957947483792,307.813871012063));
#14891=CARTESIAN_POINT('Ctrl Pts',(-31.8951302479454,2.28049753168308,307.818923289013));
#14892=CARTESIAN_POINT('Ctrl Pts',(-31.9681627809449,2.33820822865134,307.823975565963));
#14893=CARTESIAN_POINT('Ctrl Pts',(-32.043880421301,2.3923995417236,307.829027842913));
#14894=CARTESIAN_POINT('Ctrl Pts',(-32.1194936330039,2.44651611493576,307.834073151837));
#14895=CARTESIAN_POINT('Ctrl Pts',(-32.1977842350866,2.49712269321824,307.839118460761));
#14896=CARTESIAN_POINT('Ctrl Pts',(-32.2783916616912,2.5439461856072,307.844163769685));
#14897=CARTESIAN_POINT('Ctrl Pts',(-32.3589128221362,2.59071956744134,307.849203679114));
#14898=CARTESIAN_POINT('Ctrl Pts',(-32.4417454967018,2.63371768876346,307.854243588543));
#14899=CARTESIAN_POINT('Ctrl Pts',(-32.5264995233976,2.6727102736117,307.859283497971));
#14900=CARTESIAN_POINT('Ctrl Pts',(-32.6111924565383,2.71167475129234,307.864319774464));
#14901=CARTESIAN_POINT('Ctrl Pts',(-32.6978035865456,2.74663924631596,307.869356050956));
#14902=CARTESIAN_POINT('Ctrl Pts',(-32.7859184220596,2.77741953371839,307.874392327449));
#14903=CARTESIAN_POINT('Ctrl Pts',(-32.8740012167619,2.80818862861977,307.879426772622));
#14904=CARTESIAN_POINT('Ctrl Pts',(-32.9635862117413,2.83477639213306,307.884461217795));
#14905=CARTESIAN_POINT('Ctrl Pts',(-33.0542401927121,2.8570472299735,307.889495662968));
#14906=CARTESIAN_POINT('Ctrl Pts',(-33.1448865696438,2.87931619974021,307.894529685853));
#14907=CARTESIAN_POINT('Ctrl Pts',(-33.2366013228173,2.89726885796858,307.899563708738));
#14908=CARTESIAN_POINT('Ctrl Pts',(-33.328938494487,2.91082015232443,307.904597731623));
#14909=CARTESIAN_POINT('Ctrl Pts',(-33.4212937515515,2.92437410087149,307.909632740484));
#14910=CARTESIAN_POINT('Ctrl Pts',(-33.5142712296474,2.93352490934955,307.914667749346));
#14911=CARTESIAN_POINT('Ctrl Pts',(-33.6074183974593,2.93823922511738,307.919702758207));
#14912=CARTESIAN_POINT('Ctrl Pts',(-33.7006679154236,2.94295872097761,307.924743299539));
#14913=CARTESIAN_POINT('Ctrl Pts',(-33.7940870509152,2.94323197091793,307.929783840871));
#14914=CARTESIAN_POINT('Ctrl Pts',(-33.8872221179377,2.93907775954894,307.934824382202));
#14915=CARTESIAN_POINT('Ctrl Pts',(-33.9804144057108,2.93492099589646,307.939868020365));
#14916=CARTESIAN_POINT('Ctrl Pts',(-34.0733218355228,2.92633139648949,307.944911658527));
#14917=CARTESIAN_POINT('Ctrl Pts',(-34.1654968812254,2.91337953604142,307.94995529669));
#14918=CARTESIAN_POINT('Ctrl Pts',(-34.2578211785276,2.90040670369281,307.955007101608));
#14919=CARTESIAN_POINT('Ctrl Pts',(-34.3494102882879,2.88305759155798,307.960058906526));
#14920=CARTESIAN_POINT('Ctrl Pts',(-34.4398280703308,2.86145363075585,307.965110711444));
#14921=CARTESIAN_POINT('Ctrl Pts',(-34.4855970852982,2.85051781721379,307.96766790904));
#14922=CARTESIAN_POINT('Ctrl Pts',(-34.5310662230126,2.83849256113043,307.970225106637));
#14923=CARTESIAN_POINT('Ctrl Pts',(-34.5761807616741,2.82539835587645,307.972782304233));
#14924=CARTESIAN_POINT('Ctrl Pts',(-34.6653139378073,2.7995280236542,307.977834581183));
#14925=CARTESIAN_POINT('Ctrl Pts',(-34.7533817034997,2.76938927675325,307.982886858132));
#14926=CARTESIAN_POINT('Ctrl Pts',(-34.8399451512711,2.73508725084313,307.987939135081));
#14927=CARTESIAN_POINT('Ctrl Pts',(-34.9263892120112,2.70083253378156,307.992984444005));
#14928=CARTESIAN_POINT('Ctrl Pts',(-35.0113326681612,2.66242610990136,307.998029752928));
#14929=CARTESIAN_POINT('Ctrl Pts',(-35.0943506689344,2.62002318300898,308.003075061852));
#14930=CARTESIAN_POINT('Ctrl Pts',(-35.1772798237484,2.57766563577736,308.00811497128));
#14931=CARTESIAN_POINT('Ctrl Pts',(-35.258287225477,2.53132028783189,308.013154880708));
#14932=CARTESIAN_POINT('Ctrl Pts',(-35.336967986493,2.48119041092786,308.018194790136));
#14933=CARTESIAN_POINT('Ctrl Pts',(-35.4155920317679,2.43109666932659,308.023231066628));
#14934=CARTESIAN_POINT('Ctrl Pts',(-35.4918923962477,2.37722405910758,308.02826734312));
#14935=CARTESIAN_POINT('Ctrl Pts',(-35.5654897282066,2.31982124509135,308.033303619612));
#14936=CARTESIAN_POINT('Ctrl Pts',(-35.6390602982899,2.262439304209,308.038338064784));
#14937=CARTESIAN_POINT('Ctrl Pts',(-35.7099294385199,2.20152998262855,308.043372509957));
#14938=CARTESIAN_POINT('Ctrl Pts',(-35.7777485380565,2.13738402234807,308.04840695513));
#14939=CARTESIAN_POINT('Ctrl Pts',(-35.8455619489394,2.07324344261896,308.053440978014));
#14940=CARTESIAN_POINT('Ctrl Pts',(-35.9103255051623,2.00586706938051,308.058475000898));
#14941=CARTESIAN_POINT('Ctrl Pts',(-35.9717261818855,1.93558373033819,308.063509023782));
#14942=CARTESIAN_POINT('Ctrl Pts',(-36.0331388847023,1.86528662542124,308.068544032643));
#14943=CARTESIAN_POINT('Ctrl Pts',(-36.0911871079274,1.79208175872787,308.073579041504));
#14944=CARTESIAN_POINT('Ctrl Pts',(-36.1455977275192,1.71633148401857,308.078614050365));
#14945=CARTESIAN_POINT('Ctrl Pts',(-36.2000681335256,1.64049797487165,308.083654591696));
#14946=CARTESIAN_POINT('Ctrl Pts',(-36.2508926978361,1.56211383615403,308.088695133027));
#14947=CARTESIAN_POINT('Ctrl Pts',(-36.2978414998532,1.48157062930902,308.093735674358));
#14948=CARTESIAN_POINT('Ctrl Pts',(-36.3448191464911,1.4009779379584,308.09877931252));
#14949=CARTESIAN_POINT('Ctrl Pts',(-36.387916085266,1.31822393141601,308.103822950682));
#14950=CARTESIAN_POINT('Ctrl Pts',(-36.4269492686713,1.23372304188852,308.108866588844));
#14951=CARTESIAN_POINT('Ctrl Pts',(-36.4660456553548,1.14908532690217,308.113918393761));
#14952=CARTESIAN_POINT('Ctrl Pts',(-36.5010649836003,1.06269549320563,308.118970198679));
#14953=CARTESIAN_POINT('Ctrl Pts',(-36.5318731245027,0.974985944783638,
308.124022003596));
#14954=CARTESIAN_POINT('Ctrl Pts',(-36.5474680465801,0.930587823604574,
308.126579201198));
#14955=CARTESIAN_POINT('Ctrl Pts',(-36.5619847260853,0.885851761033045,
308.1291363988));
#14956=CARTESIAN_POINT('Ctrl Pts',(-36.5754107538507,0.84083485756132,308.131693596402));
#14957=CARTESIAN_POINT('Ctrl Pts',(-36.6081304217728,0.731127194340305,
308.137925570431));
#14958=CARTESIAN_POINT('Ctrl Pts',(-36.6344647399623,0.619433443808255,
308.144157544461));
#14959=CARTESIAN_POINT('Ctrl Pts',(-36.6542128972751,0.506421048548363,
308.15038951849));
#14960=CARTESIAN_POINT('Ctrl Pts',(-36.6736758184333,0.395040968674961,
308.156531479852));
#14961=CARTESIAN_POINT('Ctrl Pts',(-36.6867414406795,0.282380013901316,
308.162673441214));
#14962=CARTESIAN_POINT('Ctrl Pts',(-36.6932633563957,0.169098114443563,
308.168815402576));
#14963=CARTESIAN_POINT('Ctrl Pts',(-36.6964519441951,0.113714190729772,
308.17181822934));
#14964=CARTESIAN_POINT('Ctrl Pts',(-36.6980771128039,0.0581821699086846,
308.174821056104));
#14965=CARTESIAN_POINT('Ctrl Pts',(-36.6981258930304,0.00258108961789325,
308.177823882867));
#14966=CARTESIAN_POINT('',(-36.6981267404242,-0.00129458858357652,309.177823882939));
#14967=CARTESIAN_POINT('Ctrl Pts',(-36.6981258930311,0.00258108883062432,
308.17782388291));
#14968=CARTESIAN_POINT('Ctrl Pts',(-36.6982071222146,-0.0900062577063865,
308.182824213132));
#14969=CARTESIAN_POINT('Ctrl Pts',(-36.6939133701504,-0.182678244833167,
308.187824543354));
#14970=CARTESIAN_POINT('Ctrl Pts',(-36.6852474248329,-0.274986699299511,
308.192824873577));
#14971=CARTESIAN_POINT('Ctrl Pts',(-36.6765849946573,-0.367257710958717,
308.197823175529));
#14972=CARTESIAN_POINT('Ctrl Pts',(-36.6635539350238,-0.459165034091684,
308.202821477483));
#14973=CARTESIAN_POINT('Ctrl Pts',(-36.6462090565882,-0.550263438890801,
308.207819779435));
#14974=CARTESIAN_POINT('Ctrl Pts',(-36.6288661880875,-0.641351287152581,
308.212817502182));
#14975=CARTESIAN_POINT('Ctrl Pts',(-36.6072105787433,-0.731629960143632,
308.217815224929));
#14976=CARTESIAN_POINT('Ctrl Pts',(-36.5813483292237,-0.820663502061557,
308.222812947676));
#14977=CARTESIAN_POINT('Ctrl Pts',(-36.5554815829753,-0.909712524446245,
308.227811539388));
#14978=CARTESIAN_POINT('Ctrl Pts',(-36.5254068711011,-0.99751555287184,
308.2328101311));
#14979=CARTESIAN_POINT('Ctrl Pts',(-36.491280062755,-1.08365209429455,308.237808722813));
#14980=CARTESIAN_POINT('Ctrl Pts',(-36.4571158737413,-1.16988298504469,
308.242812789713));
#14981=CARTESIAN_POINT('Ctrl Pts',(-36.4188908962147,-1.25444332544956,
308.247816856613));
#14982=CARTESIAN_POINT('Ctrl Pts',(-36.3768088818397,-1.33693328426721,
308.252820923514));
#14983=CARTESIAN_POINT('Ctrl Pts',(-36.3347011113665,-1.41947373067443,
308.25782805313));
#14984=CARTESIAN_POINT('Ctrl Pts',(-36.2887318303635,-1.4999408827083,308.262835182746));
#14985=CARTESIAN_POINT('Ctrl Pts',(-36.2391492620189,-1.57796215789515,
308.267842312361));
#14986=CARTESIAN_POINT('Ctrl Pts',(-36.1894851734741,-1.65611171022004,
308.272857674351));
#14987=CARTESIAN_POINT('Ctrl Pts',(-36.1361961997231,-1.73180699119541,
308.27787303634));
#14988=CARTESIAN_POINT('Ctrl Pts',(-36.0795719503602,-1.8047070898112,308.282888398329));
#14989=CARTESIAN_POINT('Ctrl Pts',(-36.0505318087128,-1.84209441438916,
308.285460561743));
#14990=CARTESIAN_POINT('Ctrl Pts',(-36.0206150366796,-1.87874711751359,
308.288032725157));
#14991=CARTESIAN_POINT('Ctrl Pts',(-35.989864380682,-1.91462305088542,308.290604888572));
#14992=CARTESIAN_POINT('Ctrl Pts',(-35.9294635408192,-1.98509102746083,
308.295657165522));
#14993=CARTESIAN_POINT('Ctrl Pts',(-35.8656164209312,-2.05282448081025,
308.300709442472));
#14994=CARTESIAN_POINT('Ctrl Pts',(-35.798600181269,-2.11746721508803,308.305761719422));
#14995=CARTESIAN_POINT('Ctrl Pts',(-35.7316763694166,-2.18202079505965,
308.310807028346));
#14996=CARTESIAN_POINT('Ctrl Pts',(-35.6615924401032,-2.24349182068722,
308.31585233727));
#14997=CARTESIAN_POINT('Ctrl Pts',(-35.588665333503,-2.30155759189577,308.320897646194));
#14998=CARTESIAN_POINT('Ctrl Pts',(-35.5158162735753,-2.35956122104986,
308.325937555622));
#14999=CARTESIAN_POINT('Ctrl Pts',(-35.4401304300073,-2.41416656415945,
308.330977465051));
#15000=CARTESIAN_POINT('Ctrl Pts',(-35.3619602600894,-2.46508896835582,
308.33601737448));
#15001=CARTESIAN_POINT('Ctrl Pts',(-35.2838464378613,-2.51597466596913,
308.341053650972));
#15002=CARTESIAN_POINT('Ctrl Pts',(-35.2032522198908,-2.56318245963645,
308.346089927464));
#15003=CARTESIAN_POINT('Ctrl Pts',(-35.1205608413697,-2.60646971235993,
308.351126203956));
#15004=CARTESIAN_POINT('Ctrl Pts',(-35.0378995315525,-2.6497412247293,308.356160649129));
#15005=CARTESIAN_POINT('Ctrl Pts',(-34.9531429693265,-2.68909482245021,
308.361195094303));
#15006=CARTESIAN_POINT('Ctrl Pts',(-34.8666999969098,-2.72433325322649,
308.366229539476));
#15007=CARTESIAN_POINT('Ctrl Pts',(-34.7802642753136,-2.75956872820971,
308.371263562361));
#15008=CARTESIAN_POINT('Ctrl Pts',(-34.6921428362306,-2.79068955501309,
308.376297585245));
#15009=CARTESIAN_POINT('Ctrl Pts',(-34.6027644916219,-2.81754662792797,
308.38133160813));
#15010=CARTESIAN_POINT('Ctrl Pts',(-34.513368641142,-2.84440896113784,308.386366616991));
#15011=CARTESIAN_POINT('Ctrl Pts',(-34.4227158217651,-2.86700575444401,
308.391401625853));
#15012=CARTESIAN_POINT('Ctrl Pts',(-34.3312488797567,-2.88523809285777,
308.396436634714));
#15013=CARTESIAN_POINT('Ctrl Pts',(-34.2396814338288,-2.90349046497365,
308.401477176046));
#15014=CARTESIAN_POINT('Ctrl Pts',(-34.1472985159844,-2.91736872250044,
308.406517717377));
#15015=CARTESIAN_POINT('Ctrl Pts',(-34.0545517094405,-2.92682536340492,
308.411558258709));
#15016=CARTESIAN_POINT('Ctrl Pts',(-33.9617479206874,-2.9362878143239,308.416601896871));
#15017=CARTESIAN_POINT('Ctrl Pts',(-33.868580241436,-2.94132321649804,308.421645535034));
#15018=CARTESIAN_POINT('Ctrl Pts',(-33.775501704775,-2.94193620287619,308.426689173196));
#15019=CARTESIAN_POINT('Ctrl Pts',(-33.6822724535647,-2.94255018181363,
308.431740978114));
#15020=CARTESIAN_POINT('Ctrl Pts',(-33.5891330764316,-2.93872746737211,
308.436792783032));
#15021=CARTESIAN_POINT('Ctrl Pts',(-33.4965327499461,-2.9305246650089,308.44184458795));
#15022=CARTESIAN_POINT('Ctrl Pts',(-33.4496589422253,-2.92637244875505,
308.444401785547));
#15023=CARTESIAN_POINT('Ctrl Pts',(-33.4029231193229,-2.92109872832869,
308.446958983144));
#15024=CARTESIAN_POINT('Ctrl Pts',(-33.3563824045443,-2.91471580745203,
308.449516180741));
#15025=CARTESIAN_POINT('Ctrl Pts',(-33.264431520192,-2.90210501661758,308.454568457691));
#15026=CARTESIAN_POINT('Ctrl Pts',(-33.1729129228356,-2.88511614501208,
308.459620734641));
#15027=CARTESIAN_POINT('Ctrl Pts',(-33.0822761531534,-2.86378927335172,
308.46467301159));
#15028=CARTESIAN_POINT('Ctrl Pts',(-32.9917643883678,-2.84249181539838,
308.469718320514));
#15029=CARTESIAN_POINT('Ctrl Pts',(-32.9021324631982,-2.81686834705423,
308.474763629438));
#15030=CARTESIAN_POINT('Ctrl Pts',(-32.8138233047469,-2.78701053071416,
308.479808938362));
#15031=CARTESIAN_POINT('Ctrl Pts',(-32.7256086548571,-2.75718466824303,
308.484848847791));
#15032=CARTESIAN_POINT('Ctrl Pts',(-32.6387143765055,-2.72313360655016,
308.48988875722));
#15033=CARTESIAN_POINT('Ctrl Pts',(-32.5535706483933,-2.68499947122209,
308.494928666648));
#15034=CARTESIAN_POINT('Ctrl Pts',(-32.4684882947465,-2.64689282426248,
308.499964943141));
#15035=CARTESIAN_POINT('Ctrl Pts',(-32.385154387507,-2.60470913479207,308.505001219633));
#15036=CARTESIAN_POINT('Ctrl Pts',(-32.3039804540349,-2.5586391569907,308.510037496125));
#15037=CARTESIAN_POINT('Ctrl Pts',(-32.2228360374847,-2.51258593141363,
308.515071941298));
#15038=CARTESIAN_POINT('Ctrl Pts',(-32.1438504203556,-2.46264944394638,
308.520106386471));
#15039=CARTESIAN_POINT('Ctrl Pts',(-32.0674108461888,-2.40906655502732,
308.525140831644));
#15040=CARTESIAN_POINT('Ctrl Pts',(-31.9909776837593,-2.3554881606311,308.530174854529));
#15041=CARTESIAN_POINT('Ctrl Pts',(-31.9170905033577,-2.29826422805754,
308.535208877414));
#15042=CARTESIAN_POINT('Ctrl Pts',(-31.8461068898516,-2.23767448087155,
308.540242900298));
#15043=CARTESIAN_POINT('Ctrl Pts',(-31.775109373313,-2.17707286642237,308.54527790916));
#15044=CARTESIAN_POINT('Ctrl Pts',(-31.7070168907496,-2.1131044168003,308.550312918021));
#15045=CARTESIAN_POINT('Ctrl Pts',(-31.6421524353964,-2.04608783619408,
308.555347926883));
#15046=CARTESIAN_POINT('Ctrl Pts',(-31.5772167069492,-1.97899761773754,
308.560388468214));
#15047=CARTESIAN_POINT('Ctrl Pts',(-31.5155163953081,-1.90885290243605,
308.565429009546));
#15048=CARTESIAN_POINT('Ctrl Pts',(-31.4573360056194,-1.83600758387077,
308.570469550877));
#15049=CARTESIAN_POINT('Ctrl Pts',(-31.3991198707955,-1.7631175102638,308.575513189039));
#15050=CARTESIAN_POINT('Ctrl Pts',(-31.3444282234248,-1.68752388989831,
308.580556827202));
#15051=CARTESIAN_POINT('Ctrl Pts',(-31.2935025269897,-1.60961007095846,
308.585600465364));
#15052=CARTESIAN_POINT('Ctrl Pts',(-31.2424943706916,-1.53157009247067,
308.590652270282));
#15053=CARTESIAN_POINT('Ctrl Pts',(-31.1952645638429,-1.45120279773318,
308.5957040752));
#15054=CARTESIAN_POINT('Ctrl Pts',(-31.1520087909573,-1.36891644076053,
308.600755880118));
#15055=CARTESIAN_POINT('Ctrl Pts',(-31.130112941793,-1.32726351121248,308.603313077715));
#15056=CARTESIAN_POINT('Ctrl Pts',(-31.1092346082724,-1.28511918230092,
308.605870275313));
#15057=CARTESIAN_POINT('Ctrl Pts',(-31.0893943847638,-1.24253813789563,
308.60842747291));
#15058=CARTESIAN_POINT('Ctrl Pts',(-31.0501958871502,-1.15841040784325,
308.61347974986));
#15059=CARTESIAN_POINT('Ctrl Pts',(-31.0149119140892,-1.07227495250789,
308.61853202681));
#15060=CARTESIAN_POINT('Ctrl Pts',(-30.9837522386971,-0.984531382356039,
308.62358430376));
#15061=CARTESIAN_POINT('Ctrl Pts',(-30.95263553827,-0.896908826842626,308.628629612684));
#15062=CARTESIAN_POINT('Ctrl Pts',(-30.9256319797742,-0.807682978746629,
308.633674921608));
#15063=CARTESIAN_POINT('Ctrl Pts',(-30.9029043927106,-0.717275824994563,
308.638720230532));
#15064=CARTESIAN_POINT('Ctrl Pts',(-30.8802011287366,-0.626965425081251,
308.643760139961));
#15065=CARTESIAN_POINT('Ctrl Pts',(-30.8617648481379,-0.53547666090447,
308.648800049389));
#15066=CARTESIAN_POINT('Ctrl Pts',(-30.8477090544894,-0.443248132892643,
308.653839958818));
#15067=CARTESIAN_POINT('Ctrl Pts',(-30.8336633927302,-0.351086086308426,
308.65887623531));
#15068=CARTESIAN_POINT('Ctrl Pts',(-30.8239920084853,-0.258185773713838,
308.663912511803));
#15069=CARTESIAN_POINT('Ctrl Pts',(-30.8187574246728,-0.164996453174808,
308.668948788295));
#15070=CARTESIAN_POINT('Ctrl Pts',(-30.813524744289,-0.0718410186604065,
308.673983233468));
#15071=CARTESIAN_POINT('Ctrl Pts',(-30.8127256841677,0.0216027719144301,
308.679017678641));
#15072=CARTESIAN_POINT('Ctrl Pts',(-30.8163708564597,0.114881103819076,
308.684052123814));
#15073=CARTESIAN_POINT('Ctrl Pts',(-30.8200157229953,0.208151611554675,
308.689086146699));
#15074=CARTESIAN_POINT('Ctrl Pts',(-30.8281040632372,0.301256244303458,
308.694120169584));
#15075=CARTESIAN_POINT('Ctrl Pts',(-30.8405943939178,0.393742905450918,
308.699154192469));
#15076=CARTESIAN_POINT('Ctrl Pts',(-30.8530871709866,0.486247681272225,
308.70418920133));
#15077=CARTESIAN_POINT('Ctrl Pts',(-30.8699835909764,0.578133804927413,
308.709224210192));
#15078=CARTESIAN_POINT('Ctrl Pts',(-30.8911906673589,0.668957147498904,
308.714259219053));
#15079=CARTESIAN_POINT('Ctrl Pts',(-30.912421046087,0.759880286802425,308.719299760385));
#15080=CARTESIAN_POINT('Ctrl Pts',(-30.9379714347535,0.849737880697215,
308.724340301716));
#15081=CARTESIAN_POINT('Ctrl Pts',(-30.9676984203594,0.93809909678332,308.729380843048));
#15082=CARTESIAN_POINT('Ctrl Pts',(-30.9974436697674,1.02651460063949,308.734424481211));
#15083=CARTESIAN_POINT('Ctrl Pts',(-31.0313704631717,1.11343148289836,308.739468119373));
#15084=CARTESIAN_POINT('Ctrl Pts',(-31.0692873158421,1.19843914151204,308.744511757536));
#15085=CARTESIAN_POINT('Ctrl Pts',(-31.1072655642066,1.28358444615482,308.749563562454));
#15086=CARTESIAN_POINT('Ctrl Pts',(-31.1492465701699,1.36681395929135,308.754615367372));
#15087=CARTESIAN_POINT('Ctrl Pts',(-31.1949931186672,1.44774207389058,308.75966717229));
#15088=CARTESIAN_POINT('Ctrl Pts',(-31.218149785594,1.48870746814093,308.762224369886));
#15089=CARTESIAN_POINT('Ctrl Pts',(-31.2422706200595,1.52908363206688,308.764781567483));
#15090=CARTESIAN_POINT('Ctrl Pts',(-31.2673208061614,1.56882363692934,308.767338765079));
#15091=CARTESIAN_POINT('Ctrl Pts',(-31.3168126710084,1.64733830111873,308.772391042029));
#15092=CARTESIAN_POINT('Ctrl Pts',(-31.3701123826518,1.72364961194092,308.777443318979));
#15093=CARTESIAN_POINT('Ctrl Pts',(-31.4269976224083,1.79736480014019,308.782495595929));
#15094=CARTESIAN_POINT('Ctrl Pts',(-31.4838044068807,1.87097832143846,308.787540904853));
#15095=CARTESIAN_POINT('Ctrl Pts',(-31.5441866238552,1.94200248643167,308.792586213777));
#15096=CARTESIAN_POINT('Ctrl Pts',(-31.6078777198504,2.01007186981402,308.797631522701));
#15097=CARTESIAN_POINT('Ctrl Pts',(-31.6715006535621,2.07806840526463,308.80267143213));
#15098=CARTESIAN_POINT('Ctrl Pts',(-31.7384251257932,2.14311612182166,308.807711341559));
#15099=CARTESIAN_POINT('Ctrl Pts',(-31.8083439026182,2.20488206196187,308.812751250987));
#15100=CARTESIAN_POINT('Ctrl Pts',(-31.8782122796357,2.26660347913357,308.817787527479));
#15101=CARTESIAN_POINT('Ctrl Pts',(-31.9510703391439,2.32504752859942,308.822823803972));
#15102=CARTESIAN_POINT('Ctrl Pts',(-32.0265742773425,2.37991833729216,308.827860080464));
#15103=CARTESIAN_POINT('Ctrl Pts',(-32.1020507603748,2.43476919355305,308.832894525637));
#15104=CARTESIAN_POINT('Ctrl Pts',(-32.1801708517482,2.48604912937403,308.83792897081));
#15105=CARTESIAN_POINT('Ctrl Pts',(-32.2605588027884,2.53350344225939,308.842963415984));
#15106=CARTESIAN_POINT('Ctrl Pts',(-32.3409400109021,2.58095377468577,308.847997438868));
#15107=CARTESIAN_POINT('Ctrl Pts',(-32.4235883178011,2.62457889650524,308.853031461753));
#15108=CARTESIAN_POINT('Ctrl Pts',(-32.5081012047816,2.66416882937724,308.858065484638));
#15109=CARTESIAN_POINT('Ctrl Pts',(-32.5926306446725,2.70376651643478,308.8631004935));
#15110=CARTESIAN_POINT('Ctrl Pts',(-32.6790249875007,2.73932725681039,308.868135502361));
#15111=CARTESIAN_POINT('Ctrl Pts',(-32.7668605189049,2.7706886832354,308.873170511222));
#15112=CARTESIAN_POINT('Ctrl Pts',(-32.8547925640327,2.80208456961065,308.878211052554));
#15113=CARTESIAN_POINT('Ctrl Pts',(-32.9441685397122,2.82927178191354,308.883251593885));
#15114=CARTESIAN_POINT('Ctrl Pts',(-33.0345485987383,2.85213754478671,308.888292135217));
#15115=CARTESIAN_POINT('Ctrl Pts',(-33.1249841858805,2.87501735603237,308.893335773379));
#15116=CARTESIAN_POINT('Ctrl Pts',(-33.2164246494203,2.89357034392718,308.898379411542));
#15117=CARTESIAN_POINT('Ctrl Pts',(-33.30842111349,2.90773510082476,308.903423049704));
#15118=CARTESIAN_POINT('Ctrl Pts',(-33.4005665399964,2.921922793568,308.908474854623));
#15119=CARTESIAN_POINT('Ctrl Pts',(-33.4932693230957,2.93170802346448,308.91352665954));
#15120=CARTESIAN_POINT('Ctrl Pts',(-33.586076831716,2.93708136279478,308.918578464459));
#15121=CARTESIAN_POINT('Ctrl Pts',(-33.6330555139631,2.939801319453,308.921135662055));
#15122=CARTESIAN_POINT('Ctrl Pts',(-33.680061047337,2.94139163438224,308.923692859652));
#15123=CARTESIAN_POINT('Ctrl Pts',(-33.7270351255883,2.94185615919161,308.926250057249));
#15124=CARTESIAN_POINT('Ctrl Pts',(-33.8198422098282,2.9427739247917,308.931302334199));
#15125=CARTESIAN_POINT('Ctrl Pts',(-33.9128593521207,2.93929733732222,308.936354611149));
#15126=CARTESIAN_POINT('Ctrl Pts',(-34.00563596825,2.9314005675388,308.941406888099));
#15127=CARTESIAN_POINT('Ctrl Pts',(-34.0982846282381,2.92351468886386,308.946452197023));
#15128=CARTESIAN_POINT('Ctrl Pts',(-34.1906929824389,2.91122077924747,308.951497505947));
#15129=CARTESIAN_POINT('Ctrl Pts',(-34.2824094760139,2.89454500431863,308.956542814871));
#15130=CARTESIAN_POINT('Ctrl Pts',(-34.3740278144935,2.87788707582303,308.9615827243));
#15131=CARTESIAN_POINT('Ctrl Pts',(-34.4649553293214,2.85685668210224,308.966622633728));
#15132=CARTESIAN_POINT('Ctrl Pts',(-34.5547457273513,2.83153177073226,308.971662543157));
#15133=CARTESIAN_POINT('Ctrl Pts',(-34.6444714014394,2.80622511441097,308.976698819649));
#15134=CARTESIAN_POINT('Ctrl Pts',(-34.7330611615965,2.77663021369175,308.981735096142));
#15135=CARTESIAN_POINT('Ctrl Pts',(-34.8200800835844,2.74287584292052,308.986771372634));
#15136=CARTESIAN_POINT('Ctrl Pts',(-34.9070673632628,2.70913374610333,308.991805817807));
#15137=CARTESIAN_POINT('Ctrl Pts',(-34.9924845257453,2.67123534445613,308.99684026298));
#15138=CARTESIAN_POINT('Ctrl Pts',(-35.0759139555198,2.62935856411959,309.001874708153));
#15139=CARTESIAN_POINT('Ctrl Pts',(-35.1593363872495,2.58748529639949,309.006908731038));
#15140=CARTESIAN_POINT('Ctrl Pts',(-35.2407710208066,2.54163451293277,309.011942753923));
#15141=CARTESIAN_POINT('Ctrl Pts',(-35.319823339343,2.49203086604394,309.016976776808));
#15142=CARTESIAN_POINT('Ctrl Pts',(-35.3988911412688,2.44241750365789,309.022011785669));
#15143=CARTESIAN_POINT('Ctrl Pts',(-35.4755753254025,2.38905005447213,309.02704679453));
#15144=CARTESIAN_POINT('Ctrl Pts',(-35.5495099194493,2.33219677446405,309.032081803392));
#15145=CARTESIAN_POINT('Ctrl Pts',(-35.6235257528628,2.27528102404519,309.037122344723));
#15146=CARTESIAN_POINT('Ctrl Pts',(-35.6947856126963,2.21487206843455,309.042162886055));
#15147=CARTESIAN_POINT('Ctrl Pts',(-35.7629564783556,2.15127858404679,309.047203427386));
#15148=CARTESIAN_POINT('Ctrl Pts',(-35.8311692271447,2.08764602880179,309.052247065549));
#15149=CARTESIAN_POINT('Ctrl Pts',(-35.8962888937197,2.02082536764564,309.057290703711));
#15150=CARTESIAN_POINT('Ctrl Pts',(-35.958020749553,1.95116068710615,309.062334341874));
#15151=CARTESIAN_POINT('Ctrl Pts',(-36.0198525627897,1.88138320418158,309.067386146792));
#15152=CARTESIAN_POINT('Ctrl Pts',(-36.0782853358122,1.80875285408324,309.07243795171));
#15153=CARTESIAN_POINT('Ctrl Pts',(-36.133066002866,1.73364503192726,309.077489756628));
#15154=CARTESIAN_POINT('Ctrl Pts',(-36.1607956940189,1.69562583969093,309.080046954224));
#15155=CARTESIAN_POINT('Ctrl Pts',(-36.1875903022301,1.65697227271461,309.082604151821));
#15156=CARTESIAN_POINT('Ctrl Pts',(-36.2134214872523,1.61773543172242,309.085161349418));
#15157=CARTESIAN_POINT('Ctrl Pts',(-36.2654575656193,1.5386940973436,309.090312740437));
#15158=CARTESIAN_POINT('Ctrl Pts',(-36.313762507844,1.4570088875049,309.095464131457));
#15159=CARTESIAN_POINT('Ctrl Pts',(-36.3580634308538,1.37305897223426,309.100615522476));
#15160=CARTESIAN_POINT('Ctrl Pts',(-36.4022962455816,1.28923812164482,309.105758993742));
#15161=CARTESIAN_POINT('Ctrl Pts',(-36.4425370864889,1.20315985805626,309.110902465008));
#15162=CARTESIAN_POINT('Ctrl Pts',(-36.4785563061367,1.11523217789491,309.116045936274));
#15163=CARTESIAN_POINT('Ctrl Pts',(-36.5146083760685,1.02722430584439,309.121194098494));
#15164=CARTESIAN_POINT('Ctrl Pts',(-36.5464308897537,0.937363999677886,
309.126342260713));
#15165=CARTESIAN_POINT('Ctrl Pts',(-36.5738393479957,0.84608585042522,309.131490422933));
#15166=CARTESIAN_POINT('Ctrl Pts',(-36.6011527392662,0.755124301878006,
309.136620728614));
#15167=CARTESIAN_POINT('Ctrl Pts',(-36.6240824965273,0.662755125579855,
309.141751034295));
#15168=CARTESIAN_POINT('Ctrl Pts',(-36.6424942460327,0.569428017255287,
309.146881339976));
#15169=CARTESIAN_POINT('Ctrl Pts',(-36.6610021214227,0.475613657523854,
309.152038430465));
#15170=CARTESIAN_POINT('Ctrl Pts',(-36.6749445213043,0.380831736906949,
309.157195520954));
#15171=CARTESIAN_POINT('Ctrl Pts',(-36.6842362316534,0.28555292927936,309.162352611443));
#15172=CARTESIAN_POINT('Ctrl Pts',(-36.6935279420025,0.190274121651772,
309.167509701932));
#15173=CARTESIAN_POINT('Ctrl Pts',(-36.6981688930621,0.0944988561008657,
309.172666792421));
#15174=CARTESIAN_POINT('Ctrl Pts',(-36.6981267404244,-0.00129458804859771,
309.17782388291));
#15175=CARTESIAN_POINT('',(-36.6981263554947,-0.00198516614128411,310.177823882873));
#15176=CARTESIAN_POINT('Ctrl Pts',(-36.6981267404242,-0.00129458858357462,
309.177823882939));
#15177=CARTESIAN_POINT('Ctrl Pts',(-36.6980816154796,-0.103842668990332,
309.183344612826));
#15178=CARTESIAN_POINT('Ctrl Pts',(-36.6926705574948,-0.206216608946654,
309.188865342713));
#15179=CARTESIAN_POINT('Ctrl Pts',(-36.6819732173234,-0.307876696704694,
309.194386072601));
#15180=CARTESIAN_POINT('Ctrl Pts',(-36.6712685285798,-0.409606620186989,
309.199910594971));
#15181=CARTESIAN_POINT('Ctrl Pts',(-36.6552704312908,-0.510621430714575,
309.205435117342));
#15182=CARTESIAN_POINT('Ctrl Pts',(-36.6341091164029,-0.610395841275999,
309.210959639712));
#15183=CARTESIAN_POINT('Ctrl Pts',(-36.6128527097254,-0.710618604281967,
309.216508987417));
#15184=CARTESIAN_POINT('Ctrl Pts',(-36.5863867044715,-0.809589515636939,
309.222058335122));
#15185=CARTESIAN_POINT('Ctrl Pts',(-36.5548919122116,-0.906796067235132,
309.227607682827));
#15186=CARTESIAN_POINT('Ctrl Pts',(-36.5237434792017,-1.00293360437476,
309.233096002414));
#15187=CARTESIAN_POINT('Ctrl Pts',(-36.487676512234,-1.09734517951563,309.238584322001));
#15188=CARTESIAN_POINT('Ctrl Pts',(-36.4469105673794,-1.18955787141553,
309.244072641587));
#15189=CARTESIAN_POINT('Ctrl Pts',(-36.4093834444996,-1.27444433810589,
309.249124918537));
#15190=CARTESIAN_POINT('Ctrl Pts',(-36.3677681375394,-1.35770562351083,
309.254177195487));
#15191=CARTESIAN_POINT('Ctrl Pts',(-36.3222273810831,-1.43892076356983,
309.259229472437));
#15192=CARTESIAN_POINT('Ctrl Pts',(-36.2767494337668,-1.52002389290482,
309.264274781361));
#15193=CARTESIAN_POINT('Ctrl Pts',(-36.2273570105023,-1.59908610046198,
309.269320090285));
#15194=CARTESIAN_POINT('Ctrl Pts',(-36.1742605919241,-1.67570703100528,
309.274365399209));
#15195=CARTESIAN_POINT('Ctrl Pts',(-36.1212209971936,-1.7522459617415,309.279405308638));
#15196=CARTESIAN_POINT('Ctrl Pts',(-36.0644855379172,-1.8263484453264,309.284445218066));
#15197=CARTESIAN_POINT('Ctrl Pts',(-36.0043096707011,-1.89764032227573,
309.289485127495));
#15198=CARTESIAN_POINT('Ctrl Pts',(-35.9441771802757,-1.96888080964038,
309.294521403987));
#15199=CARTESIAN_POINT('Ctrl Pts',(-35.88060949691,-2.03731437877704,309.29955768048));
#15200=CARTESIAN_POINT('Ctrl Pts',(-35.8139036589452,-2.10259823215213,
309.304593956972));
#15201=CARTESIAN_POINT('Ctrl Pts',(-35.7472220769321,-2.16785834664556,
309.309628402145));
#15202=CARTESIAN_POINT('Ctrl Pts',(-35.6774049244454,-2.22997071025078,
309.314662847318));
#15203=CARTESIAN_POINT('Ctrl Pts',(-35.6047868410956,-2.28862860361957,
309.319697292492));
#15204=CARTESIAN_POINT('Ctrl Pts',(-35.5321748489373,-2.34728157677513,
309.324731315376));
#15205=CARTESIAN_POINT('Ctrl Pts',(-35.4567627387438,-2.40248037679104,
309.329765338261));
#15206=CARTESIAN_POINT('Ctrl Pts',(-35.3789181493797,-2.45395863198031,
309.334799361146));
#15207=CARTESIAN_POINT('Ctrl Pts',(-35.3010583131751,-2.50544696983236,
309.339834370008));
#15208=CARTESIAN_POINT('Ctrl Pts',(-35.2207654223469,-2.55321307090029,
309.344869378869));
#15209=CARTESIAN_POINT('Ctrl Pts',(-35.1384350206219,-2.59703457927538,
309.34990438773));
#15210=CARTESIAN_POINT('Ctrl Pts',(-35.0560141542123,-2.64090423874465,
309.354944929062));
#15211=CARTESIAN_POINT('Ctrl Pts',(-34.9715517007319,-2.68082044464556,
309.359985470393));
#15212=CARTESIAN_POINT('Ctrl Pts',(-34.8854663884954,-2.71660755403532,
309.365026011725));
#15213=CARTESIAN_POINT('Ctrl Pts',(-34.7993281867691,-2.7524166504738,309.370069649887));
#15214=CARTESIAN_POINT('Ctrl Pts',(-34.7115655589009,-2.78409144931857,
309.37511328805));
#15215=CARTESIAN_POINT('Ctrl Pts',(-34.6226136480587,-2.81150581228402,
309.380156926213));
#15216=CARTESIAN_POINT('Ctrl Pts',(-34.5335177045785,-2.83896456511108,
309.385208731131));
#15217=CARTESIAN_POINT('Ctrl Pts',(-34.4432290634392,-2.86214899953839,
309.390260536049));
#15218=CARTESIAN_POINT('Ctrl Pts',(-34.3521941546287,-2.88098385578317,
309.395312340967));
#15219=CARTESIAN_POINT('Ctrl Pts',(-34.3061127532644,-2.89051796288117,
309.397869538563));
#15220=CARTESIAN_POINT('Ctrl Pts',(-34.2598402376198,-2.89893838835919,
309.40042673616));
#15221=CARTESIAN_POINT('Ctrl Pts',(-34.2134348530919,-2.90624044955015,
309.402983933757));
#15222=CARTESIAN_POINT('Ctrl Pts',(-34.1217513418569,-2.92066719368881,
309.408036210707));
#15223=CARTESIAN_POINT('Ctrl Pts',(-34.029219908507,-2.93077705337543,309.413088487657));
#15224=CARTESIAN_POINT('Ctrl Pts',(-33.9362825688734,-2.93647884039788,
309.418140764607));
#15225=CARTESIAN_POINT('Ctrl Pts',(-33.8434734070486,-2.94217276359973,
309.423186073531));
#15226=CARTESIAN_POINT('Ctrl Pts',(-33.7502598909476,-2.9434706680037,309.428231382455));
#15227=CARTESIAN_POINT('Ctrl Pts',(-33.6570925705185,-2.94033266430425,
309.433276691379));
#15228=CARTESIAN_POINT('Ctrl Pts',(-33.5640249578617,-2.93719801889993,
309.438316600808));
#15229=CARTESIAN_POINT('Ctrl Pts',(-33.471003884229,-2.92963691626866,309.443356510236));
#15230=CARTESIAN_POINT('Ctrl Pts',(-33.3784822368284,-2.91766146318799,
309.448396419665));
#15231=CARTESIAN_POINT('Ctrl Pts',(-33.2860272821458,-2.90569464241702,
309.453432696157));
#15232=CARTESIAN_POINT('Ctrl Pts',(-33.1940714774529,-2.8893198527529,309.458468972649));
#15233=CARTESIAN_POINT('Ctrl Pts',(-33.1030638660051,-2.86860114167639,
309.463505249142));
#15234=CARTESIAN_POINT('Ctrl Pts',(-33.0120893472565,-2.84788996445406,
309.468539694315));
#15235=CARTESIAN_POINT('Ctrl Pts',(-32.9220627695326,-2.8228381023016,309.473574139488));
#15236=CARTESIAN_POINT('Ctrl Pts',(-32.8334232116875,-2.79356075151824,
309.478608584661));
#15237=CARTESIAN_POINT('Ctrl Pts',(-32.744791088912,-2.76428585651363,309.483642607546));
#15238=CARTESIAN_POINT('Ctrl Pts',(-32.6575461764826,-2.73078631708073,
309.488676630431));
#15239=CARTESIAN_POINT('Ctrl Pts',(-32.5721115073424,-2.6932269219908,309.493710653315));
#15240=CARTESIAN_POINT('Ctrl Pts',(-32.4866601047493,-2.65566017042164,
309.498745662177));
#15241=CARTESIAN_POINT('Ctrl Pts',(-32.403020056118,-2.61403216309794,309.503780671038));
#15242=CARTESIAN_POINT('Ctrl Pts',(-32.3215925058338,-2.568554985314,309.5088156799));
#15243=CARTESIAN_POINT('Ctrl Pts',(-32.2400754829186,-2.52302783718558,
309.513856221231));
#15244=CARTESIAN_POINT('Ctrl Pts',(-32.1607761995675,-2.47364329302981,
309.518896762563));
#15245=CARTESIAN_POINT('Ctrl Pts',(-32.0840690877834,-2.42065822736906,
309.523937303894));
#15246=CARTESIAN_POINT('Ctrl Pts',(-32.0073148483313,-2.36764060850013,
309.528980942057));
#15247=CARTESIAN_POINT('Ctrl Pts',(-31.9331563038188,-2.31101833366077,
309.534024580219));
#15248=CARTESIAN_POINT('Ctrl Pts',(-31.8619351606309,-2.25108888762352,
309.539068218381));
#15249=CARTESIAN_POINT('Ctrl Pts',(-31.7905986948039,-2.19106240267938,
309.544120023299));
#15250=CARTESIAN_POINT('Ctrl Pts',(-31.7222094511841,-2.1277183573741,309.549171828217));
#15251=CARTESIAN_POINT('Ctrl Pts',(-31.657072478335,-2.06139127994748,309.554223633135));
#15252=CARTESIAN_POINT('Ctrl Pts',(-31.6241004785967,-2.02781685540956,
309.556780830732));
#15253=CARTESIAN_POINT('Ctrl Pts',(-31.5919611817867,-1.9934786133201,309.559338028329));
#15254=CARTESIAN_POINT('Ctrl Pts',(-31.5606900694731,-1.95842298117025,
309.561895225926));
#15255=CARTESIAN_POINT('Ctrl Pts',(-31.498907468028,-1.88916327183208,309.566947502876));
#15256=CARTESIAN_POINT('Ctrl Pts',(-31.4402945985846,-1.81685278188497,
309.571999779826));
#15257=CARTESIAN_POINT('Ctrl Pts',(-31.3851675091636,-1.74181370216312,
309.577052056776));
#15258=CARTESIAN_POINT('Ctrl Pts',(-31.3301164502117,-1.66687811523385,
309.5820973657));
#15259=CARTESIAN_POINT('Ctrl Pts',(-31.2785418788373,-1.58922177146578,
309.587142674624));
#15260=CARTESIAN_POINT('Ctrl Pts',(-31.2307213409938,-1.50920181880628,
309.592187983548));
#15261=CARTESIAN_POINT('Ctrl Pts',(-31.1829519807444,-1.42926750359124,
309.597227892976));
#15262=CARTESIAN_POINT('Ctrl Pts',(-31.1389288951702,-1.34697498662043,
309.602267802405));
#15263=CARTESIAN_POINT('Ctrl Pts',(-31.0988871859254,-1.26271154119455,
309.607307711834));
#15264=CARTESIAN_POINT('Ctrl Pts',(-31.0588743400925,-1.1785088356965,309.612343988326));
#15265=CARTESIAN_POINT('Ctrl Pts',(-31.0228373563694,-1.09233842570844,
309.617380264819));
#15266=CARTESIAN_POINT('Ctrl Pts',(-30.9909655909837,-1.0046124836992,309.622416541311));
#15267=CARTESIAN_POINT('Ctrl Pts',(-30.9591054149884,-0.916918441090031,
309.627450986484));
#15268=CARTESIAN_POINT('Ctrl Pts',(-30.931407600005,-0.827670407278449,
309.632485431657));
#15269=CARTESIAN_POINT('Ctrl Pts',(-30.9080131077536,-0.737299879913195,
309.63751987683));
#15270=CARTESIAN_POINT('Ctrl Pts',(-30.8846205778279,-0.646936932811046,
309.642553899715));
#15271=CARTESIAN_POINT('Ctrl Pts',(-30.8655307641165,-0.555452109481651,
309.6475879226));
#15272=CARTESIAN_POINT('Ctrl Pts',(-30.8508342484798,-0.463290277474835,
309.652621945485));
#15273=CARTESIAN_POINT('Ctrl Pts',(-30.836134854346,-0.371110394415744,
309.657656954346));
#15274=CARTESIAN_POINT('Ctrl Pts',(-30.8258305367978,-0.278253678079413,
309.662691963208));
#15275=CARTESIAN_POINT('Ctrl Pts',(-30.8199602635903,-0.185172210874213,
309.667726972069));
#15276=CARTESIAN_POINT('Ctrl Pts',(-30.8140835401238,-0.0919884657087816,
309.672767513401));
#15277=CARTESIAN_POINT('Ctrl Pts',(-30.8126506143522,0.00142007921788039,
309.677808054732));
#15278=CARTESIAN_POINT('Ctrl Pts',(-30.8156483351303,0.0945995396776959,
309.682848596064));
#15279=CARTESIAN_POINT('Ctrl Pts',(-30.8186478976619,0.187836248162711,
309.687892234226));
#15280=CARTESIAN_POINT('Ctrl Pts',(-30.8260834905748,0.280843149467654,
309.692935872389));
#15281=CARTESIAN_POINT('Ctrl Pts',(-30.837890100144,0.373171875820337,309.697979510551));
#15282=CARTESIAN_POINT('Ctrl Pts',(-30.8497158272015,0.465650102615157,
309.70303131547));
#15283=CARTESIAN_POINT('Ctrl Pts',(-30.8659266233817,0.557447525268726,
309.708083120388));
#15284=CARTESIAN_POINT('Ctrl Pts',(-30.8864064811281,0.648126529777455,
309.713134925306));
#15285=CARTESIAN_POINT('Ctrl Pts',(-30.8967732795013,0.694027774212889,
309.715692122902));
#15286=CARTESIAN_POINT('Ctrl Pts',(-30.9082331591181,0.739642688745836,
309.718249320499));
#15287=CARTESIAN_POINT('Ctrl Pts',(-30.9207663074984,0.784916301390221,
309.720806518095));
#15288=CARTESIAN_POINT('Ctrl Pts',(-30.9455281549042,0.874363761341351,
309.725858795045));
#15289=CARTESIAN_POINT('Ctrl Pts',(-30.9745713139954,0.962798880669171,
309.730911071995));
#15290=CARTESIAN_POINT('Ctrl Pts',(-31.0077961057622,1.04978148056891,309.735963348945));
#15291=CARTESIAN_POINT('Ctrl Pts',(-31.0409750743859,1.13664411534911,309.741008657869));
#15292=CARTESIAN_POINT('Ctrl Pts',(-31.0783240582896,1.22205780008977,309.746053966793));
#15293=CARTESIAN_POINT('Ctrl Pts',(-31.1196931396859,1.30559579005501,309.751099275717));
#15294=CARTESIAN_POINT('Ctrl Pts',(-31.1610179478442,1.38904437756827,309.756139185145));
#15295=CARTESIAN_POINT('Ctrl Pts',(-31.2063541059076,1.47062086428266,309.761179094574));
#15296=CARTESIAN_POINT('Ctrl Pts',(-31.2555033840231,1.54991787037215,309.766219004002));
#15297=CARTESIAN_POINT('Ctrl Pts',(-31.3046172336844,1.62915771651045,309.771255280495));
#15298=CARTESIAN_POINT('Ctrl Pts',(-31.3575385067491,1.7061209714464,309.776291556987));
#15299=CARTESIAN_POINT('Ctrl Pts',(-31.4140232667962,1.78042522578204,309.781327833479));
#15300=CARTESIAN_POINT('Ctrl Pts',(-31.4704874875374,1.85470246118713,309.786362278652));
#15301=CARTESIAN_POINT('Ctrl Pts',(-31.5305123524841,1.92632226349048,309.791396723825));
#15302=CARTESIAN_POINT('Ctrl Pts',(-31.5938114696656,1.99493243946875,309.796431168998));
#15303=CARTESIAN_POINT('Ctrl Pts',(-31.6571052773288,2.06353686043815,309.801465191883));
#15304=CARTESIAN_POINT('Ctrl Pts',(-31.7236724897918,2.12913183060961,309.806499214768));
#15305=CARTESIAN_POINT('Ctrl Pts',(-31.7931881905498,2.19140026722548,309.811533237653));
#15306=CARTESIAN_POINT('Ctrl Pts',(-31.8627175068308,2.25368089989671,309.816568246514));
#15307=CARTESIAN_POINT('Ctrl Pts',(-31.9351961271814,2.3126334089249,309.821603255375));
#15308=CARTESIAN_POINT('Ctrl Pts',(-32.0102651163,2.36798019308669,309.826638264237));
#15309=CARTESIAN_POINT('Ctrl Pts',(-32.0854165912594,2.42338779232112,309.831678805568));
#15310=CARTESIAN_POINT('Ctrl Pts',(-32.1631637584059,2.47518149408124,309.8367193469));
#15311=CARTESIAN_POINT('Ctrl Pts',(-32.243117940682,2.52312653467709,309.841759888231));
#15312=CARTESIAN_POINT('Ctrl Pts',(-32.3231212455761,2.57110103196735,309.846803526394));
#15313=CARTESIAN_POINT('Ctrl Pts',(-32.4053338738849,2.61522195079954,309.851847164556));
#15314=CARTESIAN_POINT('Ctrl Pts',(-32.4893436976716,2.65530111304727,309.856890802718));
#15315=CARTESIAN_POINT('Ctrl Pts',(-32.5734895517741,2.69544517224219,309.861942607636));
#15316=CARTESIAN_POINT('Ctrl Pts',(-32.6594380018191,2.73153423780507,309.866994412554));
#15317=CARTESIAN_POINT('Ctrl Pts',(-32.7467583422055,2.76342882334134,309.872046217472));
#15318=CARTESIAN_POINT('Ctrl Pts',(-32.7909594481981,2.77957369805941,309.87460341507));
#15319=CARTESIAN_POINT('Ctrl Pts',(-32.8355118547494,2.79464460846844,309.877160612667));
#15320=CARTESIAN_POINT('Ctrl Pts',(-32.8803586198137,2.80862843751649,309.879717810264));
#15321=CARTESIAN_POINT('Ctrl Pts',(-32.9689627533585,2.83625640699573,309.884770087214));
#15322=CARTESIAN_POINT('Ctrl Pts',(-33.059034585095,2.85973704898571,309.889822364164));
#15323=CARTESIAN_POINT('Ctrl Pts',(-33.1501500967158,2.87891576154549,309.894874641114));
#15324=CARTESIAN_POINT('Ctrl Pts',(-33.2411399431661,2.89806802310761,309.899919950038));
#15325=CARTESIAN_POINT('Ctrl Pts',(-33.3331701782177,2.91293005446495,309.904965258962));
#15326=CARTESIAN_POINT('Ctrl Pts',(-33.4258008680034,2.92339676230129,309.910010567886));
#15327=CARTESIAN_POINT('Ctrl Pts',(-33.5183324243195,2.93385226865499,309.915050477315));
#15328=CARTESIAN_POINT('Ctrl Pts',(-33.6114627190154,2.93992175154605,309.920090386743));
#15329=CARTESIAN_POINT('Ctrl Pts',(-33.704741931871,2.94155121869017,309.925130296172));
#15330=CARTESIAN_POINT('Ctrl Pts',(-33.7979539059301,2.94317951125953,309.930166572664));
#15331=CARTESIAN_POINT('Ctrl Pts',(-33.8913141418738,2.94037414181105,309.935202849157));
#15332=CARTESIAN_POINT('Ctrl Pts',(-33.9843690564791,2.93313306469104,309.940239125649));
#15333=CARTESIAN_POINT('Ctrl Pts',(-34.0773901339334,2.9258946206122,309.945273570822));
#15334=CARTESIAN_POINT('Ctrl Pts',(-34.1701056681364,2.91422370756331,309.950308015995));
#15335=CARTESIAN_POINT('Ctrl Pts',(-34.2620644833797,2.89817033461957,309.955342461169));
#15336=CARTESIAN_POINT('Ctrl Pts',(-34.3540155851347,2.88211830822978,309.960376484053));
#15337=CARTESIAN_POINT('Ctrl Pts',(-34.4452096565233,2.86168462939899,309.965410506938));
#15338=CARTESIAN_POINT('Ctrl Pts',(-34.5352041727013,2.83697070804952,309.970444529823));
#15339=CARTESIAN_POINT('Ctrl Pts',(-34.6252163154354,2.81225194616819,309.975479538684));
#15340=CARTESIAN_POINT('Ctrl Pts',(-34.7140280080785,2.78325139481781,309.980514547546));
#15341=CARTESIAN_POINT('Ctrl Pts',(-34.8012114914192,2.75012044437833,309.985549556407));
#15342=CARTESIAN_POINT('Ctrl Pts',(-34.8884907720128,2.7169530896348,309.990590097739));
#15343=CARTESIAN_POINT('Ctrl Pts',(-34.9741378561696,2.6796464345063,309.99563063907));
#15344=CARTESIAN_POINT('Ctrl Pts',(-35.0577448879104,2.6384000719419,310.000671180402));
#15345=CARTESIAN_POINT('Ctrl Pts',(-35.1414032865237,2.5971283682477,310.005714818564));
#15346=CARTESIAN_POINT('Ctrl Pts',(-35.223018749177,2.55191235351768,310.010758456727));
#15347=CARTESIAN_POINT('Ctrl Pts',(-35.3022098809528,2.50299656478496,310.015802094889));
#15348=CARTESIAN_POINT('Ctrl Pts',(-35.381529240526,2.45400157067023,310.020853899807));
#15349=CARTESIAN_POINT('Ctrl Pts',(-35.4584160664295,2.40129509363968,310.025905704725));
#15350=CARTESIAN_POINT('Ctrl Pts',(-35.5325198346268,2.34516365885654,310.030957509643));
#15351=CARTESIAN_POINT('Ctrl Pts',(-35.5700307799295,2.3167502160434,310.03351470724));
#15352=CARTESIAN_POINT('Ctrl Pts',(-35.6068291656455,2.2874598067233,310.036071904837));
#15353=CARTESIAN_POINT('Ctrl Pts',(-35.642873125783,2.25733319475707,310.038629102434));
#15354=CARTESIAN_POINT('Ctrl Pts',(-35.7130960226271,2.19863881277755,310.043611180496));
#15355=CARTESIAN_POINT('Ctrl Pts',(-35.7807203985796,2.1365446975608,310.048593258558));
#15356=CARTESIAN_POINT('Ctrl Pts',(-35.8453917268001,2.07131287035265,310.05357533662));
#15357=CARTESIAN_POINT('Ctrl Pts',(-35.9125935919664,2.00352857432506,310.05875235938));
#15358=CARTESIAN_POINT('Ctrl Pts',(-35.9766061277763,1.93235620548142,310.063929382141));
#15359=CARTESIAN_POINT('Ctrl Pts',(-36.0370672991168,1.85813763405383,310.069106404901));
#15360=CARTESIAN_POINT('Ctrl Pts',(-36.0951028747957,1.78689658093877,310.074075734631));
#15361=CARTESIAN_POINT('Ctrl Pts',(-36.149866219895,1.71284943135371,310.07904506436));
#15362=CARTESIAN_POINT('Ctrl Pts',(-36.2010742862668,1.63633642350331,310.084014394089));
#15363=CARTESIAN_POINT('Ctrl Pts',(-36.252251367175,1.5598697128711,310.088980716929));
#15364=CARTESIAN_POINT('Ctrl Pts',(-36.2998771858322,1.4809404851409,310.093947039769));
#15365=CARTESIAN_POINT('Ctrl Pts',(-36.3437102606287,1.39992035488687,310.098913362609));
#15366=CARTESIAN_POINT('Ctrl Pts',(-36.3875298767662,1.31892510133392,310.103878160573));
#15367=CARTESIAN_POINT('Ctrl Pts',(-36.4275588445785,1.2358406227864,310.108842958536));
#15368=CARTESIAN_POINT('Ctrl Pts',(-36.4636008360711,1.15106453501049,310.113807756499));
#15369=CARTESIAN_POINT('Ctrl Pts',(-36.4996425024049,1.06628921205609,310.118772509671));
#15370=CARTESIAN_POINT('Ctrl Pts',(-36.5316970872211,0.979822732429954,
310.123737262844));
#15371=CARTESIAN_POINT('Ctrl Pts',(-36.5596162898467,0.89208292402314,310.128702016016));
#15372=CARTESIAN_POINT('Ctrl Pts',(-36.5875575363704,0.804273839733983,
310.133670689161));
#15373=CARTESIAN_POINT('Ctrl Pts',(-36.6113567457612,0.715189857057896,
310.138639362306));
#15374=CARTESIAN_POINT('Ctrl Pts',(-36.6309156226946,0.625263560465722,
310.143608035451));
#15375=CARTESIAN_POINT('Ctrl Pts',(-36.6504837121961,0.535294907038126,
310.148579048927));
#15376=CARTESIAN_POINT('Ctrl Pts',(-36.665807418628,0.444483601232109,310.153550062402));
#15377=CARTESIAN_POINT('Ctrl Pts',(-36.6768400203945,0.353269868568233,
310.158521075878));
#15378=CARTESIAN_POINT('Ctrl Pts',(-36.6878871247899,0.261936233188972,
310.163498623874));
#15379=CARTESIAN_POINT('Ctrl Pts',(-36.6946318385709,0.170199571086817,
310.168476171871));
#15380=CARTESIAN_POINT('Ctrl Pts',(-36.697079495602,0.0785020201984402,
310.173453719867));
#15381=CARTESIAN_POINT('Ctrl Pts',(-36.697795822879,0.0516659659204363,
310.174910440869));
#15382=CARTESIAN_POINT('Ctrl Pts',(-36.6981444516876,0.0248332378491975,
310.176367161871));
#15383=CARTESIAN_POINT('Ctrl Pts',(-36.6981263554947,-0.00198516614128179,
310.177823882873));
#15384=CARTESIAN_POINT('',(-36.6981260264717,0.00242422262951868,311.177823882937));
#15385=CARTESIAN_POINT('Ctrl Pts',(-36.6981263554942,-0.00198516682809399,
310.17782388291));
#15386=CARTESIAN_POINT('Ctrl Pts',(-36.6980447123328,-0.122979595449192,
310.184396053475));
#15387=CARTESIAN_POINT('Ctrl Pts',(-36.690499043274,-0.243723585403416,
310.190968224039));
#15388=CARTESIAN_POINT('Ctrl Pts',(-36.6755806319958,-0.363530793885655,
310.197540394603));
#15389=CARTESIAN_POINT('Ctrl Pts',(-36.664112283041,-0.455631142144333,
310.202592671552));
#15390=CARTESIAN_POINT('Ctrl Pts',(-36.6482608242988,-0.547353585824939,
310.207644948502));
#15391=CARTESIAN_POINT('Ctrl Pts',(-36.6280607528387,-0.638248121330511,
310.212697225451));
#15392=CARTESIAN_POINT('Ctrl Pts',(-36.6078885410195,-0.729017296432616,
310.217742534374));
#15393=CARTESIAN_POINT('Ctrl Pts',(-36.5833797299021,-0.81896040242599,
310.222787843298));
#15394=CARTESIAN_POINT('Ctrl Pts',(-36.5546204763606,-0.907633408449618,
310.227833152221));
#15395=CARTESIAN_POINT('Ctrl Pts',(-36.5258920010048,-0.996211516521299,
310.232873061649));
#15396=CARTESIAN_POINT('Ctrl Pts',(-36.4929222610277,-1.08352180604662,
310.237912971077));
#15397=CARTESIAN_POINT('Ctrl Pts',(-36.4558480308637,-1.16913236713767,
310.242952880505));
#15398=CARTESIAN_POINT('Ctrl Pts',(-36.4188005250528,-1.25468121725462,
310.247989156997));
#15399=CARTESIAN_POINT('Ctrl Pts',(-36.3776545858314,-1.33853236773728,
310.253025433489));
#15400=CARTESIAN_POINT('Ctrl Pts',(-36.3325958440165,-1.42027195493082,
310.258061709981));
#15401=CARTESIAN_POINT('Ctrl Pts',(-36.2875534867145,-1.50198181951631,
310.263096155153));
#15402=CARTESIAN_POINT('Ctrl Pts',(-36.2386013676048,-1.58158125749836,
310.268130600326));
#15403=CARTESIAN_POINT('Ctrl Pts',(-36.1859715216672,-1.65868011481058,
310.273165045499));
#15404=CARTESIAN_POINT('Ctrl Pts',(-36.1333460903113,-1.73577250508494,
310.278199068383));
#15405=CARTESIAN_POINT('Ctrl Pts',(-36.0770437960919,-1.81036436490259,
310.283233091267));
#15406=CARTESIAN_POINT('Ctrl Pts',(-36.0173399019926,-1.88209466448626,
310.288267114152));
#15407=CARTESIAN_POINT('Ctrl Pts',(-35.9576243141357,-1.95383901335018,
310.293302123013));
#15408=CARTESIAN_POINT('Ctrl Pts',(-35.894506087705,-2.02272034768265,310.298337131874));
#15409=CARTESIAN_POINT('Ctrl Pts',(-35.8282998927217,-2.08841174277138,
310.303372140734));
#15410=CARTESIAN_POINT('Ctrl Pts',(-35.7620209503401,-2.15417531959619,
310.308412682066));
#15411=CARTESIAN_POINT('Ctrl Pts',(-35.6926475823017,-2.21674164717611,
310.313453223397));
#15412=CARTESIAN_POINT('Ctrl Pts',(-35.6205301230968,-2.27582184908392,
310.318493764728));
#15413=CARTESIAN_POINT('Ctrl Pts',(-35.5483683560356,-2.33493834895779,
310.32353740289));
#15414=CARTESIAN_POINT('Ctrl Pts',(-35.4734594978642,-2.39056419455085,
310.328581041052));
#15415=CARTESIAN_POINT('Ctrl Pts',(-35.3961838697211,-2.44245318213646,
310.333624679214));
#15416=CARTESIAN_POINT('Ctrl Pts',(-35.3187831154005,-2.49442618936478,
310.338676484131));
#15417=CARTESIAN_POINT('Ctrl Pts',(-35.2390083200674,-2.54265002938534,
310.343728289049));
#15418=CARTESIAN_POINT('Ctrl Pts',(-35.1572652770677,-2.58692396473389,
310.348780093967));
#15419=CARTESIAN_POINT('Ctrl Pts',(-35.1158873701716,-2.60933520252919,
310.351337291569));
#15420=CARTESIAN_POINT('Ctrl Pts',(-35.0740054704259,-2.63073510327062,
310.353894489171));
#15421=CARTESIAN_POINT('Ctrl Pts',(-35.0316740018305,-2.65110239533592,
310.356451686773));
#15422=CARTESIAN_POINT('Ctrl Pts',(-34.9480393609716,-2.69134222668754,
310.361503963723));
#15423=CARTESIAN_POINT('Ctrl Pts',(-34.8623485549746,-2.72769275884657,
310.366556240673));
#15424=CARTESIAN_POINT('Ctrl Pts',(-34.7749985594086,-2.75993927413208,
310.371608517623));
#15425=CARTESIAN_POINT('Ctrl Pts',(-34.687769035669,-2.79214131549904,310.376653826547));
#15426=CARTESIAN_POINT('Ctrl Pts',(-34.5988852827091,-2.8202504350076,310.381699135471));
#15427=CARTESIAN_POINT('Ctrl Pts',(-34.508767233588,-2.84409857719532,310.386744444395));
#15428=CARTESIAN_POINT('Ctrl Pts',(-34.4187456289057,-2.86792119707408,
310.391784353824));
#15429=CARTESIAN_POINT('Ctrl Pts',(-34.3274927808052,-2.88749179048213,
310.396824263252));
#15430=CARTESIAN_POINT('Ctrl Pts',(-34.2354458468949,-2.90269141784383,
310.401864172681));
#15431=CARTESIAN_POINT('Ctrl Pts',(-34.1434652635131,-2.91788008880247,
310.406900449174));
#15432=CARTESIAN_POINT('Ctrl Pts',(-34.0506921691141,-2.92870398407811,
310.411936725666));
#15433=CARTESIAN_POINT('Ctrl Pts',(-33.957575010992,-2.93509500852077,310.416973002158));
#15434=CARTESIAN_POINT('Ctrl Pts',(-33.8644917126544,-2.94148370902321,
310.422007447331));
#15435=CARTESIAN_POINT('Ctrl Pts',(-33.7710650419058,-2.94344271052497,
310.427041892505));
#15436=CARTESIAN_POINT('Ctrl Pts',(-33.6777486467697,-2.94095576807704,
310.432076337678));
#15437=CARTESIAN_POINT('Ctrl Pts',(-33.5844400789956,-2.93846903423339,
310.437110360563));
#15438=CARTESIAN_POINT('Ctrl Pts',(-33.4912422125369,-2.93153710992043,
310.442144383447));
#15439=CARTESIAN_POINT('Ctrl Pts',(-33.3986076241413,-2.92019586292178,
310.447178406332));
#15440=CARTESIAN_POINT('Ctrl Pts',(-33.3059548920983,-2.90885239459747,
310.452213415194));
#15441=CARTESIAN_POINT('Ctrl Pts',(-33.2138660981168,-2.89309794278401,
310.457248424055));
#15442=CARTESIAN_POINT('Ctrl Pts',(-33.1227864912185,-2.87301997346749,
310.462283432917));
#15443=CARTESIAN_POINT('Ctrl Pts',(-33.0316068060052,-2.85291994246881,
310.467323974248));
#15444=CARTESIAN_POINT('Ctrl Pts',(-32.941438955873,-2.82848700682606,310.47236451558));
#15445=CARTESIAN_POINT('Ctrl Pts',(-32.85271552034,-2.79985922017207,310.477405056911));
#15446=CARTESIAN_POINT('Ctrl Pts',(-32.763937574495,-2.77121384504694,310.482448695074));
#15447=CARTESIAN_POINT('Ctrl Pts',(-32.6766062254526,-2.73836864438079,
310.487492333236));
#15448=CARTESIAN_POINT('Ctrl Pts',(-32.5911344206962,-2.70150999097119,
310.492535971399));
#15449=CARTESIAN_POINT('Ctrl Pts',(-32.5055242183565,-2.66459165532409,
310.497587776317));
#15450=CARTESIAN_POINT('Ctrl Pts',(-32.4217799700218,-2.62364708804665,
310.502639581235));
#15451=CARTESIAN_POINT('Ctrl Pts',(-32.3402901977767,-2.57890869903316,
310.507691386153));
#15452=CARTESIAN_POINT('Ctrl Pts',(-32.2990404953244,-2.55626235723886,
310.510248583749));
#15453=CARTESIAN_POINT('Ctrl Pts',(-32.2583680087024,-2.53264460754716,
310.512805781346));
#15454=CARTESIAN_POINT('Ctrl Pts',(-32.2183200952352,-2.50808968060854,
310.515362978942));
#15455=CARTESIAN_POINT('Ctrl Pts',(-32.1391970933683,-2.45957630346107,
310.520415255894));
#15456=CARTESIAN_POINT('Ctrl Pts',(-32.0622300048175,-2.40722802069624,
310.525467532846));
#15457=CARTESIAN_POINT('Ctrl Pts',(-31.987814328418,-2.35126225806393,310.530519809798));
#15458=CARTESIAN_POINT('Ctrl Pts',(-31.9135012850222,-2.2953736825863,310.535565118725));
#15459=CARTESIAN_POINT('Ctrl Pts',(-31.8417330133074,-2.23587780607076,
310.540610427651));
#15460=CARTESIAN_POINT('Ctrl Pts',(-31.7728782193927,-2.17303662510217,
310.545655736577));
#15461=CARTESIAN_POINT('Ctrl Pts',(-31.7040971139568,-2.11026269683695,
310.550695646008));
#15462=CARTESIAN_POINT('Ctrl Pts',(-31.6382236151875,-2.04415087807505,
310.555735555439));
#15463=CARTESIAN_POINT('Ctrl Pts',(-31.5755944689269,-1.975004245763,310.56077546487));
#15464=CARTESIAN_POINT('Ctrl Pts',(-31.513010467863,-1.90590745667101,310.565811741365));
#15465=CARTESIAN_POINT('Ctrl Pts',(-31.4536664683148,-1.8337805305052,310.570848017859));
#15466=CARTESIAN_POINT('Ctrl Pts',(-31.397862588501,-1.75896357163216,310.575884294354));
#15467=CARTESIAN_POINT('Ctrl Pts',(-31.3420790004076,-1.68417381812222,
310.580918739529));
#15468=CARTESIAN_POINT('Ctrl Pts',(-31.2898332400781,-1.60669633088394,
310.585953184704));
#15469=CARTESIAN_POINT('Ctrl Pts',(-31.2413846548929,-1.52690366778402,
310.59098762988));
#15470=CARTESIAN_POINT('Ctrl Pts',(-31.192940133566,-1.44711769767798,310.596021652767));
#15471=CARTESIAN_POINT('Ctrl Pts',(-31.148292384532,-1.3650173176519,310.601055675654));
#15472=CARTESIAN_POINT('Ctrl Pts',(-31.1076563667832,-1.28100240874095,
310.606089698541));
#15473=CARTESIAN_POINT('Ctrl Pts',(-31.06701238996,-1.19697104445505,310.611124707405));
#15474=CARTESIAN_POINT('Ctrl Pts',(-31.030381898013,-1.11102480663302,310.616159716268));
#15475=CARTESIAN_POINT('Ctrl Pts',(-30.9979325056523,-1.02358536137399,
310.621194725132));
#15476=CARTESIAN_POINT('Ctrl Pts',(-30.9654474578841,-0.936049837611584,
310.626235266466));
#15477=CARTESIAN_POINT('Ctrl Pts',(-30.937152835064,-0.847018248452105,
310.6312758078));
#15478=CARTESIAN_POINT('Ctrl Pts',(-30.9131668640838,-0.756929007225038,
310.636316349133));
#15479=CARTESIAN_POINT('Ctrl Pts',(-30.8891661564926,-0.666784416556086,
310.641359987298));
#15480=CARTESIAN_POINT('Ctrl Pts',(-30.8694794644035,-0.575581314118212,
310.646403625463));
#15481=CARTESIAN_POINT('Ctrl Pts',(-30.8541737630365,-0.483767778881916,
310.651447263627));
#15482=CARTESIAN_POINT('Ctrl Pts',(-30.8388432783848,-0.39180557741157,
310.656499068548));
#15483=CARTESIAN_POINT('Ctrl Pts',(-30.827907998374,-0.299231410511365,
310.661550873468));
#15484=CARTESIAN_POINT('Ctrl Pts',(-30.8213829689193,-0.206497757341061,
310.666602678388));
#15485=CARTESIAN_POINT('Ctrl Pts',(-30.81808003269,-0.159556460775926,310.669159875962));
#15486=CARTESIAN_POINT('Ctrl Pts',(-30.8159063177971,-0.112574291881349,
310.671717073537));
#15487=CARTESIAN_POINT('Ctrl Pts',(-30.814858696737,-0.0656096002259395,
310.674274271111));
#15488=CARTESIAN_POINT('Ctrl Pts',(-30.81278890292,0.0271789395537369,310.679326548055));
#15489=CARTESIAN_POINT('Ctrl Pts',(-30.815110515912,0.120232072311605,310.684378825));
#15490=CARTESIAN_POINT('Ctrl Pts',(-30.8218549564799,0.213099569194949,
310.689431101944));
#15491=CARTESIAN_POINT('Ctrl Pts',(-30.8285900952148,0.305838984595543,
310.694476410863));
#15492=CARTESIAN_POINT('Ctrl Pts',(-30.8397359083539,0.398392833634469,
310.699521719781));
#15493=CARTESIAN_POINT('Ctrl Pts',(-30.8552718378466,0.490309271450782,
310.7045670287));
#15494=CARTESIAN_POINT('Ctrl Pts',(-30.8707911407698,0.582127340190802,
310.709606938123));
#15495=CARTESIAN_POINT('Ctrl Pts',(-30.8906911478108,0.673308917910803,
310.714646847546));
#15496=CARTESIAN_POINT('Ctrl Pts',(-30.9148994576439,0.763406778219993,
310.719686756969));
#15497=CARTESIAN_POINT('Ctrl Pts',(-30.9390903173126,0.853439692959391,
310.724723033456));
#15498=CARTESIAN_POINT('Ctrl Pts',(-30.9675831920734,0.942390015186752,
310.729759309943));
#15499=CARTESIAN_POINT('Ctrl Pts',(-31.0002547166145,1.02982125558468,310.73479558643));
#15500=CARTESIAN_POINT('Ctrl Pts',(-31.0329143609523,1.11722070374403,310.739830031598));
#15501=CARTESIAN_POINT('Ctrl Pts',(-31.0697494811424,1.20310175169881,310.744864476765));
#15502=CARTESIAN_POINT('Ctrl Pts',(-31.1105873489966,1.28704460735787,310.749898921933));
#15503=CARTESIAN_POINT('Ctrl Pts',(-31.1514217913783,1.37098042190631,310.754932944812));
#15504=CARTESIAN_POINT('Ctrl Pts',(-31.1962581193606,1.45297796798695,310.759966967692));
#15505=CARTESIAN_POINT('Ctrl Pts',(-31.2448765954274,1.53263997033799,310.765000990571));
#15506=CARTESIAN_POINT('Ctrl Pts',(-31.2935045940337,1.61231757549331,310.770035999427));
#15507=CARTESIAN_POINT('Ctrl Pts',(-31.3459159801803,1.68965834943481,310.775071008283));
#15508=CARTESIAN_POINT('Ctrl Pts',(-31.4018470617087,1.76429301796272,310.780106017139));
#15509=CARTESIAN_POINT('Ctrl Pts',(-31.457839600337,1.83900969510125,310.785146558466));
#15510=CARTESIAN_POINT('Ctrl Pts',(-31.5173592873925,1.9110139753696,310.790187099792));
#15511=CARTESIAN_POINT('Ctrl Pts',(-31.5801016043343,1.97996903195367,310.795227641118));
#15512=CARTESIAN_POINT('Ctrl Pts',(-31.6428824691898,2.04896645346304,310.800271279276));
#15513=CARTESIAN_POINT('Ctrl Pts',(-31.7088895915387,2.11491060796936,310.805314917433));
#15514=CARTESIAN_POINT('Ctrl Pts',(-31.7777825701013,2.17750251819656,310.81035855559));
#15515=CARTESIAN_POINT('Ctrl Pts',(-31.8467871014961,2.24019577844526,310.815410360503));
#15516=CARTESIAN_POINT('Ctrl Pts',(-31.9186864756149,2.29952567564314,310.820462165416));
#15517=CARTESIAN_POINT('Ctrl Pts',(-31.9931084678045,2.35523450341486,310.825513970329));
#15518=CARTESIAN_POINT('Ctrl Pts',(-32.0307804972763,2.38343402535606,310.828071167979));
#15519=CARTESIAN_POINT('Ctrl Pts',(-32.0690984606701,2.41070641144219,310.83062836563));
#15520=CARTESIAN_POINT('Ctrl Pts',(-32.1080116130096,2.43702268924819,310.83318556328));
#15521=CARTESIAN_POINT('Ctrl Pts',(-32.184892656084,2.4890159811284,310.838237840233));
#15522=CARTESIAN_POINT('Ctrl Pts',(-32.2643744688606,2.53746096915058,310.843290117185));
#15523=CARTESIAN_POINT('Ctrl Pts',(-32.3460955868427,2.58208740027939,310.848342394138));
#15524=CARTESIAN_POINT('Ctrl Pts',(-32.4277039962628,2.62665228329182,310.853387703064));
#15525=CARTESIAN_POINT('Ctrl Pts',(-32.5115451872888,2.66740886353547,310.858433011991));
#15526=CARTESIAN_POINT('Ctrl Pts',(-32.5972281857368,2.7041297083826,310.863478320917));
#15527=CARTESIAN_POINT('Ctrl Pts',(-32.6828194861414,2.74081125453939,310.868518230348));
#15528=CARTESIAN_POINT('Ctrl Pts',(-32.7702482699579,2.77346547600095,310.873558139779));
#15529=CARTESIAN_POINT('Ctrl Pts',(-32.8590993676928,2.80191102313471,310.87859804921));
#15530=CARTESIAN_POINT('Ctrl Pts',(-32.9478864185641,2.83033606576011,310.883634325705));
#15531=CARTESIAN_POINT('Ctrl Pts',(-33.0380933236371,2.8545583290018,310.8886706022));
#15532=CARTESIAN_POINT('Ctrl Pts',(-33.129286337883,2.87444512082797,310.893706878694));
#15533=CARTESIAN_POINT('Ctrl Pts',(-33.2204461920115,2.89432468130691,310.89874132387));
#15534=CARTESIAN_POINT('Ctrl Pts',(-33.3125910093486,2.90987180767159,310.903775769045));
#15535=CARTESIAN_POINT('Ctrl Pts',(-33.4052743468349,2.92100434748797,310.908810214221));
#15536=CARTESIAN_POINT('Ctrl Pts',(-33.4979499100589,2.93213595350883,310.913844237108));
#15537=CARTESIAN_POINT('Ctrl Pts',(-33.5911634625136,2.93885365641506,310.918878259995));
#15538=CARTESIAN_POINT('Ctrl Pts',(-33.6844620299747,2.94112701671504,310.923912282882));
#15539=CARTESIAN_POINT('Ctrl Pts',(-33.7777788711309,2.94340082228116,310.928947291745));
#15540=CARTESIAN_POINT('Ctrl Pts',(-33.8711803162558,2.94122854601305,310.933982300609));
#15541=CARTESIAN_POINT('Ctrl Pts',(-33.9642131246277,2.93463186366688,310.939017309472));
#15542=CARTESIAN_POINT('Ctrl Pts',(-34.0573481574917,2.92802793288315,310.944057850806));
#15543=CARTESIAN_POINT('Ctrl Pts',(-34.1501133012287,2.91698992328308,310.94909839214));
#15544=CARTESIAN_POINT('Ctrl Pts',(-34.2420604806244,2.90159140420482,310.954138933473));
#15545=CARTESIAN_POINT('Ctrl Pts',(-34.3340641509496,2.88618342451382,310.959182571638));
#15546=CARTESIAN_POINT('Ctrl Pts',(-34.4252484226218,2.86640969600237,310.964226209802));
#15547=CARTESIAN_POINT('Ctrl Pts',(-34.5151776046413,2.84239445150339,310.969269847967));
#15548=CARTESIAN_POINT('Ctrl Pts',(-34.6052524017129,2.81834032106104,310.974321652887));
#15549=CARTESIAN_POINT('Ctrl Pts',(-34.6940676292192,2.79003109837152,310.979373457807));
#15550=CARTESIAN_POINT('Ctrl Pts',(-34.7812050550307,2.75764012026162,310.984425262726));
#15551=CARTESIAN_POINT('Ctrl Pts',(-34.8253135701994,2.74124397433485,310.986982460301));
#15552=CARTESIAN_POINT('Ctrl Pts',(-34.868992526545,2.72380270133821,310.989539657876));
#15553=CARTESIAN_POINT('Ctrl Pts',(-34.9121900856443,2.70534326849836,310.99209685545));
#15554=CARTESIAN_POINT('Ctrl Pts',(-34.9975358700768,2.66887281024228,310.997149132419));
#15555=CARTESIAN_POINT('Ctrl Pts',(-35.0813073487881,2.62829430803813,311.002201409388));
#15556=CARTESIAN_POINT('Ctrl Pts',(-35.1630815699805,2.58376525812304,311.007253686357));
#15557=CARTESIAN_POINT('Ctrl Pts',(-35.2447430093745,2.53929762201609,311.0122989953));
#15558=CARTESIAN_POINT('Ctrl Pts',(-35.3244122781905,2.4908904757454,311.017344304243));
#15559=CARTESIAN_POINT('Ctrl Pts',(-35.4016864391525,2.43874931375529,311.022389613186));
#15560=CARTESIAN_POINT('Ctrl Pts',(-35.4788779012206,2.3866639532953,311.027429522634));
#15561=CARTESIAN_POINT('Ctrl Pts',(-35.5536789839904,2.33085276721458,311.032469432082));
#15562=CARTESIAN_POINT('Ctrl Pts',(-35.6257123855913,2.27156654765511,311.037509341529));
#15563=CARTESIAN_POINT('Ctrl Pts',(-35.6976938630922,2.21232306359795,311.042545618041));
#15564=CARTESIAN_POINT('Ctrl Pts',(-35.7669112828091,2.14960980644723,311.047581894552));
#15565=CARTESIAN_POINT('Ctrl Pts',(-35.8330181862139,2.08371953620005,311.052618171064));
#15566=CARTESIAN_POINT('Ctrl Pts',(-35.899101051455,2.01785322534312,311.057652616256));
#15567=CARTESIAN_POINT('Ctrl Pts',(-35.9620753330269,1.948812509708,311.062687061448));
#15568=CARTESIAN_POINT('Ctrl Pts',(-36.0216301810279,1.87692819553516,311.06772150664));
#15569=CARTESIAN_POINT('Ctrl Pts',(-36.081180033579,1.8050499110056,311.072755529544));
#15570=CARTESIAN_POINT('Ctrl Pts',(-36.1373107395428,1.73032884439181,311.077789552448));
#15571=CARTESIAN_POINT('Ctrl Pts',(-36.1897513839202,1.65312929951775,311.082823575352));
#15572=CARTESIAN_POINT('Ctrl Pts',(-36.2422022994558,1.57591463414406,311.087858584233));
#15573=CARTESIAN_POINT('Ctrl Pts',(-36.2909614687216,1.49622089409765,311.092893593113));
#15574=CARTESIAN_POINT('Ctrl Pts',(-36.3358016426966,1.41444083232241,311.097928601994));
#15575=CARTESIAN_POINT('Ctrl Pts',(-36.3806910870742,1.33257091057981,311.102969143344));
#15576=CARTESIAN_POINT('Ctrl Pts',(-36.4216527265697,1.24861048125042,311.108009684694));
#15577=CARTESIAN_POINT('Ctrl Pts',(-36.4585057337172,1.16297605997046,311.113050226045));
#15578=CARTESIAN_POINT('Ctrl Pts',(-36.4953813827839,1.07728902622267,311.118093864226));
#15579=CARTESIAN_POINT('Ctrl Pts',(-36.5281432182783,0.989926368693434,
311.123137502407));
#15580=CARTESIAN_POINT('Ctrl Pts',(-36.5566597098044,0.901321631153508,
311.128181140589));
#15581=CARTESIAN_POINT('Ctrl Pts',(-36.5852223757779,0.812573423131264,
311.133232945525));
#15582=CARTESIAN_POINT('Ctrl Pts',(-36.6095258587224,0.722579548340074,
311.138284750462));
#15583=CARTESIAN_POINT('Ctrl Pts',(-36.6294893627108,0.631785468102651,
311.143336555398));
#15584=CARTESIAN_POINT('Ctrl Pts',(-36.6395947846885,0.585825976501504,
311.145893752805));
#15585=CARTESIAN_POINT('Ctrl Pts',(-36.648588983502,0.539661560233308,311.148450950212));
#15586=CARTESIAN_POINT('Ctrl Pts',(-36.6564665537928,0.49335040206328,311.151008147619));
#15587=CARTESIAN_POINT('Ctrl Pts',(-36.6809714621854,0.349289397639362,
311.158962870444));
#15588=CARTESIAN_POINT('Ctrl Pts',(-36.6947476817154,0.203354132616775,
311.16691759327));
#15589=CARTESIAN_POINT('Ctrl Pts',(-36.6975782807065,0.0568199948794944,
311.174872316094));
#15590=CARTESIAN_POINT('Ctrl Pts',(-36.6979283747003,0.038696367452575,
311.1758561717));
#15591=CARTESIAN_POINT('Ctrl Pts',(-36.6981110795063,0.0205636243529551,
311.176840027305));
#15592=CARTESIAN_POINT('Ctrl Pts',(-36.6981260264713,0.00242422312990352,
311.17782388291));
#15593=CARTESIAN_POINT('',(-36.6981269603261,0.000618107681218697,312.177823882879));
#15594=CARTESIAN_POINT('Ctrl Pts',(-36.6981260264717,0.00242422262950888,
311.177823882937));
#15595=CARTESIAN_POINT('Ctrl Pts',(-36.6982015303164,-0.08920607281627,
311.182793781264));
#15596=CARTESIAN_POINT('Ctrl Pts',(-36.6939920174391,-0.180989576697442,
311.18776367959));
#15597=CARTESIAN_POINT('Ctrl Pts',(-36.6854811606969,-0.272485502704996,
311.192733577917));
#15598=CARTESIAN_POINT('Ctrl Pts',(-36.6769797232138,-0.363880167012936,
311.197697975885));
#15599=CARTESIAN_POINT('Ctrl Pts',(-36.6641864429127,-0.454987431746313,
311.202662373854));
#15600=CARTESIAN_POINT('Ctrl Pts',(-36.6471370372109,-0.54536695058065,
311.207626771822));
#15601=CARTESIAN_POINT('Ctrl Pts',(-36.6300979046698,-0.635692011017376,
311.212588178481));
#15602=CARTESIAN_POINT('Ctrl Pts',(-36.6088078208921,-0.725289746294086,
311.217549585139));
#15603=CARTESIAN_POINT('Ctrl Pts',(-36.5833541612158,-0.813726441564893,
311.222510991797));
#15604=CARTESIAN_POINT('Ctrl Pts',(-36.5579082237446,-0.902136306654335,
311.22747089325));
#15605=CARTESIAN_POINT('Ctrl Pts',(-36.5283013451067,-0.989385390561597,
311.232430794703));
#15606=CARTESIAN_POINT('Ctrl Pts',(-36.4946713648304,-1.07505297552896,
311.237390696155));
#15607=CARTESIAN_POINT('Ctrl Pts',(-36.461041526873,-1.1607201979592,311.242350576618));
#15608=CARTESIAN_POINT('Ctrl Pts',(-36.4233887902628,-1.24480550829142,
311.24731045708));
#15609=CARTESIAN_POINT('Ctrl Pts',(-36.3818994618245,-1.32690734844808,
311.252270337543));
#15610=CARTESIAN_POINT('Ctrl Pts',(-36.3403707750732,-1.40908707344996,
311.257234923132));
#15611=CARTESIAN_POINT('Ctrl Pts',(-36.2949984353924,-1.48927916026966,
311.262199508721));
#15612=CARTESIAN_POINT('Ctrl Pts',(-36.2460149194563,-1.56710633791168,
311.26716409431));
#15613=CARTESIAN_POINT('Ctrl Pts',(-36.1970083707436,-1.64497011104825,
311.27213101432));
#15614=CARTESIAN_POINT('Ctrl Pts',(-36.1443875290459,-1.72046638555712,
311.277097934331));
#15615=CARTESIAN_POINT('Ctrl Pts',(-36.0884270842775,-1.79324857024776,
311.282064854342));
#15616=CARTESIAN_POINT('Ctrl Pts',(-36.0323714334215,-1.86615458002741,
311.287040224625));
#15617=CARTESIAN_POINT('Ctrl Pts',(-35.9729651288959,-1.9363369277628,311.292015594909));
#15618=CARTESIAN_POINT('Ctrl Pts',(-35.9105217632539,-2.00348379401826,
311.296990965192));
#15619=CARTESIAN_POINT('Ctrl Pts',(-35.8564355063254,-2.06164405848986,
311.301300456725));
#15620=CARTESIAN_POINT('Ctrl Pts',(-35.8000714528542,-2.11752745102219,
311.305609948257));
#15621=CARTESIAN_POINT('Ctrl Pts',(-35.7416530584122,-2.17095609620858,
311.309919439789));
#15622=CARTESIAN_POINT('Ctrl Pts',(-35.6731656491964,-2.23359372125257,
311.314971716779));
#15623=CARTESIAN_POINT('Ctrl Pts',(-35.601588345643,-2.29309973061535,311.32002399377));
#15624=CARTESIAN_POINT('Ctrl Pts',(-35.5272393903716,-2.34915410097772,
311.32507627076));
#15625=CARTESIAN_POINT('Ctrl Pts',(-35.452992976089,-2.40513116197449,311.330121579725));
#15626=CARTESIAN_POINT('Ctrl Pts',(-35.3759828577769,-2.4576657784631,311.335166888689));
#15627=CARTESIAN_POINT('Ctrl Pts',(-35.2965627104359,-2.50647599227066,
311.340212197653));
#15628=CARTESIAN_POINT('Ctrl Pts',(-35.2172275586343,-2.55523396932734,
311.345252107122));
#15629=CARTESIAN_POINT('Ctrl Pts',(-35.1354878808409,-2.60027523483785,
311.35029201659));
#15630=CARTESIAN_POINT('Ctrl Pts',(-35.0517280019881,-2.64135989768432,
311.355331926058));
#15631=CARTESIAN_POINT('Ctrl Pts',(-34.9680285000898,-2.6824149453158,311.36036820259));
#15632=CARTESIAN_POINT('Ctrl Pts',(-34.8823120893024,-2.71951886405753,
311.365404479121));
#15633=CARTESIAN_POINT('Ctrl Pts',(-34.7949885596874,-2.75247719559713,
311.370440755652));
#15634=CARTESIAN_POINT('Ctrl Pts',(-34.7076967831545,-2.78542354263936,
311.375475200863));
#15635=CARTESIAN_POINT('Ctrl Pts',(-34.6187994639651,-2.81422714045836,
311.380509646075));
#15636=CARTESIAN_POINT('Ctrl Pts',(-34.5287263166366,-2.83874168161893,
311.385544091286));
#15637=CARTESIAN_POINT('Ctrl Pts',(-34.438660724638,-2.86325416650133,311.390578114208));
#15638=CARTESIAN_POINT('Ctrl Pts',(-34.3474199293088,-2.88347819353403,
311.395612137131));
#15639=CARTESIAN_POINT('Ctrl Pts',(-34.2554476394487,-2.89931766528675,
311.400646160053));
#15640=CARTESIAN_POINT('Ctrl Pts',(-34.1634573356725,-2.9151602393969,311.405681168952));
#15641=CARTESIAN_POINT('Ctrl Pts',(-34.070735690674,-2.92661647767692,311.41071617785));
#15642=CARTESIAN_POINT('Ctrl Pts',(-33.9777342682891,-2.93364180326024,
311.415751186749));
#15643=CARTESIAN_POINT('Ctrl Pts',(-33.8846306559204,-2.94067484827288,
311.420791728116));
#15644=CARTESIAN_POINT('Ctrl Pts',(-33.7912470961995,-2.94326722859512,
311.425832269483));
#15645=CARTESIAN_POINT('Ctrl Pts',(-33.6980376016428,-2.94142645987693,
311.430872810851));
#15646=CARTESIAN_POINT('Ctrl Pts',(-33.6047708406207,-2.93958456021902,
311.435916449048));
#15647=CARTESIAN_POINT('Ctrl Pts',(-33.5116788005859,-2.9333041191332,311.440960087246));
#15648=CARTESIAN_POINT('Ctrl Pts',(-33.419210621842,-2.92264457933385,311.446003725443));
#15649=CARTESIAN_POINT('Ctrl Pts',(-33.3265927168774,-2.9119677794064,311.451055530395));
#15650=CARTESIAN_POINT('Ctrl Pts',(-33.2346011277437,-2.89689779674547,
311.456107335347));
#15651=CARTESIAN_POINT('Ctrl Pts',(-33.1436748748383,-2.87754519746376,
311.461159140299));
#15652=CARTESIAN_POINT('Ctrl Pts',(-33.0976484816358,-2.86774901302232,
311.463716337518));
#15653=CARTESIAN_POINT('Ctrl Pts',(-33.0518948267786,-2.85685627741267,
311.466273534738));
#15654=CARTESIAN_POINT('Ctrl Pts',(-33.006469123943,-2.84488611916128,311.468830731957));
#15655=CARTESIAN_POINT('Ctrl Pts',(-32.9167211621574,-2.82123657191711,
311.47388300906));
#15656=CARTESIAN_POINT('Ctrl Pts',(-32.8279323153016,-2.79329347552532,
311.478935286163));
#15657=CARTESIAN_POINT('Ctrl Pts',(-32.7405439656881,-2.76115103699805,
311.483987563266));
#15658=CARTESIAN_POINT('Ctrl Pts',(-32.6532761407779,-2.72905292884073,
311.489032872344));
#15659=CARTESIAN_POINT('Ctrl Pts',(-32.5674053882141,-2.69276713935733,
311.494078181422));
#15660=CARTESIAN_POINT('Ctrl Pts',(-32.483360280933,-2.65243827723499,311.4991234905));
#15661=CARTESIAN_POINT('Ctrl Pts',(-32.3994051188064,-2.61215257509963,
311.504163400083));
#15662=CARTESIAN_POINT('Ctrl Pts',(-32.3172721168548,-2.56783259185325,
311.509203309667));
#15663=CARTESIAN_POINT('Ctrl Pts',(-32.2373710843367,-2.51967148491972,
311.51424321925));
#15664=CARTESIAN_POINT('Ctrl Pts',(-32.1575276471636,-2.47154509412792,
311.519279495898));
#15665=CARTESIAN_POINT('Ctrl Pts',(-32.0799133609419,-2.41958331172726,
311.524315772545));
#15666=CARTESIAN_POINT('Ctrl Pts',(-32.0049136338218,-2.36402530816736,
311.529352049192));
#15667=CARTESIAN_POINT('Ctrl Pts',(-31.9299411785199,-2.30848750691804,
311.534386494521));
#15668=CARTESIAN_POINT('Ctrl Pts',(-31.857581750232,-2.2493563465259,311.53942093985));
#15669=CARTESIAN_POINT('Ctrl Pts',(-31.7881910703001,-2.18691382481923,
311.544455385178));
#15670=CARTESIAN_POINT('Ctrl Pts',(-31.7188062108451,-2.12447654077925,
311.549489408218));
#15671=CARTESIAN_POINT('Ctrl Pts',(-31.6523899347525,-2.05872874497333,
311.554523431259));
#15672=CARTESIAN_POINT('Ctrl Pts',(-31.5892633338439,-1.98999139265296,
311.559557454299));
#15673=CARTESIAN_POINT('Ctrl Pts',(-31.5261243688003,-1.92124057726179,
311.564592463315));
#15674=CARTESIAN_POINT('Ctrl Pts',(-31.4662766587785,-1.8494993699054,311.569627472332));
#15675=CARTESIAN_POINT('Ctrl Pts',(-31.4100022394138,-1.77512323213051,
311.574662481349));
#15676=CARTESIAN_POINT('Ctrl Pts',(-31.3536659857059,-1.70066536984051,
311.579703022834));
#15677=CARTESIAN_POINT('Ctrl Pts',(-31.3009111285474,-1.62356715267035,
311.58474356432));
#15678=CARTESIAN_POINT('Ctrl Pts',(-31.2519772385529,-1.54421431341205,
311.589784105805));
#15679=CARTESIAN_POINT('Ctrl Pts',(-31.2030132843353,-1.46481272100019,
311.594827744121));
#15680=CARTESIAN_POINT('Ctrl Pts',(-31.1578751855412,-1.38315413735048,
311.599871382437));
#15681=CARTESIAN_POINT('Ctrl Pts',(-31.1167562219282,-1.29964832263674,
311.604915020754));
#15682=CARTESIAN_POINT('Ctrl Pts',(-31.0755706777221,-1.21600729374959,
311.609966825823));
#15683=CARTESIAN_POINT('Ctrl Pts',(-31.0384174376808,-1.13051346942785,
311.615018630892));
#15684=CARTESIAN_POINT('Ctrl Pts',(-31.005441324204,-1.04359579053353,311.620070435962));
#15685=CARTESIAN_POINT('Ctrl Pts',(-30.9887489961861,-0.99959853756195,
311.622627632017));
#15686=CARTESIAN_POINT('Ctrl Pts',(-30.9731261874234,-0.955236679455002,
311.625184828072));
#15687=CARTESIAN_POINT('Ctrl Pts',(-30.958586720807,-0.910566990931599,
311.627742024127));
#15688=CARTESIAN_POINT('Ctrl Pts',(-30.9298609591932,-0.822312665120583,
311.632794300543));
#15689=CARTESIAN_POINT('Ctrl Pts',(-30.9052639847033,-0.732539269766924,
311.637846576958));
#15690=CARTESIAN_POINT('Ctrl Pts',(-30.8849556511083,-0.641668871198852,
311.642898853374));
#15691=CARTESIAN_POINT('Ctrl Pts',(-30.8646753264713,-0.550923799761345,
311.647944161764));
#15692=CARTESIAN_POINT('Ctrl Pts',(-30.8486719852641,-0.459085161372459,
311.652989470153));
#15693=CARTESIAN_POINT('Ctrl Pts',(-30.8370561740245,-0.366591551295231,
311.658034778543));
#15694=CARTESIAN_POINT('Ctrl Pts',(-30.8254527940393,-0.2741969279853,311.663074687437));
#15695=CARTESIAN_POINT('Ctrl Pts',(-30.8182276659885,-0.181149164659398,
311.668114596332));
#15696=CARTESIAN_POINT('Ctrl Pts',(-30.8154403620448,-0.0878973765402973,
311.673154505227));
#15697=CARTESIAN_POINT('Ctrl Pts',(-30.8126550672823,0.00528719259989155,
311.678190781188));
#15698=CARTESIAN_POINT('Ctrl Pts',(-30.8143012515402,0.098675051434181,
311.68322705715));
#15699=CARTESIAN_POINT('Ctrl Pts',(-30.8203865910775,0.191812677162036,
311.688263333111));
#15700=CARTESIAN_POINT('Ctrl Pts',(-30.8264697178317,0.284916435697699,
311.693297777755));
#15701=CARTESIAN_POINT('Ctrl Pts',(-30.8369887641721,0.377769699025832,
311.6983322224));
#15702=CARTESIAN_POINT('Ctrl Pts',(-30.8518993257529,0.469920705470309,
311.703366667044));
#15703=CARTESIAN_POINT('Ctrl Pts',(-30.8668086366464,0.562063982353962,
311.708400689403));
#15704=CARTESIAN_POINT('Ctrl Pts',(-30.8861086592593,0.653504680946815,
311.713434711761));
#15705=CARTESIAN_POINT('Ctrl Pts',(-30.9097034849681,0.743799051683824,
311.71846873412));
#15706=CARTESIAN_POINT('Ctrl Pts',(-30.9333029320361,0.834111107769477,
311.723503742459));
#15707=CARTESIAN_POINT('Ctrl Pts',(-30.9611987401457,0.923275960390066,
311.728538750797));
#15708=CARTESIAN_POINT('Ctrl Pts',(-30.9932448407682,1.0108640040238,311.733573759136));
#15709=CARTESIAN_POINT('Ctrl Pts',(-31.0253261537173,1.09854828959467,311.738614299953));
#15710=CARTESIAN_POINT('Ctrl Pts',(-31.061566709298,1.18465188984667,311.74365484077));
#15711=CARTESIAN_POINT('Ctrl Pts',(-31.10177199305,1.26876450257491,311.748695381587));
#15712=CARTESIAN_POINT('Ctrl Pts',(-31.1420019783427,1.35292879286734,311.753739019239));
#15713=CARTESIAN_POINT('Ctrl Pts',(-31.1862013308537,1.43509926946008,311.758782656891));
#15714=CARTESIAN_POINT('Ctrl Pts',(-31.2341302670182,1.51489153124244,311.763826294542));
#15715=CARTESIAN_POINT('Ctrl Pts',(-31.2821368107472,1.59481299437146,311.768878098961));
#15716=CARTESIAN_POINT('Ctrl Pts',(-31.3338847479845,1.67234818587392,311.773929903379));
#15717=CARTESIAN_POINT('Ctrl Pts',(-31.3890919270446,1.74714305190724,311.778981707798));
#15718=CARTESIAN_POINT('Ctrl Pts',(-31.417037576359,1.7850039086341,311.781538910631));
#15719=CARTESIAN_POINT('Ctrl Pts',(-31.4458689738935,1.82216314442311,311.784096113463));
#15720=CARTESIAN_POINT('Ctrl Pts',(-31.4755458783913,1.85857839021061,311.786653316296));
#15721=CARTESIAN_POINT('Ctrl Pts',(-31.534178676157,1.9305241600941,311.791705593785));
#15722=CARTESIAN_POINT('Ctrl Pts',(-31.5963245793649,1.99982180600417,311.796757871274));
#15723=CARTESIAN_POINT('Ctrl Pts',(-31.6617153560105,2.06610836107927,311.801810148764));
#15724=CARTESIAN_POINT('Ctrl Pts',(-31.7270159466201,2.13230349467329,311.806855458223));
#15725=CARTESIAN_POINT('Ctrl Pts',(-31.7955522084267,2.19549547615848,311.811900767682));
#15726=CARTESIAN_POINT('Ctrl Pts',(-31.8670153102018,2.25535383654962,311.816946077142));
#15727=CARTESIAN_POINT('Ctrl Pts',(-31.9384019320278,2.31514813640814,311.821985987101));
#15728=CARTESIAN_POINT('Ctrl Pts',(-32.0127088291449,2.37161562267808,311.827025897061));
#15729=CARTESIAN_POINT('Ctrl Pts',(-32.0895907196,2.42446298011023,311.83206580702));
#15730=CARTESIAN_POINT('Ctrl Pts',(-32.1664171908701,2.47727224329867,311.837102084034));
#15731=CARTESIAN_POINT('Ctrl Pts',(-32.2458146010754,2.52646631349717,311.842138361048));
#15732=CARTESIAN_POINT('Ctrl Pts',(-32.327405856766,2.57179311428893,311.847174638063));
#15733=CARTESIAN_POINT('Ctrl Pts',(-32.4089674436963,2.61710343304501,311.852209083752));
#15734=CARTESIAN_POINT('Ctrl Pts',(-32.4927209033532,2.65854906051797,311.857243529441));
#15735=CARTESIAN_POINT('Ctrl Pts',(-32.5782624164361,2.69592265528625,311.862277975131));
#15736=CARTESIAN_POINT('Ctrl Pts',(-32.6637967542063,2.73329311511788,311.867311998525));
#15737=CARTESIAN_POINT('Ctrl Pts',(-32.7511184400287,2.76659204366298,311.87234602192));
#15738=CARTESIAN_POINT('Ctrl Pts',(-32.8398024957292,2.79565973548009,311.877380045315));
#15739=CARTESIAN_POINT('Ctrl Pts',(-32.9285039211922,2.82473312052919,311.882415054679));
#15740=CARTESIAN_POINT('Ctrl Pts',(-33.018567824221,2.84957348497027,311.887450064043));
#15741=CARTESIAN_POINT('Ctrl Pts',(-33.1095539506286,2.87007095019703,311.892485073408));
#15742=CARTESIAN_POINT('Ctrl Pts',(-33.2006400523817,2.89059093799119,311.897525615229));
#15743=CARTESIAN_POINT('Ctrl Pts',(-33.2926499661888,2.90675840337116,311.90256615705));
#15744=CARTESIAN_POINT('Ctrl Pts',(-33.3851334272274,2.91851464793662,311.907606698871));
#15745=CARTESIAN_POINT('Ctrl Pts',(-33.4776737085474,2.9302781153408,311.912650337516));
#15746=CARTESIAN_POINT('Ctrl Pts',(-33.5706876737533,2.93762493153835,311.917693976161));
#15747=CARTESIAN_POINT('Ctrl Pts',(-33.6637223142929,2.94054848104763,311.922737614806));
#15748=CARTESIAN_POINT('Ctrl Pts',(-33.7569075980058,2.94347676441489,311.927789420191));
#15749=CARTESIAN_POINT('Ctrl Pts',(-33.8501131802449,2.94196748977706,311.932841225576));
#15750=CARTESIAN_POINT('Ctrl Pts',(-33.9428886175165,2.93606609388428,311.937893030961));
#15751=CARTESIAN_POINT('Ctrl Pts',(-33.9898509674947,2.93307884394587,311.940450223463));
#15752=CARTESIAN_POINT('Ctrl Pts',(-34.0367032179707,2.92896701435596,311.943007415965));
#15753=CARTESIAN_POINT('Ctrl Pts',(-34.0833879581403,2.92374148682963,311.945564608466));
#15754=CARTESIAN_POINT('Ctrl Pts',(-34.1756235996956,2.9134173448915,311.950616886579));
#15755=CARTESIAN_POINT('Ctrl Pts',(-34.2675357765239,2.89870573751808,311.955669164692));
#15756=CARTESIAN_POINT('Ctrl Pts',(-34.3586740912813,2.87963557298944,311.960721442804));
#15757=CARTESIAN_POINT('Ctrl Pts',(-34.4496867096227,2.86059170970787,311.965766752901));
#15758=CARTESIAN_POINT('Ctrl Pts',(-34.5399271556838,2.83720132458121,311.970812062998));
#15759=CARTESIAN_POINT('Ctrl Pts',(-34.6289503631172,2.80954505585649,311.975857373094));
#15760=CARTESIAN_POINT('Ctrl Pts',(-34.7178782979768,2.78191838485106,311.980897283704));
#15761=CARTESIAN_POINT('Ctrl Pts',(-34.805591161522,2.7500350356528,311.985937194313));
#15762=CARTESIAN_POINT('Ctrl Pts',(-34.8916553791004,2.71402641063402,311.990977104922));
#15763=CARTESIAN_POINT('Ctrl Pts',(-34.9776575588258,2.67804374178903,311.996013382602));
#15764=CARTESIAN_POINT('Ctrl Pts',(-35.0620130460367,2.63794187860835,312.001049660282));
#15765=CARTESIAN_POINT('Ctrl Pts',(-35.1443057044382,2.59390130010153,312.006085937962));
#15766=CARTESIAN_POINT('Ctrl Pts',(-35.2265684391902,2.54987673584024,312.011120384326));
#15767=CARTESIAN_POINT('Ctrl Pts',(-35.3067694439806,2.50191651090943,312.01615483069));
#15768=CARTESIAN_POINT('Ctrl Pts',(-35.3845157142294,2.45024779922945,312.021189277055));
#15769=CARTESIAN_POINT('Ctrl Pts',(-35.4622554631727,2.39858342148666,312.026223301133));
#15770=CARTESIAN_POINT('Ctrl Pts',(-35.5375405170566,2.34321142151244,312.031257325212));
#15771=CARTESIAN_POINT('Ctrl Pts',(-35.6100064567246,2.28440255944164,312.03629134929));
#15772=CARTESIAN_POINT('Ctrl Pts',(-35.6824865897655,2.22558217890967,312.041326359346));
#15773=CARTESIAN_POINT('Ctrl Pts',(-35.7521461672983,2.16332387961225,312.046361369402));
#15774=CARTESIAN_POINT('Ctrl Pts',(-35.8186543834119,2.09793824905908,312.051396379458));
#15775=CARTESIAN_POINT('Ctrl Pts',(-35.8852356786866,2.03248077284068,312.056436921978));
#15776=CARTESIAN_POINT('Ctrl Pts',(-35.9486583832679,1.96388941802114,312.061477464498));
#15777=CARTESIAN_POINT('Ctrl Pts',(-36.0086292938647,1.89251090615609,312.066518007017));
#15778=CARTESIAN_POINT('Ctrl Pts',(-36.0686370496362,1.82108854046741,312.071561646366));
#15779=CARTESIAN_POINT('Ctrl Pts',(-36.1251885204058,1.74687596180443,312.076605285716));
#15780=CARTESIAN_POINT('Ctrl Pts',(-36.1780328000423,1.67025040579686,312.081648925065));
#15781=CARTESIAN_POINT('Ctrl Pts',(-36.2309626459783,1.59350077646818,312.086700731155));
#15782=CARTESIAN_POINT('Ctrl Pts',(-36.2801730828093,1.51433074652193,312.091752537245));
#15783=CARTESIAN_POINT('Ctrl Pts',(-36.3254583509524,1.43314358624782,312.096804343336));
#15784=CARTESIAN_POINT('Ctrl Pts',(-36.3483814087769,1.39204726406881,312.099361529102));
#15785=CARTESIAN_POINT('Ctrl Pts',(-36.3702994732512,1.35043443810575,312.101918714868));
#15786=CARTESIAN_POINT('Ctrl Pts',(-36.3911905990756,1.30835926332855,312.104475900635));
#15787=CARTESIAN_POINT('Ctrl Pts',(-36.4354099813449,1.21930048051519,312.109888590018));
#15788=CARTESIAN_POINT('Ctrl Pts',(-36.4751667113802,1.12788489735598,312.1153012794));
#15789=CARTESIAN_POINT('Ctrl Pts',(-36.5102214562109,1.03456651085936,312.120713968783));
#15790=CARTESIAN_POINT('Ctrl Pts',(-36.5451612253897,0.94155419825884,312.126108905148));
#15791=CARTESIAN_POINT('Ctrl Pts',(-36.5754296261192,0.846651844587571,
312.131503841514));
#15792=CARTESIAN_POINT('Ctrl Pts',(-36.6008348302367,0.750334261706711,
312.136898777879));
#15793=CARTESIAN_POINT('Ctrl Pts',(-36.6261882476559,0.654213015355424,
312.142282717051));
#15794=CARTESIAN_POINT('Ctrl Pts',(-36.6466981192475,0.556682616613729,
312.147666656223));
#15795=CARTESIAN_POINT('Ctrl Pts',(-36.6622213344253,0.458235601217396,
312.153050595395));
#15796=CARTESIAN_POINT('Ctrl Pts',(-36.6776995355044,0.360074061710941,
312.158418922262));
#15797=CARTESIAN_POINT('Ctrl Pts',(-36.688219842539,0.261001543111834,312.163787249129));
#15798=CARTESIAN_POINT('Ctrl Pts',(-36.6936897286263,0.16152202257669,312.169155575996));
#15799=CARTESIAN_POINT('Ctrl Pts',(-36.69663382725,0.107978399396601,312.172045011624));
#15800=CARTESIAN_POINT('Ctrl Pts',(-36.6981156782847,0.0543171084516736,
312.174934447252));
#15801=CARTESIAN_POINT('Ctrl Pts',(-36.6981269603261,0.000618107681204032,
312.177823882879));
#15802=CARTESIAN_POINT('',(-36.6981257736749,-0.00271372645954632,313.177823882956));
#15803=CARTESIAN_POINT('Ctrl Pts',(-36.6981269603262,0.000618107113904726,
312.17782388291));
#15804=CARTESIAN_POINT('Ctrl Pts',(-36.6981472510316,-0.0959594160750109,
312.183020525908));
#15805=CARTESIAN_POINT('Ctrl Pts',(-36.693407656044,-0.192478386360223,
312.188217168906));
#15806=CARTESIAN_POINT('Ctrl Pts',(-36.683951507351,-0.288457626098284,
312.193413811904));
#15807=CARTESIAN_POINT('Ctrl Pts',(-36.6744864103721,-0.384527690305954,
312.198615372448));
#15808=CARTESIAN_POINT('Ctrl Pts',(-36.6602959088366,-0.48005660696899,
312.203816932992));
#15809=CARTESIAN_POINT('Ctrl Pts',(-36.6414748179091,-0.574571244878503,
312.209018493536));
#15810=CARTESIAN_POINT('Ctrl Pts',(-36.6226162191874,-0.669274237203749,
312.214230420061));
#15811=CARTESIAN_POINT('Ctrl Pts',(-36.5991086761896,-0.762958518130133,
312.219442346586));
#15812=CARTESIAN_POINT('Ctrl Pts',(-36.5710976252041,-0.855163447205775,
312.22465427311));
#15813=CARTESIAN_POINT('Ctrl Pts',(-36.5430558604506,-0.947469477836219,
312.229871914448));
#15814=CARTESIAN_POINT('Ctrl Pts',(-36.5105008799693,-1.03829254542981,
312.235089555785));
#15815=CARTESIAN_POINT('Ctrl Pts',(-36.473626493746,-1.12719148274162,312.240307197122));
#15816=CARTESIAN_POINT('Ctrl Pts',(-36.4366733133957,-1.21628038156532,
312.245535987648));
#15817=CARTESIAN_POINT('Ctrl Pts',(-36.3953824581606,-1.30343657214762,
312.250764778174));
#15818=CARTESIAN_POINT('Ctrl Pts',(-36.34999418024,-1.38824247964953,312.2559935687));
#15819=CARTESIAN_POINT('Ctrl Pts',(-36.3286008411863,-1.42821494866716,
312.258458110068));
#15820=CARTESIAN_POINT('Ctrl Pts',(-36.3062978410755,-1.46766568669913,
312.260922651436));
#15821=CARTESIAN_POINT('Ctrl Pts',(-36.2831135879918,-1.50655332191096,
312.263387192804));
#15822=CARTESIAN_POINT('Ctrl Pts',(-36.2355861173756,-1.58627255777278,
312.268439476224));
#15823=CARTESIAN_POINT('Ctrl Pts',(-36.1841972653882,-1.66388364616725,
312.273491759643));
#15824=CARTESIAN_POINT('Ctrl Pts',(-36.1291595320973,-1.73898841901895,
312.278544043063));
#15825=CARTESIAN_POINT('Ctrl Pts',(-36.0741977062961,-1.81398960812129,
312.283589358424));
#15826=CARTESIAN_POINT('Ctrl Pts',(-36.0155972597245,-1.88649099532476,
312.288634673786));
#15827=CARTESIAN_POINT('Ctrl Pts',(-35.95361559243,-1.95612064994633,312.293679989147));
#15828=CARTESIAN_POINT('Ctrl Pts',(-35.8917002584041,-2.02567578636307,
312.298719904972));
#15829=CARTESIAN_POINT('Ctrl Pts',(-35.8264111899827,-2.09236496889872,
312.303759820796));
#15830=CARTESIAN_POINT('Ctrl Pts',(-35.7580472611431,-2.15584771474055,
312.308799736621));
#15831=CARTESIAN_POINT('Ctrl Pts',(-35.6897326124361,-2.21928469905018,
312.313836019423));
#15832=CARTESIAN_POINT('Ctrl Pts',(-35.618347833547,-2.27951953938701,312.318872302225));
#15833=CARTESIAN_POINT('Ctrl Pts',(-35.5442292776944,-2.33624791810079,
312.323908585027));
#15834=CARTESIAN_POINT('Ctrl Pts',(-35.4701376740366,-2.39295566831891,
312.328943036454));
#15835=CARTESIAN_POINT('Ctrl Pts',(-35.39331462073,-2.44615922024994,312.333977487881));
#15836=CARTESIAN_POINT('Ctrl Pts',(-35.3141294281189,-2.49559462106297,
312.339011939308));
#15837=CARTESIAN_POINT('Ctrl Pts',(-35.2349508785342,-2.54502587462749,
312.344045968383));
#15838=CARTESIAN_POINT('Ctrl Pts',(-35.153410960587,-2.5906893704818,312.349079997459));
#15839=CARTESIAN_POINT('Ctrl Pts',(-35.0699068567329,-2.63236520156467,
312.354114026534));
#15840=CARTESIAN_POINT('Ctrl Pts',(-34.9863863987443,-2.67404919478714,
312.359149041515));
#15841=CARTESIAN_POINT('Ctrl Pts',(-34.9009013885088,-2.71174377417091,
312.364184056497));
#15842=CARTESIAN_POINT('Ctrl Pts',(-34.8138713796262,-2.74527610283581,
312.369219071478));
#15843=CARTESIAN_POINT('Ctrl Pts',(-34.7267457447288,-2.7788452758375,312.374259618785));
#15844=CARTESIAN_POINT('Ctrl Pts',(-34.6380721377659,-2.80824290918259,
312.379300166093));
#15845=CARTESIAN_POINT('Ctrl Pts',(-34.5482874714049,-2.83334534209292,
312.384340713401));
#15846=CARTESIAN_POINT('Ctrl Pts',(-34.4584476440895,-2.85846319717071,
312.389384357467));
#15847=CARTESIAN_POINT('Ctrl Pts',(-34.3674958311872,-2.87928049935423,
312.394428001532));
#15848=CARTESIAN_POINT('Ctrl Pts',(-34.2758792465645,-2.89572471558444,
312.399471645598));
#15849=CARTESIAN_POINT('Ctrl Pts',(-34.1841143178764,-2.91219555801879,
312.404523456249));
#15850=CARTESIAN_POINT('Ctrl Pts',(-34.0916829085481,-2.92427912097878,
312.409575266901));
#15851=CARTESIAN_POINT('Ctrl Pts',(-33.9990372770051,-2.93195474207839,
312.414627077552));
#15852=CARTESIAN_POINT('Ctrl Pts',(-33.9521417224921,-2.93584000360344,
312.417184213359));
#15853=CARTESIAN_POINT('Ctrl Pts',(-33.9051912835796,-2.9385966924718,312.419741349166));
#15854=CARTESIAN_POINT('Ctrl Pts',(-33.8582443398703,-2.94022721129784,
312.422298484973));
#15855=CARTESIAN_POINT('Ctrl Pts',(-33.7654884768215,-2.94344872411588,
312.427350769956));
#15856=CARTESIAN_POINT('Ctrl Pts',(-33.6724135305641,-2.94228243713677,
312.43240305494));
#15857=CARTESIAN_POINT('Ctrl Pts',(-33.5794693066669,-2.93669134409157,
312.437455339923));
#15858=CARTESIAN_POINT('Ctrl Pts',(-33.4866532680901,-2.93110796208018,
312.442500656977));
#15859=CARTESIAN_POINT('Ctrl Pts',(-33.3939680332237,-2.92111192695525,
312.447545974032));
#15860=CARTESIAN_POINT('Ctrl Pts',(-33.3018656686103,-2.90671818720992,
312.452591291086));
#15861=CARTESIAN_POINT('Ctrl Pts',(-33.2098618703539,-2.89233985139583,
312.457631208729));
#15862=CARTESIAN_POINT('Ctrl Pts',(-33.1184401390671,-2.87357323376419,
312.462671126372));
#15863=CARTESIAN_POINT('Ctrl Pts',(-33.0280485666081,-2.85048517941255,
312.467711044015));
#15864=CARTESIAN_POINT('Ctrl Pts',(-32.9377221497179,-2.82741376726849,
312.472747328812));
#15865=CARTESIAN_POINT('Ctrl Pts',(-32.8484248449244,-2.80002721943948,
312.477783613609));
#15866=CARTESIAN_POINT('Ctrl Pts',(-32.7605946403837,-2.76844347434933,
312.482819898405));
#15867=CARTESIAN_POINT('Ctrl Pts',(-32.6727963721871,-2.73687121356978,
312.487854351936));
#15868=CARTESIAN_POINT('Ctrl Pts',(-32.5864645620957,-2.70110493759086,
312.492888805466));
#15869=CARTESIAN_POINT('Ctrl Pts',(-32.5020211150125,-2.66131215115555,
312.497923258996));
#15870=CARTESIAN_POINT('Ctrl Pts',(-32.4175847503165,-2.62152270219566,
312.502957290279));
#15871=CARTESIAN_POINT('Ctrl Pts',(-32.3350368355249,-2.57770760376478,
312.507991321563));
#15872=CARTESIAN_POINT('Ctrl Pts',(-32.2547773439412,-2.5300816457994,312.513025352847));
#15873=CARTESIAN_POINT('Ctrl Pts',(-32.1745021320575,-2.4824463594128,312.518060370138));
#15874=CARTESIAN_POINT('Ctrl Pts',(-32.0965166154096,-2.43099895809983,
312.523095387429));
#15875=CARTESIAN_POINT('Ctrl Pts',(-32.0211933139959,-2.3759985306241,312.528130404721));
#15876=CARTESIAN_POINT('Ctrl Pts',(-31.9457872475172,-2.32093766880901,
312.533170954477));
#15877=CARTESIAN_POINT('Ctrl Pts',(-31.8730495947316,-2.26231625025901,
312.538211504233));
#15878=CARTESIAN_POINT('Ctrl Pts',(-31.8033209375348,-2.20043458974651,
312.54325205399));
#15879=CARTESIAN_POINT('Ctrl Pts',(-31.7335494400637,-2.13851491004045,
312.548295700587));
#15880=CARTESIAN_POINT('Ctrl Pts',(-31.6667909361748,-2.07333131083482,
312.553339347184));
#15881=CARTESIAN_POINT('Ctrl Pts',(-31.6033486065793,-2.00522045672617,
312.558382993781));
#15882=CARTESIAN_POINT('Ctrl Pts',(-31.5398035509794,-1.93699931732458,
312.563434807065));
#15883=CARTESIAN_POINT('Ctrl Pts',(-31.4795856759634,-1.86584179924721,
312.568486620349));
#15884=CARTESIAN_POINT('Ctrl Pts',(-31.4229572895715,-1.79211690033832,
312.573538433634));
#15885=CARTESIAN_POINT('Ctrl Pts',(-31.3942932713292,-1.75479901116856,
312.576095548137));
#15886=CARTESIAN_POINT('Ctrl Pts',(-31.3665482396374,-1.71682377199302,
312.57865266264));
#15887=CARTESIAN_POINT('Ctrl Pts',(-31.3397517917505,-1.67824155916049,
312.581209777143));
#15888=CARTESIAN_POINT('Ctrl Pts',(-31.2868086003306,-1.60201259448517,
312.586262006573));
#15889=CARTESIAN_POINT('Ctrl Pts',(-31.2373810767036,-1.52313904501004,
312.591314236002));
#15890=CARTESIAN_POINT('Ctrl Pts',(-31.1917439396311,-1.44197898394981,
312.596366465432));
#15891=CARTESIAN_POINT('Ctrl Pts',(-31.1461697458949,-1.360930859907,312.601411726761));
#15892=CARTESIAN_POINT('Ctrl Pts',(-31.1043757663751,-1.27760287473358,
312.60645698809));
#15893=CARTESIAN_POINT('Ctrl Pts',(-31.0665942694062,-1.19238314110958,
312.611502249418));
#15894=CARTESIAN_POINT('Ctrl Pts',(-31.0288532066941,-1.10725461076966,
312.616542111242));
#15895=CARTESIAN_POINT('Ctrl Pts',(-30.9951162702355,-1.02023876008219,
312.621581973065));
#15896=CARTESIAN_POINT('Ctrl Pts',(-30.9655699495079,-0.931748467658128,
312.626621834889));
#15897=CARTESIAN_POINT('Ctrl Pts',(-30.9360449258947,-0.843321959415589,
312.631658063958));
#15898=CARTESIAN_POINT('Ctrl Pts',(-30.9107046544222,-0.7534235420511,312.636694293028));
#15899=CARTESIAN_POINT('Ctrl Pts',(-30.8896872014526,-0.662485272670189,
312.641730522097));
#15900=CARTESIAN_POINT('Ctrl Pts',(-30.8686773904944,-0.57158006872722,
312.646764919978));
#15901=CARTESIAN_POINT('Ctrl Pts',(-30.8519873754526,-0.479636196309396,
312.651799317859));
#15902=CARTESIAN_POINT('Ctrl Pts',(-30.8397048446733,-0.387099037193126,
312.65683371574));
#15903=CARTESIAN_POINT('Ctrl Pts',(-30.8274233437007,-0.294569636688765,
312.661867691521));
#15904=CARTESIAN_POINT('Ctrl Pts',(-30.8195486505376,-0.201447488814254,
312.666901667302));
#15905=CARTESIAN_POINT('Ctrl Pts',(-30.8161168256602,-0.108185148072898,
312.671935643083));
#15906=CARTESIAN_POINT('Ctrl Pts',(-30.8126843284428,-0.0149045359998572,
312.676970605087));
#15907=CARTESIAN_POINT('Ctrl Pts',(-30.8136964441276,0.0785158795345645,
312.68200556709));
#15908=CARTESIAN_POINT('Ctrl Pts',(-30.8191371252647,0.171622630616089,
312.687040529094));
#15909=CARTESIAN_POINT('Ctrl Pts',(-30.8245837853907,0.264831700547405,
312.692081024225));
#15910=CARTESIAN_POINT('Ctrl Pts',(-30.8344686995876,0.357725973770652,
312.697121519356));
#15911=CARTESIAN_POINT('Ctrl Pts',(-30.8487238666971,0.449856503334521,
312.702162014487));
#15912=CARTESIAN_POINT('Ctrl Pts',(-30.862987792904,0.542043642567136,312.707205606754));
#15913=CARTESIAN_POINT('Ctrl Pts',(-30.8816272292481,0.633465668903467,
312.712249199021));
#15914=CARTESIAN_POINT('Ctrl Pts',(-30.9045233612998,0.7236853900019,312.717292791288));
#15915=CARTESIAN_POINT('Ctrl Pts',(-30.9274565717259,0.814051214407146,
312.722344551231));
#15916=CARTESIAN_POINT('Ctrl Pts',(-30.9546601101224,0.90321042216864,312.727396311175));
#15917=CARTESIAN_POINT('Ctrl Pts',(-30.9859658451968,0.990742669154766,
312.732448071118));
#15918=CARTESIAN_POINT('Ctrl Pts',(-31.0018156910173,1.03505955281071,312.735005737183));
#15919=CARTESIAN_POINT('Ctrl Pts',(-31.0187163010574,1.0789597352799,312.737563403247));
#15920=CARTESIAN_POINT('Ctrl Pts',(-31.0366413382941,1.12239101849619,312.740121069312));
#15921=CARTESIAN_POINT('Ctrl Pts',(-31.0720500112955,1.20818409580586,312.745173419281));
#15922=CARTESIAN_POINT('Ctrl Pts',(-31.1115860558145,1.2924539236927,312.75022576925));
#15923=CARTESIAN_POINT('Ctrl Pts',(-31.1550972300989,1.37477561976373,312.755278119219));
#15924=CARTESIAN_POINT('Ctrl Pts',(-31.198548393021,1.45698377633121,312.7603235009));
#15925=CARTESIAN_POINT('Ctrl Pts',(-31.2459635853537,1.53724875094398,312.765368882581));
#15926=CARTESIAN_POINT('Ctrl Pts',(-31.2971423226019,1.61516507890224,312.770414264261));
#15927=CARTESIAN_POINT('Ctrl Pts',(-31.3482662854831,1.69299801641815,312.775454246091));
#15928=CARTESIAN_POINT('Ctrl Pts',(-31.403145544521,1.7684869342367,312.78049422792));
#15929=CARTESIAN_POINT('Ctrl Pts',(-31.4615340029829,1.84125143913817,312.785534209749));
#15930=CARTESIAN_POINT('Ctrl Pts',(-31.5198803641481,1.91396348180589,312.790570557819));
#15931=CARTESIAN_POINT('Ctrl Pts',(-31.5817306186015,1.98395467032566,312.795606905888));
#15932=CARTESIAN_POINT('Ctrl Pts',(-31.6467963223114,2.05087493173238,312.800643253958));
#15933=CARTESIAN_POINT('Ctrl Pts',(-31.7118383598756,2.11777085244102,312.805677770173));
#15934=CARTESIAN_POINT('Ctrl Pts',(-31.7800932138977,2.18159774684734,312.810712286387));
#15935=CARTESIAN_POINT('Ctrl Pts',(-31.8512339550428,2.24204067560063,312.815746802602));
#15936=CARTESIAN_POINT('Ctrl Pts',(-31.9223687202328,2.30247852703496,312.820780895907));
#15937=CARTESIAN_POINT('Ctrl Pts',(-31.9963885518909,2.35953269049083,312.825814989213));
#15938=CARTESIAN_POINT('Ctrl Pts',(-32.0729325298441,2.41292774251732,312.830849082519));
#15939=CARTESIAN_POINT('Ctrl Pts',(-32.1494914889608,2.46633324500677,312.835884161096));
#15940=CARTESIAN_POINT('Ctrl Pts',(-32.2285752109656,2.51607795992609,312.840919239673));
#15941=CARTESIAN_POINT('Ctrl Pts',(-32.3097937864364,2.56192977309703,312.84595431825));
#15942=CARTESIAN_POINT('Ctrl Pts',(-32.3911015796948,2.60783195402318,312.85099492781));
#15943=CARTESIAN_POINT('Ctrl Pts',(-32.4745485200974,2.64983247843533,312.85603553737));
#15944=CARTESIAN_POINT('Ctrl Pts',(-32.5597203608117,2.68774535498985,312.86107614693));
#15945=CARTESIAN_POINT('Ctrl Pts',(-32.6449445165234,2.72568151872499,312.866119852578));
#15946=CARTESIAN_POINT('Ctrl Pts',(-32.7318952680904,2.75952487516603,312.871163558226));
#15947=CARTESIAN_POINT('Ctrl Pts',(-32.8201407292169,2.78913851459979,312.876207263873));
#15948=CARTESIAN_POINT('Ctrl Pts',(-32.908529045529,2.8188000937452,312.881259134468));
#15949=CARTESIAN_POINT('Ctrl Pts',(-32.9982158287868,2.84421816524307,312.886311005062));
#15950=CARTESIAN_POINT('Ctrl Pts',(-33.0887566456159,2.86530640183156,312.891362875657));
#15951=CARTESIAN_POINT('Ctrl Pts',(-33.1345747571572,2.87597808792916,312.893919370932));
#15952=CARTESIAN_POINT('Ctrl Pts',(-33.1806114499131,2.88554178628865,312.896475866207));
#15953=CARTESIAN_POINT('Ctrl Pts',(-33.2268086614984,2.89399137348184,312.899032361481));
#15954=CARTESIAN_POINT('Ctrl Pts',(-33.318106787295,2.91069003229739,312.90408468432));
#15955=CARTESIAN_POINT('Ctrl Pts',(-33.4103597300015,2.92309408354272,312.909137007159));
#15956=CARTESIAN_POINT('Ctrl Pts',(-33.5031278634048,2.93110140119747,312.914189329998));
#15957=CARTESIAN_POINT('Ctrl Pts',(-33.595768070785,2.9390976768676,312.919234685751));
#15958=CARTESIAN_POINT('Ctrl Pts',(-33.6889216183641,2.94270922910701,312.924280041504));
#15959=CARTESIAN_POINT('Ctrl Pts',(-33.7821390761671,2.9418850033962,312.929325397257));
#15960=CARTESIAN_POINT('Ctrl Pts',(-33.8752567894102,2.94106165962354,312.934365354378));
#15961=CARTESIAN_POINT('Ctrl Pts',(-33.9684378351084,2.93581197594322,312.939405311499));
#15962=CARTESIAN_POINT('Ctrl Pts',(-34.0612291570517,2.92613681996839,312.944445268619));
#15963=CARTESIAN_POINT('Ctrl Pts',(-34.1539536122272,2.9164686360508,312.949481593874));
#15964=CARTESIAN_POINT('Ctrl Pts',(-34.2462884612768,2.90238136447852,312.954517919128));
#15965=CARTESIAN_POINT('Ctrl Pts',(-34.3377832022272,2.88392789296007,312.959554244383));
#15966=CARTESIAN_POINT('Ctrl Pts',(-34.429244685366,2.86548112917226,312.964588738962));
#15967=CARTESIAN_POINT('Ctrl Pts',(-34.5198662320261,2.84267140610266,312.969623233542));
#15968=CARTESIAN_POINT('Ctrl Pts',(-34.609206032639,2.81560299175241,312.974657728121));
#15969=CARTESIAN_POINT('Ctrl Pts',(-34.6985383497843,2.78853684476344,312.979691800991));
#15970=CARTESIAN_POINT('Ctrl Pts',(-34.7865887092408,2.75721284473957,312.98472587386));
#15971=CARTESIAN_POINT('Ctrl Pts',(-34.8729301119596,2.72178523501266,312.98975994673));
#15972=CARTESIAN_POINT('Ctrl Pts',(-34.9592884343651,2.68635068279884,312.994795006089));
#15973=CARTESIAN_POINT('Ctrl Pts',(-35.0439367241078,2.64681109279851,312.999830065449));
#15974=CARTESIAN_POINT('Ctrl Pts',(-35.1264686903429,2.60336853344491,313.004865124808));
#15975=CARTESIAN_POINT('Ctrl Pts',(-35.2090913493738,2.55987823589556,313.009905717098));
#15976=CARTESIAN_POINT('Ctrl Pts',(-35.2895926490284,2.5124766150874,313.014946309388));
#15977=CARTESIAN_POINT('Ctrl Pts',(-35.3675918910899,2.46141117779781,313.019986901678));
#15978=CARTESIAN_POINT('Ctrl Pts',(-35.4456390594115,2.41031436359532,313.025030591135));
#15979=CARTESIAN_POINT('Ctrl Pts',(-35.5211807501152,2.35554951173853,313.030074280593));
#15980=CARTESIAN_POINT('Ctrl Pts',(-35.5938679726108,2.29740553895508,313.03511797005));
#15981=CARTESIAN_POINT('Ctrl Pts',(-35.6666728906397,2.23916741914481,313.040169826276));
#15982=CARTESIAN_POINT('Ctrl Pts',(-35.7366137803689,2.17753954857637,313.045221682502));
#15983=CARTESIAN_POINT('Ctrl Pts',(-35.8033773782909,2.11284878588248,313.050273538729));
#15984=CARTESIAN_POINT('Ctrl Pts',(-35.8371659136847,2.08010929620596,313.052830243703));
#15985=CARTESIAN_POINT('Ctrl Pts',(-35.8701412748032,2.04658585996007,313.055386948677));
#15986=CARTESIAN_POINT('Ctrl Pts',(-35.9022668598925,2.01232398241272,313.057943653651));
#15987=CARTESIAN_POINT('Ctrl Pts',(-35.96503030191,1.94538688667172,313.062938663203));
#15988=CARTESIAN_POINT('Ctrl Pts',(-36.0247853386703,1.87537575228471,313.067933672756));
#15989=CARTESIAN_POINT('Ctrl Pts',(-36.0812105112672,1.80259556836398,313.072928682308));
#15990=CARTESIAN_POINT('Ctrl Pts',(-36.1375118641317,1.72997509370923,313.077912730782));
#15991=CARTESIAN_POINT('Ctrl Pts',(-36.1904976205588,1.65459802241339,313.082896779256));
#15992=CARTESIAN_POINT('Ctrl Pts',(-36.2398843068163,1.57680492335112,313.08788082773));
#15993=CARTESIAN_POINT('Ctrl Pts',(-36.289223520604,1.49908660214551,313.092860085336));
#15994=CARTESIAN_POINT('Ctrl Pts',(-36.3349702892972,1.41895724594861,313.097839342942));
#15995=CARTESIAN_POINT('Ctrl Pts',(-36.3768824674861,1.33678903048679,313.102818600548));
#15996=CARTESIAN_POINT('Ctrl Pts',(-36.4187667597575,1.25467548496026,313.107794545247));
#15997=CARTESIAN_POINT('Ctrl Pts',(-36.4568213220447,1.17052617915665,313.112770489945));
#15998=CARTESIAN_POINT('Ctrl Pts',(-36.4908489574481,1.08473957869907,313.117746434644));
#15999=CARTESIAN_POINT('Ctrl Pts',(-36.5250852286384,0.998426989448164,
313.122752888666));
#16000=CARTESIAN_POINT('Ctrl Pts',(-36.5552447983262,0.91045736888119,313.127759342688));
#16001=CARTESIAN_POINT('Ctrl Pts',(-36.5811755664054,0.821258022888564,
313.13276579671));
#16002=CARTESIAN_POINT('Ctrl Pts',(-36.6069440501183,0.73261691949377,313.137740918486));
#16003=CARTESIAN_POINT('Ctrl Pts',(-36.6285364213618,0.642761892145859,
313.142716040262));
#16004=CARTESIAN_POINT('Ctrl Pts',(-36.6458536373614,0.552126894200304,
313.147691162037));
#16005=CARTESIAN_POINT('Ctrl Pts',(-36.6633344435117,0.460635696679663,
313.152713282183));
#16006=CARTESIAN_POINT('Ctrl Pts',(-36.6764587920037,0.368350176472159,
313.157735402328));
#16007=CARTESIAN_POINT('Ctrl Pts',(-36.6851780352602,0.275724828049647,
313.162757522474));
#16008=CARTESIAN_POINT('Ctrl Pts',(-36.6938972785166,0.183099479627143,
313.167779642619));
#16009=CARTESIAN_POINT('Ctrl Pts',(-36.6982114179565,0.0901347795703585,
313.172801762765));
#16010=CARTESIAN_POINT('Ctrl Pts',(-36.6981257736756,-0.00271372561674938,
313.17782388291));
#16011=CARTESIAN_POINT('',(-35.0450520381518,2.64462403965778,313.999935411543));
#16012=CARTESIAN_POINT('Ctrl Pts',(-36.6981257736749,-0.00271372645954639,
313.177823882956));
#16013=CARTESIAN_POINT('Ctrl Pts',(-36.698013371732,-0.124570656500899,
313.184415051462));
#16014=CARTESIAN_POINT('Ctrl Pts',(-36.6903263421818,-0.246089772706434,
313.191006219968));
#16015=CARTESIAN_POINT('Ctrl Pts',(-36.67521211245,-0.366478176336686,313.197597388474));
#16016=CARTESIAN_POINT('Ctrl Pts',(-36.6604922568569,-0.483725296961528,
313.204016574256));
#16017=CARTESIAN_POINT('Ctrl Pts',(-36.6387280713999,-0.599900445757358,
313.210435760038));
#16018=CARTESIAN_POINT('Ctrl Pts',(-36.610097867168,-0.714292960573622,
313.21685494582));
#16019=CARTESIAN_POINT('Ctrl Pts',(-36.5875606888686,-0.804340676673007,
313.221908012621));
#16020=CARTESIAN_POINT('Ctrl Pts',(-36.5607171932186,-0.893482126933944,
313.226961079422));
#16021=CARTESIAN_POINT('Ctrl Pts',(-36.5296561804346,-0.981274694152054,
313.232014146222));
#16022=CARTESIAN_POINT('Ctrl Pts',(-36.4986380120204,-1.06894616366983,
313.237060243017));
#16023=CARTESIAN_POINT('Ctrl Pts',(-36.4634140334802,-1.15527203236899,
313.242106339811));
#16024=CARTESIAN_POINT('Ctrl Pts',(-36.4241236001709,-1.23982187279091,
313.247152436605));
#16025=CARTESIAN_POINT('Ctrl Pts',(-36.384875232422,-1.32428119152297,313.252193130891));
#16026=CARTESIAN_POINT('Ctrl Pts',(-36.3415692497026,-1.40696786088303,
313.257233825177));
#16027=CARTESIAN_POINT('Ctrl Pts',(-36.2943937834563,-1.48746961791609,
313.262274519463));
#16028=CARTESIAN_POINT('Ctrl Pts',(-36.2472523894463,-1.5679132329718,313.267311573134));
#16029=CARTESIAN_POINT('Ctrl Pts',(-36.1962472907678,-1.64617469026335,
313.272348626805));
#16030=CARTESIAN_POINT('Ctrl Pts',(-36.1416129292153,-1.7218655586366,313.277385680475));
#16031=CARTESIAN_POINT('Ctrl Pts',(-36.0869984857682,-1.79752883231216,
313.282420897782));
#16032=CARTESIAN_POINT('Ctrl Pts',(-36.0287576676608,-1.87062301912678,
313.287456115089));
#16033=CARTESIAN_POINT('Ctrl Pts',(-35.9671681084419,-1.94078884180407,
313.292491332396));
#16034=CARTESIAN_POINT('Ctrl Pts',(-35.9055837875718,-2.0109486966996,313.297526121445));
#16035=CARTESIAN_POINT('Ctrl Pts',(-35.8406515849871,-2.07818034901596,
313.302560910493));
#16036=CARTESIAN_POINT('Ctrl Pts',(-35.7726885189259,-2.14215866411762,
313.307595699542));
#16037=CARTESIAN_POINT('Ctrl Pts',(-35.7047122366137,-2.20614942058663,
313.312631467668));
#16038=CARTESIAN_POINT('Ctrl Pts',(-35.6337042438977,-2.26688527927062,
313.317667235793));
#16039=CARTESIAN_POINT('Ctrl Pts',(-35.5600165494819,-2.32407972849336,
313.322703003918));
#16040=CARTESIAN_POINT('Ctrl Pts',(-35.4862481190206,-2.38133684290998,
313.327744289491));
#16041=CARTESIAN_POINT('Ctrl Pts',(-35.4097944775704,-2.43504452987422,
313.332785575064));
#16042=CARTESIAN_POINT('Ctrl Pts',(-35.3310384321946,-2.4849583618845,313.337826860637));
#16043=CARTESIAN_POINT('Ctrl Pts',(-35.252234123565,-2.53490278207288,313.342871235609));
#16044=CARTESIAN_POINT('Ctrl Pts',(-35.1711249877506,-2.58104849926232,
313.347915610581));
#16045=CARTESIAN_POINT('Ctrl Pts',(-35.0881184382244,-2.62319707147263,
313.352959985553));
#16046=CARTESIAN_POINT('Ctrl Pts',(-35.0049778100673,-2.66541372533304,
313.358012508592));
#16047=CARTESIAN_POINT('Ctrl Pts',(-34.9199340541806,-2.7036201627846,313.36306503163));
#16048=CARTESIAN_POINT('Ctrl Pts',(-34.8334143707933,-2.73766615480207,
313.368117554669));
#16049=CARTESIAN_POINT('Ctrl Pts',(-34.7897555456756,-2.75484615307824,
313.370667115776));
#16050=CARTESIAN_POINT('Ctrl Pts',(-34.7457211432041,-2.77096755745217,
313.373216676883));
#16051=CARTESIAN_POINT('Ctrl Pts',(-34.7013672446505,-2.78601595968905,
313.375766237989));
#16052=CARTESIAN_POINT('Ctrl Pts',(-34.6134720100465,-2.81583707774537,
313.380818652297));
#16053=CARTESIAN_POINT('Ctrl Pts',(-34.5240066289806,-2.84154809311651,
313.385871066604));
#16054=CARTESIAN_POINT('Ctrl Pts',(-34.4333912087129,-2.86298397232829,
313.390923480911));
#16055=CARTESIAN_POINT('Ctrl Pts',(-34.3429006011634,-2.88439032598752,
313.395968936076));
#16056=CARTESIAN_POINT('Ctrl Pts',(-34.2512635306771,-2.90153314339791,
313.401014391241));
#16057=CARTESIAN_POINT('Ctrl Pts',(-34.1589172359201,-2.91429649249943,
313.406059846406));
#16058=CARTESIAN_POINT('Ctrl Pts',(-34.0666696108495,-2.92704620428439,
313.41109991063));
#16059=CARTESIAN_POINT('Ctrl Pts',(-33.9737147054072,-2.93542568821401,
313.416139974853));
#16060=CARTESIAN_POINT('Ctrl Pts',(-33.8805009020536,-2.93936985402837,
313.421180039077));
#16061=CARTESIAN_POINT('Ctrl Pts',(-33.7873540677987,-2.94331118617195,
313.426216482286));
#16062=CARTESIAN_POINT('Ctrl Pts',(-33.6939491478886,-2.94282351513798,
313.431252925495));
#16063=CARTESIAN_POINT('Ctrl Pts',(-33.600739569472,-2.9378935887102,313.436289368704));
#16064=CARTESIAN_POINT('Ctrl Pts',(-33.5075637480035,-2.93296544771341,
313.441323987905));
#16065=CARTESIAN_POINT('Ctrl Pts',(-33.4145835706385,-2.92359827085021,
313.446358607107));
#16066=CARTESIAN_POINT('Ctrl Pts',(-33.3222513426158,-2.90983090436748,
313.451393226308));
#16067=CARTESIAN_POINT('Ctrl Pts',(-33.2299267299149,-2.89606467338131,
313.456427430267));
#16068=CARTESIAN_POINT('Ctrl Pts',(-33.1382503996357,-2.87789904003722,
313.461461634227));
#16069=CARTESIAN_POINT('Ctrl Pts',(-33.0476672780537,-2.85542444946311,
313.466495838186));
#16070=CARTESIAN_POINT('Ctrl Pts',(-32.9570662931595,-2.83294542682022,
313.471531034908));
#16071=CARTESIAN_POINT('Ctrl Pts',(-32.8675593761473,-2.80615586666568,
313.47656623163));
#16072=CARTESIAN_POINT('Ctrl Pts',(-32.7795779268821,-2.77519654411396,
313.481601428352));
#16073=CARTESIAN_POINT('Ctrl Pts',(-32.6914996494938,-2.74420314923082,
313.486642166568));
#16074=CARTESIAN_POINT('Ctrl Pts',(-32.6049506107236,-2.70903097937245,
313.491682904784));
#16075=CARTESIAN_POINT('Ctrl Pts',(-32.5203435052314,-2.66986948962524,
313.496723643));
#16076=CARTESIAN_POINT('Ctrl Pts',(-32.4356843295594,-2.63068389852384,
313.501767483462));
#16077=CARTESIAN_POINT('Ctrl Pts',(-32.3529698599341,-2.58750430519844,
313.506811323925));
#16078=CARTESIAN_POINT('Ctrl Pts',(-32.2725874490644,-2.54056574917254,
313.511855164388));
#16079=CARTESIAN_POINT('Ctrl Pts',(-32.1920747856778,-2.49355113340923,
313.516907177944));
#16080=CARTESIAN_POINT('Ctrl Pts',(-32.1139020971782,-2.4427656365906,313.5219591915));
#16081=CARTESIAN_POINT('Ctrl Pts',(-32.0384269135352,-2.38848703705688,
313.527011205056));
#16082=CARTESIAN_POINT('Ctrl Pts',(-32.0002495750241,-2.3610314898388,313.529566646757));
#16083=CARTESIAN_POINT('Ctrl Pts',(-31.9627618847262,-2.33268283049408,
313.532122088458));
#16084=CARTESIAN_POINT('Ctrl Pts',(-31.9260066147779,-2.30348068868517,
313.534677530159));
#16085=CARTESIAN_POINT('Ctrl Pts',(-31.8533945198067,-2.24579022151206,
313.539725948406));
#16086=CARTESIAN_POINT('Ctrl Pts',(-31.7833813566834,-2.18455843129818,
313.544774366654));
#16087=CARTESIAN_POINT('Ctrl Pts',(-31.7163331569566,-2.12004834257189,
313.549822784901));
#16088=CARTESIAN_POINT('Ctrl Pts',(-31.6493776542288,-2.05562744179774,
313.554864223495));
#16089=CARTESIAN_POINT('Ctrl Pts',(-31.5853792874978,-1.98793755438931,
313.559905662089));
#16090=CARTESIAN_POINT('Ctrl Pts',(-31.5246721392417,-1.91728273649867,
313.564947100682));
#16091=CARTESIAN_POINT('Ctrl Pts',(-31.4640300858115,-1.84670368008263,
313.569983133462));
#16092=CARTESIAN_POINT('Ctrl Pts',(-31.4066725249717,-1.77316634781203,
313.575019166241));
#16093=CARTESIAN_POINT('Ctrl Pts',(-31.3528968716914,-1.69701173507727,
313.580055199021));
#16094=CARTESIAN_POINT('Ctrl Pts',(-31.2991599408614,-1.62091195930001,
313.585087605484));
#16095=CARTESIAN_POINT('Ctrl Pts',(-31.2490000472261,-1.54219901129288,
313.590120011947));
#16096=CARTESIAN_POINT('Ctrl Pts',(-31.2026737868128,-1.46124623492275,
313.59515241841));
#16097=CARTESIAN_POINT('Ctrl Pts',(-31.1563643343673,-1.38032282961867,
313.600182999029));
#16098=CARTESIAN_POINT('Ctrl Pts',(-31.1138859729088,-1.29716159613364,
313.605213579648));
#16099=CARTESIAN_POINT('Ctrl Pts',(-31.0754509106536,-1.21216317737825,
313.610244160267));
#16100=CARTESIAN_POINT('Ctrl Pts',(-31.0370189971839,-1.1271717221027,313.615274328757));
#16101=CARTESIAN_POINT('Ctrl Pts',(-31.0026299075449,-1.04034378635827,
313.620304497246));
#16102=CARTESIAN_POINT('Ctrl Pts',(-30.9724484854758,-0.95210177352955,
313.625334665736));
#16103=CARTESIAN_POINT('Ctrl Pts',(-30.9422610583467,-0.863842203589976,
313.630365835055));
#16104=CARTESIAN_POINT('Ctrl Pts',(-30.9162831050408,-0.774168418976915,
313.635397004374));
#16105=CARTESIAN_POINT('Ctrl Pts',(-30.894629836595,-0.683518719038402,
313.640428173694));
#16106=CARTESIAN_POINT('Ctrl Pts',(-30.87295256024,-0.592768511882588,313.645464921287));
#16107=CARTESIAN_POINT('Ctrl Pts',(-30.8556096435039,-0.501040663057724,
313.65050166888));
#16108=CARTESIAN_POINT('Ctrl Pts',(-30.8426652447765,-0.408784116222606,
313.655538416473));
#16109=CARTESIAN_POINT('Ctrl Pts',(-30.8297128350154,-0.316470473626301,
313.660578281209));
#16110=CARTESIAN_POINT('Ctrl Pts',(-30.8211644029398,-0.223627924458978,
313.665618145946));
#16111=CARTESIAN_POINT('Ctrl Pts',(-30.817032060154,-0.130708783571081,
313.670658010683));
#16112=CARTESIAN_POINT('Ctrl Pts',(-30.8128929650379,-0.0376378109597996,
313.675706110659));
#16113=CARTESIAN_POINT('Ctrl Pts',(-30.8131843633999,0.0555095587920874,
313.680754210635));
#16114=CARTESIAN_POINT('Ctrl Pts',(-30.8178662867567,0.148282947718572,
313.685802310612));
#16115=CARTESIAN_POINT('Ctrl Pts',(-30.820273519263,0.195982813891284,313.688397814517));
#16116=CARTESIAN_POINT('Ctrl Pts',(-30.8238405673749,0.243583925396814,
313.690993318422));
#16117=CARTESIAN_POINT('Ctrl Pts',(-30.8285567317385,0.291026075299615,
313.693588822328));
#16118=CARTESIAN_POINT('Ctrl Pts',(-30.8377518180949,0.383523840785478,
313.698649265669));
#16119=CARTESIAN_POINT('Ctrl Pts',(-30.8513511994363,0.475748885997435,
313.70370970901));
#16120=CARTESIAN_POINT('Ctrl Pts',(-30.8693308450819,0.567249340346028,
313.708770152352));
#16121=CARTESIAN_POINT('Ctrl Pts',(-30.8872856905938,0.658623584003588,
313.713823615596));
#16122=CARTESIAN_POINT('Ctrl Pts',(-30.9096087087805,0.749274792323898,
313.71887707884));
#16123=CARTESIAN_POINT('Ctrl Pts',(-30.9362240836932,0.838755864454321,
313.723930542084));
#16124=CARTESIAN_POINT('Ctrl Pts',(-30.9628108991636,0.92814091954475,313.728978582745));
#16125=CARTESIAN_POINT('Ctrl Pts',(-30.9936807902049,1.01635791227163,313.734026623405));
#16126=CARTESIAN_POINT('Ctrl Pts',(-31.0287070506272,1.10297066234205,313.739074664066));
#16127=CARTESIAN_POINT('Ctrl Pts',(-31.0637076319269,1.18951991321485,313.744119003811));
#16128=CARTESIAN_POINT('Ctrl Pts',(-31.1028583595386,1.27446685025617,313.749163343555));
#16129=CARTESIAN_POINT('Ctrl Pts',(-31.1459832547663,1.35739216785919,313.7542076833));
#16130=CARTESIAN_POINT('Ctrl Pts',(-31.1890921057858,1.4402866338845,313.759250146345));
#16131=CARTESIAN_POINT('Ctrl Pts',(-31.2361719827669,1.52116058245747,313.764292609391));
#16132=CARTESIAN_POINT('Ctrl Pts',(-31.2869999383912,1.59961727575772,313.769335072437));
#16133=CARTESIAN_POINT('Ctrl Pts',(-31.3378230805654,1.67806653914332,313.774377057957));
#16134=CARTESIAN_POINT('Ctrl Pts',(-31.3923933547688,1.75409863099902,313.779419043477));
#16135=CARTESIAN_POINT('Ctrl Pts',(-31.4504438762798,1.82734485429543,313.784461028998));
#16136=CARTESIAN_POINT('Ctrl Pts',(-31.5085049997242,1.9006044547598,313.78950393535));
#16137=CARTESIAN_POINT('Ctrl Pts',(-31.570047357575,1.97107682948833,313.794546841703));
#16138=CARTESIAN_POINT('Ctrl Pts',(-31.6347638098422,2.0384263803931,313.799589748055));
#16139=CARTESIAN_POINT('Ctrl Pts',(-31.699549382117,2.10584786357019,313.804638040453));
#16140=CARTESIAN_POINT('Ctrl Pts',(-31.7675155087973,2.17013954534008,313.80968633285));
#16141=CARTESIAN_POINT('Ctrl Pts',(-31.8383184347808,2.23100296061964,313.814734625248));
#16142=CARTESIAN_POINT('Ctrl Pts',(-31.9091637838538,2.2919028435179,313.819785942438));
#16143=CARTESIAN_POINT('Ctrl Pts',(-31.9828489677308,2.34937009781821,313.824837259628));
#16144=CARTESIAN_POINT('Ctrl Pts',(-32.0589991408942,2.40314813195443,313.829888576818));
#16145=CARTESIAN_POINT('Ctrl Pts',(-32.1352696270824,2.45701113238409,313.834947874808));
#16146=CARTESIAN_POINT('Ctrl Pts',(-32.2140125048864,2.50717303817611,313.840007172797));
#16147=CARTESIAN_POINT('Ctrl Pts',(-32.2948262826152,2.55342204493357,313.845066470786));
#16148=CARTESIAN_POINT('Ctrl Pts',(-32.3344062686011,2.57607331914408,313.847544352023));
#16149=CARTESIAN_POINT('Ctrl Pts',(-32.3744826658589,2.59778671489475,313.85002223326));
#16150=CARTESIAN_POINT('Ctrl Pts',(-32.4150065832655,2.61854157119393,313.852500114497));
#16151=CARTESIAN_POINT('Ctrl Pts',(-32.4967291453233,2.66039685420849,313.857497133939));
#16152=CARTESIAN_POINT('Ctrl Pts',(-32.5805737516244,2.69850485920996,313.862494153382));
#16153=CARTESIAN_POINT('Ctrl Pts',(-32.6661578794082,2.73264180987857,313.867491172824));
#16154=CARTESIAN_POINT('Ctrl Pts',(-32.7516251033333,2.76673213109187,313.872481366575));
#16155=CARTESIAN_POINT('Ctrl Pts',(-32.8388267110154,2.79686200405708,313.877471560325));
#16156=CARTESIAN_POINT('Ctrl Pts',(-32.9273556718184,2.82285352856265,313.882461754076));
#16157=CARTESIAN_POINT('Ctrl Pts',(-33.0157868439752,2.84881634296056,313.887446435684));
#16158=CARTESIAN_POINT('Ctrl Pts',(-33.1055420212523,2.8706497665468,313.892431117291));
#16159=CARTESIAN_POINT('Ctrl Pts',(-33.1961955297968,2.88822449272751,313.897415798899));
#16160=CARTESIAN_POINT('Ctrl Pts',(-33.2867944662325,2.90578863917572,313.9023974798));
#16161=CARTESIAN_POINT('Ctrl Pts',(-33.3782902151584,2.91909909095568,313.907379160701));
#16162=CARTESIAN_POINT('Ctrl Pts',(-33.470244304611,2.92807702597382,313.912360841602));
#16163=CARTESIAN_POINT('Ctrl Pts',(-33.5621701181447,2.93705220027338,313.917340990635));
#16164=CARTESIAN_POINT('Ctrl Pts',(-33.654553539928,2.94169745945905,313.922321139667));
#16165=CARTESIAN_POINT('Ctrl Pts',(-33.7469496049711,2.94198568571584,313.927301288699));
#16166=CARTESIAN_POINT('Ctrl Pts',(-33.8393444666851,2.94227390821889,313.932281372872));
#16167=CARTESIAN_POINT('Ctrl Pts',(-33.9317515164511,2.93820521068346,313.937261457044));
#16168=CARTESIAN_POINT('Ctrl Pts',(-34.0237257062877,2.92980459176221,313.942241541217));
#16169=CARTESIAN_POINT('Ctrl Pts',(-34.1157841649718,2.92139627600259,313.947226188257));
#16170=CARTESIAN_POINT('Ctrl Pts',(-34.2074085176988,2.90864815316715,313.952210835296));
#16171=CARTESIAN_POINT('Ctrl Pts',(-34.2981592111505,2.89163709850599,313.957195482335));
#16172=CARTESIAN_POINT('Ctrl Pts',(-34.3889512416492,2.87461829528955,313.962182399887));
#16173=CARTESIAN_POINT('Ctrl Pts',(-34.4788683776911,2.85333279921205,313.967169317439));
#16174=CARTESIAN_POINT('Ctrl Pts',(-34.5674838877613,2.82790806810761,313.972156234991));
#16175=CARTESIAN_POINT('Ctrl Pts',(-34.6562458761417,2.80244131082011,313.977151395741));
#16176=CARTESIAN_POINT('Ctrl Pts',(-34.743701509796,2.77282179832228,313.982146556492));
#16177=CARTESIAN_POINT('Ctrl Pts',(-34.8294418839185,2.73922602466058,313.987141717242));
#16178=CARTESIAN_POINT('Ctrl Pts',(-34.9026418061714,2.71054399422586,313.991406282009));
#16179=CARTESIAN_POINT('Ctrl Pts',(-34.9745917256034,2.67896467102844,313.995670846776));
#16180=CARTESIAN_POINT('Ctrl Pts',(-35.0450520381518,2.64462403965778,313.999935411543));
#16181=CARTESIAN_POINT('',(-32.4672051712042,2.64462557919705,314.));
#16182=CARTESIAN_POINT('Origin',(-33.7561270252576,0.,314.));
#16183=CARTESIAN_POINT('',(-36.6981257223057,-0.00276885671560002,313.32217611709));
#16184=CARTESIAN_POINT('Ctrl Pts',(-32.4672051712041,2.64462557919703,314.));
#16185=CARTESIAN_POINT('Ctrl Pts',(-31.5870128673401,2.21564269967557,313.947029569277));
#16186=CARTESIAN_POINT('Ctrl Pts',(-30.3047647042133,0.41477504708739,313.841088707831));
#16187=CARTESIAN_POINT('Ctrl Pts',(-31.5376353324677,-2.68170030602472,
313.682177415661));
#16188=CARTESIAN_POINT('Ctrl Pts',(-34.8089410995756,-3.31499725615595,
313.523266123492));
#16189=CARTESIAN_POINT('Ctrl Pts',(-36.5488387827353,-1.49996772299205,
313.403265827269));
#16190=CARTESIAN_POINT('Ctrl Pts',(-36.6995965658053,-0.262825748460331,
313.33623596177));
#16191=CARTESIAN_POINT('Ctrl Pts',(-36.6972963689876,-0.00277565787605923,
313.322176526993));
#16192=CARTESIAN_POINT('',(-36.6981268796127,0.000925729196293329,312.322176117046));
#16193=CARTESIAN_POINT('Ctrl Pts',(-36.6981257223057,-0.00276885671560002,
313.32217611709));
#16194=CARTESIAN_POINT('Ctrl Pts',(-36.6982125227697,0.0894594086611232,
313.31719121744));
#16195=CARTESIAN_POINT('Ctrl Pts',(-36.693958203422,0.181789992050611,313.312206317791));
#16196=CARTESIAN_POINT('Ctrl Pts',(-36.6853606860934,0.273777574367638,
313.307221418141));
#16197=CARTESIAN_POINT('Ctrl Pts',(-36.6767677068704,0.365716602043123,
313.302239149716));
#16198=CARTESIAN_POINT('Ctrl Pts',(-36.6638361227904,0.457312536473602,
313.297256881291));
#16199=CARTESIAN_POINT('Ctrl Pts',(-36.6466158988542,0.548122314464703,
313.292274612867));
#16200=CARTESIAN_POINT('Ctrl Pts',(-36.629399700581,0.638910863372949,313.287293509173));
#16201=CARTESIAN_POINT('Ctrl Pts',(-36.6078969383671,0.728913174457869,
313.28231240548));
#16202=CARTESIAN_POINT('Ctrl Pts',(-36.5822089723762,0.8176948258185,313.277331301786));
#16203=CARTESIAN_POINT('Ctrl Pts',(-36.5565194576737,0.90648182976984,313.272349897785));
#16204=CARTESIAN_POINT('Ctrl Pts',(-36.5266443659156,0.994047591601018,
313.267368493784));
#16205=CARTESIAN_POINT('Ctrl Pts',(-36.4927350019615,1.07997258383734,313.262387089783));
#16206=CARTESIAN_POINT('Ctrl Pts',(-36.4587912382054,1.16598474381675,313.257400632331));
#16207=CARTESIAN_POINT('Ctrl Pts',(-36.4208051973971,1.25035238688473,313.252414174879));
#16208=CARTESIAN_POINT('Ctrl Pts',(-36.3789763092459,1.33267611724752,313.247427717427));
#16209=CARTESIAN_POINT('Ctrl Pts',(-36.3371257405411,1.41504251726122,313.242438675418));
#16210=CARTESIAN_POINT('Ctrl Pts',(-36.2914285852409,1.49536250107787,313.237449633408));
#16211=CARTESIAN_POINT('Ctrl Pts',(-36.2421290349298,1.57326348966281,313.232460591399));
#16212=CARTESIAN_POINT('Ctrl Pts',(-36.1927449189176,1.65129810526203,313.227462991465));
#16213=CARTESIAN_POINT('Ctrl Pts',(-36.1397463285022,1.72690506679231,313.222465391531));
#16214=CARTESIAN_POINT('Ctrl Pts',(-36.0834192937624,1.79974295302352,313.217467791597));
#16215=CARTESIAN_POINT('Ctrl Pts',(-36.0382449104581,1.85815906895937,313.213459707449));
#16216=CARTESIAN_POINT('Ctrl Pts',(-35.9909305000231,1.91479467579664,313.209451623302));
#16217=CARTESIAN_POINT('Ctrl Pts',(-35.9416403734495,1.96949115379456,313.205443539154));
#16218=CARTESIAN_POINT('Ctrl Pts',(-35.8795065263467,2.03844010639887,313.200391052887));
#16219=CARTESIAN_POINT('Ctrl Pts',(-35.8139951039231,2.10456965393969,313.195338566621));
#16220=CARTESIAN_POINT('Ctrl Pts',(-35.745392031301,2.16753056166023,313.190286080354));
#16221=CARTESIAN_POINT('Ctrl Pts',(-35.6768836489419,2.23040456678762,313.185240567845));
#16222=CARTESIAN_POINT('Ctrl Pts',(-35.6052924204783,2.2901183251654,313.180195055337));
#16223=CARTESIAN_POINT('Ctrl Pts',(-35.5309432084145,2.34635707342348,313.175149542828));
#16224=CARTESIAN_POINT('Ctrl Pts',(-35.456673650143,2.40253557047714,313.170109435814));
#16225=CARTESIAN_POINT('Ctrl Pts',(-35.3796523336779,2.45524619078854,313.165069328799));
#16226=CARTESIAN_POINT('Ctrl Pts',(-35.3002386850107,2.50421308642343,313.160029221784));
#16227=CARTESIAN_POINT('Ctrl Pts',(-35.2208824331836,2.55314459084892,313.154992757547));
#16228=CARTESIAN_POINT('Ctrl Pts',(-35.139137662988,2.59833751633471,313.149956293309));
#16229=CARTESIAN_POINT('Ctrl Pts',(-35.0553935274371,2.63955878061359,313.144919829072));
#16230=CARTESIAN_POINT('Ctrl Pts',(-34.9716799452144,2.68076500566842,313.139885202345));
#16231=CARTESIAN_POINT('Ctrl Pts',(-34.8859688449188,2.718002252192,313.134850575618));
#16232=CARTESIAN_POINT('Ctrl Pts',(-34.7986738552168,2.75108344245354,313.129815948891));
#16233=CARTESIAN_POINT('Ctrl Pts',(-34.7113862993168,2.7841618156116,313.124781750899));
#16234=CARTESIAN_POINT('Ctrl Pts',(-34.6225155376344,2.81308467893449,313.119747552907));
#16235=CARTESIAN_POINT('Ctrl Pts',(-34.5324939711156,2.83771358057489,313.114713354915));
#16236=CARTESIAN_POINT('Ctrl Pts',(-34.4424548932985,2.86234727311215,313.109678177654));
#16237=CARTESIAN_POINT('Ctrl Pts',(-34.351264994605,2.88268522825309,313.104643000393));
#16238=CARTESIAN_POINT('Ctrl Pts',(-34.2593694646226,2.89863951660464,313.099607823132));
#16239=CARTESIAN_POINT('Ctrl Pts',(-34.1673731693013,2.91461129916153,313.094567124695));
#16240=CARTESIAN_POINT('Ctrl Pts',(-34.074670136559,2.92618974390358,313.089526426259));
#16241=CARTESIAN_POINT('Ctrl Pts',(-33.9817130180977,2.93333853481563,313.084485727822));
#16242=CARTESIAN_POINT('Ctrl Pts',(-33.8886989041882,2.94049170891586,313.079441938747));
#16243=CARTESIAN_POINT('Ctrl Pts',(-33.7954308381143,2.94320980922228,313.074398149672));
#16244=CARTESIAN_POINT('Ctrl Pts',(-33.7023616329589,2.94150867457347,313.069354360596));
#16245=CARTESIAN_POINT('Ctrl Pts',(-33.6091419391262,2.9398047892672,313.064302415943));
#16246=CARTESIAN_POINT('Ctrl Pts',(-33.5161221908488,2.93366743266693,313.05925047129));
#16247=CARTESIAN_POINT('Ctrl Pts',(-33.4237500611861,2.92316430495355,313.054198526637));
#16248=CARTESIAN_POINT('Ctrl Pts',(-33.3770254414711,2.91785150497788,313.051643100086));
#16249=CARTESIAN_POINT('Ctrl Pts',(-33.3304663662841,2.91142247559488,313.049087673535));
#16250=CARTESIAN_POINT('Ctrl Pts',(-33.2841295196668,2.90389089924469,313.046532246984));
#16251=CARTESIAN_POINT('Ctrl Pts',(-33.1925050259082,2.88899828309429,313.041479256088));
#16252=CARTESIAN_POINT('Ctrl Pts',(-33.1014221356118,2.86973832244506,313.036426265192));
#16253=CARTESIAN_POINT('Ctrl Pts',(-33.0113293612816,2.84616240572037,313.031373274297));
#16254=CARTESIAN_POINT('Ctrl Pts',(-32.9213605804438,2.82261893621768,313.026327237765));
#16255=CARTESIAN_POINT('Ctrl Pts',(-32.8323796336531,2.79477142573066,313.021281201234));
#16256=CARTESIAN_POINT('Ctrl Pts',(-32.7448271219679,2.76272266172453,313.016235164703));
#16257=CARTESIAN_POINT('Ctrl Pts',(-32.6573680776615,2.73070811163078,313.011194515108));
#16258=CARTESIAN_POINT('Ctrl Pts',(-32.5713348522062,2.69450137472164,313.006153865513));
#16259=CARTESIAN_POINT('Ctrl Pts',(-32.487154032446,2.65425536516644,313.001113215918));
#16260=CARTESIAN_POINT('Ctrl Pts',(-32.403033623576,2.61403823745473,312.996076183657));
#16261=CARTESIAN_POINT('Ctrl Pts',(-32.3207633776623,2.56978778971267,312.991039151396));
#16262=CARTESIAN_POINT('Ctrl Pts',(-32.2407500152919,2.52170508142155,312.986002119135));
#16263=CARTESIAN_POINT('Ctrl Pts',(-32.1607655941159,2.47363976486316,312.980966908792));
#16264=CARTESIAN_POINT('Ctrl Pts',(-32.0830368150351,2.421745170032,312.975931698448));
#16265=CARTESIAN_POINT('Ctrl Pts',(-32.0079449655349,2.36626783903762,312.970896488104));
#16266=CARTESIAN_POINT('Ctrl Pts',(-31.9328592875401,2.31079506750807,312.965861691585));
#16267=CARTESIAN_POINT('Ctrl Pts',(-31.8604104653208,2.25174040930801,312.960826895065));
#16268=CARTESIAN_POINT('Ctrl Pts',(-31.7909490631511,2.1893925132901,312.955792098546));
#16269=CARTESIAN_POINT('Ctrl Pts',(-31.7214739542515,2.12703231424149,312.950756308517));
#16270=CARTESIAN_POINT('Ctrl Pts',(-31.6549877664083,2.06137788365821,312.945720518487));
#16271=CARTESIAN_POINT('Ctrl Pts',(-31.5918055080642,1.9927559735737,312.940684728458));
#16272=CARTESIAN_POINT('Ctrl Pts',(-31.5285537517061,1.92405858207097,312.935643399256));
#16273=CARTESIAN_POINT('Ctrl Pts',(-31.468613480408,1.85238752273233,312.930602070055));
#16274=CARTESIAN_POINT('Ctrl Pts',(-31.4122603478211,1.77810376480194,312.925560740853));
#16275=CARTESIAN_POINT('Ctrl Pts',(-31.3558725424498,1.70377430178639,312.920516309838));
#16276=CARTESIAN_POINT('Ctrl Pts',(-31.3030765207695,1.62682930579491,312.915471878823));
#16277=CARTESIAN_POINT('Ctrl Pts',(-31.2541041736667,1.54765811796957,312.910427447807));
#16278=CARTESIAN_POINT('Ctrl Pts',(-31.2050525418011,1.46835875436285,312.905374850009));
#16279=CARTESIAN_POINT('Ctrl Pts',(-31.1598371580439,1.38682639159117,312.900322252211));
#16280=CARTESIAN_POINT('Ctrl Pts',(-31.1186435280827,1.30347412790968,312.895269654413));
#16281=CARTESIAN_POINT('Ctrl Pts',(-31.0978570130047,1.26141415195149,312.892720087881));
#16282=CARTESIAN_POINT('Ctrl Pts',(-31.0780937735029,1.21889108890137,312.890170521348));
#16283=CARTESIAN_POINT('Ctrl Pts',(-31.0593728666175,1.17595961149077,312.887620954815));
#16284=CARTESIAN_POINT('Ctrl Pts',(-31.0222781243352,1.09089257386798,312.88256908879));
#16285=CARTESIAN_POINT('Ctrl Pts',(-30.9891457010024,1.00391569124036,312.877517222764));
#16286=CARTESIAN_POINT('Ctrl Pts',(-30.9601754184417,0.91543356522659,312.872465356738));
#16287=CARTESIAN_POINT('Ctrl Pts',(-30.9312451269952,0.827073581577323,
312.867420464402));
#16288=CARTESIAN_POINT('Ctrl Pts',(-30.9064656964087,0.73721290211214,312.862375572066));
#16289=CARTESIAN_POINT('Ctrl Pts',(-30.8859894678776,0.646277341175262,
312.857330679729));
#16290=CARTESIAN_POINT('Ctrl Pts',(-30.865535175313,0.555439198540542,312.852291191933));
#16291=CARTESIAN_POINT('Ctrl Pts',(-30.8493750189145,0.463528894372842,
312.847251704136));
#16292=CARTESIAN_POINT('Ctrl Pts',(-30.8376116192949,0.370987634778209,
312.842212216339));
#16293=CARTESIAN_POINT('Ctrl Pts',(-30.8258567132236,0.278513192913623,
312.837176367213));
#16294=CARTESIAN_POINT('Ctrl Pts',(-30.8184923098604,0.185409140651498,
312.832140518087));
#16295=CARTESIAN_POINT('Ctrl Pts',(-30.8155698016233,0.0921260795430611,
312.82710466896));
#16296=CARTESIAN_POINT('Ctrl Pts',(-30.8126483581473,-0.00112299562917563,
312.822070654551));
#16297=CARTESIAN_POINT('Ctrl Pts',(-30.8141656087479,-0.0945505064111075,
312.817036640142));
#16298=CARTESIAN_POINT('Ctrl Pts',(-30.8201209384099,-0.187702578546671,
312.812002625733));
#16299=CARTESIAN_POINT('Ctrl Pts',(-30.8260757651075,-0.280846783415015,
312.806969036478));
#16300=CARTESIAN_POINT('Ctrl Pts',(-30.8364678971054,-0.373715152463849,
312.801935447222));
#16301=CARTESIAN_POINT('Ctrl Pts',(-30.8512446824128,-0.465856817303986,
312.796901857967));
#16302=CARTESIAN_POINT('Ctrl Pts',(-30.8660243553348,-0.558016488064301,
312.79186728507));
#16303=CARTESIAN_POINT('Ctrl Pts',(-30.8851903124993,-0.649448733936276,
312.786832712172));
#16304=CARTESIAN_POINT('Ctrl Pts',(-30.9086386116362,-0.739711926557905,
312.781798139275));
#16305=CARTESIAN_POINT('Ctrl Pts',(-30.9321126738784,-0.830074293116133,
312.776758034794));
#16306=CARTESIAN_POINT('Ctrl Pts',(-30.9598783581177,-0.91926461175442,
312.771717930312));
#16307=CARTESIAN_POINT('Ctrl Pts',(-30.9917816403831,-1.00685579559491,
312.766677825831));
#16308=CARTESIAN_POINT('Ctrl Pts',(-31.0237045179241,-1.09450077870813,
312.761634625674));
#16309=CARTESIAN_POINT('Ctrl Pts',(-31.0597698811519,-1.18054426216621,
312.756591425516));
#16310=CARTESIAN_POINT('Ctrl Pts',(-31.0997761506711,-1.26458057516464,
312.751548225359));
#16311=CARTESIAN_POINT('Ctrl Pts',(-31.1398472244555,-1.34875301461476,
312.746496855959));
#16312=CARTESIAN_POINT('Ctrl Pts',(-31.1838717391617,-1.43091140158479,
312.74144548656));
#16313=CARTESIAN_POINT('Ctrl Pts',(-31.2316030189279,-1.51067618683325,
312.736394117161));
#16314=CARTESIAN_POINT('Ctrl Pts',(-31.2558069406338,-1.5511238896079,312.733832632323));
#16315=CARTESIAN_POINT('Ctrl Pts',(-31.280963330977,-1.59095659018532,312.731271147484));
#16316=CARTESIAN_POINT('Ctrl Pts',(-31.3070360320273,-1.63012800321881,
312.728709662646));
#16317=CARTESIAN_POINT('Ctrl Pts',(-31.358462392419,-1.70739054689708,312.723657334458));
#16318=CARTESIAN_POINT('Ctrl Pts',(-31.4136407908189,-1.7823558205591,312.71860500627));
#16319=CARTESIAN_POINT('Ctrl Pts',(-31.4723392186545,-1.85463669067852,
312.713552678083));
#16320=CARTESIAN_POINT('Ctrl Pts',(-31.530956689728,-1.92681787115682,312.708507318057));
#16321=CARTESIAN_POINT('Ctrl Pts',(-31.5930842654704,-1.99632166322212,
312.703461958031));
#16322=CARTESIAN_POINT('Ctrl Pts',(-31.6584463952587,-2.06278936746514,
312.698416598005));
#16323=CARTESIAN_POINT('Ctrl Pts',(-31.7237385724353,-2.12918593587593,
312.693376637682));
#16324=CARTESIAN_POINT('Ctrl Pts',(-31.7922581131499,-2.19255255992412,
312.68833667736));
#16325=CARTESIAN_POINT('Ctrl Pts',(-31.8636896051547,-2.2525640081903,312.683296717037));
#16326=CARTESIAN_POINT('Ctrl Pts',(-31.9350695999261,-2.31253219229558,
312.678260390182));
#16327=CARTESIAN_POINT('Ctrl Pts',(-32.0093570341332,-2.36914972349256,
312.673224063327));
#16328=CARTESIAN_POINT('Ctrl Pts',(-32.0862008578061,-2.42212935147171,
312.668187736472));
#16329=CARTESIAN_POINT('Ctrl Pts',(-32.1630167340359,-2.4750897112122,312.663153241286));
#16330=CARTESIAN_POINT('Ctrl Pts',(-32.2423867873326,-2.5244145442575,312.6581187461));
#16331=CARTESIAN_POINT('Ctrl Pts',(-32.3239290548795,-2.56985855129127,
312.653084250914));
#16332=CARTESIAN_POINT('Ctrl Pts',(-32.4054644760275,-2.61529874278482,
312.648050178432));
#16333=CARTESIAN_POINT('Ctrl Pts',(-32.489171360666,-2.65685854000789,312.643016105949));
#16334=CARTESIAN_POINT('Ctrl Pts',(-32.5746420944852,-2.69433801857853,
312.637982033466));
#16335=CARTESIAN_POINT('Ctrl Pts',(-32.6601295605093,-2.73182483433104,
312.632946975486));
#16336=CARTESIAN_POINT('Ctrl Pts',(-32.7473811545089,-2.76522956698514,
312.627911917506));
#16337=CARTESIAN_POINT('Ctrl Pts',(-32.835969254871,-2.79440041468597,312.622876859527));
#16338=CARTESIAN_POINT('Ctrl Pts',(-32.9246546767038,-2.82360330901372,
312.617836270113));
#16339=CARTESIAN_POINT('Ctrl Pts',(-33.0146791131183,-2.84856289472312,
312.612795680699));
#16340=CARTESIAN_POINT('Ctrl Pts',(-33.1056000456081,-2.86917734703662,
312.607755091285));
#16341=CARTESIAN_POINT('Ctrl Pts',(-33.1965768286452,-2.88980446231358,
312.602711405558));
#16342=CARTESIAN_POINT('Ctrl Pts',(-33.2884507669756,-2.90608105307196,
312.597667719831));
#16343=CARTESIAN_POINT('Ctrl Pts',(-33.3807715909833,-2.91795687047645,
312.592624034104));
#16344=CARTESIAN_POINT('Ctrl Pts',(-33.473241877852,-2.92985191424364,312.587572182899));
#16345=CARTESIAN_POINT('Ctrl Pts',(-33.5661600524894,-2.9373319255915,312.582520331693));
#16346=CARTESIAN_POINT('Ctrl Pts',(-33.6590733812322,-2.94039871279073,
312.577468480488));
#16347=CARTESIAN_POINT('Ctrl Pts',(-33.7060961077578,-2.94195079038533,
312.574911777151));
#16348=CARTESIAN_POINT('Ctrl Pts',(-33.7531176306962,-2.94237334144602,
312.572355073813));
#16349=CARTESIAN_POINT('Ctrl Pts',(-33.8000797915366,-2.9416716598452,312.569798370476));
#16350=CARTESIAN_POINT('Ctrl Pts',(-33.8928824666442,-2.94028505564163,
312.56474602823));
#16351=CARTESIAN_POINT('Ctrl Pts',(-33.985785988718,-2.93450010495286,312.559693685985));
#16352=CARTESIAN_POINT('Ctrl Pts',(-34.0783392594271,-2.9243021861893,312.554641343739));
#16353=CARTESIAN_POINT('Ctrl Pts',(-34.1707649080661,-2.91411832937615,
312.549595968188));
#16354=CARTESIAN_POINT('Ctrl Pts',(-34.2628408273101,-2.89953364451495,
312.544550592637));
#16355=CARTESIAN_POINT('Ctrl Pts',(-34.3541162411757,-2.88058551298961,
312.539505217086));
#16356=CARTESIAN_POINT('Ctrl Pts',(-34.445293995534,-2.86165765488854,312.5344652398));
#16357=CARTESIAN_POINT('Ctrl Pts',(-34.5356725142954,-2.838375719569,312.529425262514));
#16358=CARTESIAN_POINT('Ctrl Pts',(-34.6248075687399,-2.81082872359299,
312.524385285228));
#16359=CARTESIAN_POINT('Ctrl Pts',(-34.7138783998947,-2.78330157568583,
312.51934893933));
#16360=CARTESIAN_POINT('Ctrl Pts',(-34.8017071243158,-2.75151560602708,
312.514312593432));
#16361=CARTESIAN_POINT('Ctrl Pts',(-34.8878621418458,-2.7156103597315,312.509276247533));
#16362=CARTESIAN_POINT('Ctrl Pts',(-34.9739858476426,-2.67971816265264,
312.504241732019));
#16363=CARTESIAN_POINT('Ctrl Pts',(-35.0584366453236,-2.63970983378514,
312.499207216504));
#16364=CARTESIAN_POINT('Ctrl Pts',(-35.1408014596098,-2.59577362473145,
312.494172700989));
#16365=CARTESIAN_POINT('Ctrl Pts',(-35.2231593791528,-2.55184109356958,
312.489138606912));
#16366=CARTESIAN_POINT('Ctrl Pts',(-35.3034312706049,-2.50398154520596,
312.484104512836));
#16367=CARTESIAN_POINT('Ctrl Pts',(-35.3812283112679,-2.45242936905584,
312.479070418759));
#16368=CARTESIAN_POINT('Ctrl Pts',(-35.4590406010642,-2.40086708807403,
312.474035337941));
#16369=CARTESIAN_POINT('Ctrl Pts',(-35.534376706569,-2.34561098752187,312.469000257123));
#16370=CARTESIAN_POINT('Ctrl Pts',(-35.6068774241292,-2.28693833783874,
312.463965176305));
#16371=CARTESIAN_POINT('Ctrl Pts',(-35.6794578148327,-2.22820121107752,
312.458924562291));
#16372=CARTESIAN_POINT('Ctrl Pts',(-35.7491962520428,-2.1660403205648,312.453883948276));
#16373=CARTESIAN_POINT('Ctrl Pts',(-35.8157674776937,-2.1007725261648,312.448843334262));
#16374=CARTESIAN_POINT('Ctrl Pts',(-35.8823796099752,-2.03546462606553,
312.443799622895));
#16375=CARTESIAN_POINT('Ctrl Pts',(-35.9458203543912,-1.96704634688947,
312.438755911528));
#16376=CARTESIAN_POINT('Ctrl Pts',(-36.005803612625,-1.89586899659519,312.433712200161));
#16377=CARTESIAN_POINT('Ctrl Pts',(-36.0658839966621,-1.82457639485368,
312.42866032194));
#16378=CARTESIAN_POINT('Ctrl Pts',(-36.122495448521,-1.75051615561669,312.42360844372));
#16379=CARTESIAN_POINT('Ctrl Pts',(-36.1753942973603,-1.67406985103148,
312.418556565499));
#16380=CARTESIAN_POINT('Ctrl Pts',(-36.2021636839723,-1.63538430820029,
312.416000069768));
#16381=CARTESIAN_POINT('Ctrl Pts',(-36.2279830463466,-1.59608814747113,
312.413443574037));
#16382=CARTESIAN_POINT('Ctrl Pts',(-36.2528253442714,-1.55623311358982,
312.410887078307));
#16383=CARTESIAN_POINT('Ctrl Pts',(-36.3032815210905,-1.47528518185132,
312.405694684229));
#16384=CARTESIAN_POINT('Ctrl Pts',(-36.3498771649948,-1.39175301603299,
312.400502290151));
#16385=CARTESIAN_POINT('Ctrl Pts',(-36.3923463531807,-1.30602896410628,
312.395309896074));
#16386=CARTESIAN_POINT('Ctrl Pts',(-36.4347463756819,-1.22044452310699,
312.390125958374));
#16387=CARTESIAN_POINT('Ctrl Pts',(-36.4730331292883,-1.13267566198725,
312.384942020674));
#16388=CARTESIAN_POINT('Ctrl Pts',(-36.5069847334643,-1.04314230534479,
312.379758082974));
#16389=CARTESIAN_POINT('Ctrl Pts',(-36.5408749019281,-0.953770960061013,
312.374583525652));
#16390=CARTESIAN_POINT('Ctrl Pts',(-36.5704453987093,-0.86264185998207,
312.369408968331));
#16391=CARTESIAN_POINT('Ctrl Pts',(-36.5955214651476,-0.770196867509516,
312.364234411009));
#16392=CARTESIAN_POINT('Ctrl Pts',(-36.6205707907295,-0.677850457415516,
312.359065371782));
#16393=CARTESIAN_POINT('Ctrl Pts',(-36.6411351109393,-0.58419134043354,
312.353896332555));
#16394=CARTESIAN_POINT('Ctrl Pts',(-36.6570887399773,-0.489678598399612,
312.348727293328));
#16395=CARTESIAN_POINT('Ctrl Pts',(-36.6730258748099,-0.395263571598767,
312.343563598289));
#16396=CARTESIAN_POINT('Ctrl Pts',(-36.6843617411924,-0.299997080946183,
312.33839990325));
#16397=CARTESIAN_POINT('Ctrl Pts',(-36.6910214454844,-0.204349558652154,
312.333236208211));
#16398=CARTESIAN_POINT('Ctrl Pts',(-36.6957762406295,-0.136060584442952,
312.32954951117));
#16399=CARTESIAN_POINT('Ctrl Pts',(-36.6981484348598,-0.0675776627360847,
312.32586281413));
#16400=CARTESIAN_POINT('Ctrl Pts',(-36.698126879613,0.000925728376547487,
312.32217611709));
#16401=CARTESIAN_POINT('',(-36.6981261623761,0.00225326298871394,311.322176117122));
#16402=CARTESIAN_POINT('Ctrl Pts',(-36.6981268796127,0.000925729196304501,
312.322176117046));
#16403=CARTESIAN_POINT('Ctrl Pts',(-36.6980951904088,0.101635130789933,
312.316756165613));
#16404=CARTESIAN_POINT('Ctrl Pts',(-36.6928881286928,0.202195227316754,
312.311336214181));
#16405=CARTESIAN_POINT('Ctrl Pts',(-36.6825766586399,0.30208697965426,312.305916262748));
#16406=CARTESIAN_POINT('Ctrl Pts',(-36.6722226572952,0.402390751348661,
312.300473955868));
#16407=CARTESIAN_POINT('Ctrl Pts',(-36.6567221512165,0.502020334260477,
312.295031648987));
#16408=CARTESIAN_POINT('Ctrl Pts',(-36.6361975885368,0.600464445685857,
312.289589342106));
#16409=CARTESIAN_POINT('Ctrl Pts',(-36.6156282772227,0.699123189676856,
312.284135169647));
#16410=CARTESIAN_POINT('Ctrl Pts',(-36.5900131202047,0.796590984724717,
312.278680997189));
#16411=CARTESIAN_POINT('Ctrl Pts',(-36.5595242514719,0.892372115237896,
312.27322682473));
#16412=CARTESIAN_POINT('Ctrl Pts',(-36.5289401958915,0.988452276323434,
312.267755624237));
#16413=CARTESIAN_POINT('Ctrl Pts',(-36.4934521105363,1.08283493328951,312.262284423745));
#16414=CARTESIAN_POINT('Ctrl Pts',(-36.4532806102076,1.17504320737213,312.256813223253));
#16415=CARTESIAN_POINT('Ctrl Pts',(-36.4414412154882,1.20221894500509,312.255200744214));
#16416=CARTESIAN_POINT('Ctrl Pts',(-36.4291953163461,1.22920598503843,312.253588265176));
#16417=CARTESIAN_POINT('Ctrl Pts',(-36.4165493003502,1.25599256295217,312.251975786138));
#16418=CARTESIAN_POINT('Ctrl Pts',(-36.3769262856362,1.33992136481035,312.246923500842));
#16419=CARTESIAN_POINT('Ctrl Pts',(-36.3332566812781,1.42212398347406,312.241871215547));
#16420=CARTESIAN_POINT('Ctrl Pts',(-36.2857136239563,1.50218362382368,312.236818930251));
#16421=CARTESIAN_POINT('Ctrl Pts',(-36.2382361368719,1.58213284784921,312.231773612946));
#16422=CARTESIAN_POINT('Ctrl Pts',(-36.1868960372673,1.65994458793857,312.22672829564));
#16423=CARTESIAN_POINT('Ctrl Pts',(-36.1319136814722,1.7352238369019,312.221682978335));
#16424=CARTESIAN_POINT('Ctrl Pts',(-36.0769901674998,1.81042252241625,312.216643060501));
#16425=CARTESIAN_POINT('Ctrl Pts',(-36.0184324056657,1.88309374702584,312.211603142667));
#16426=CARTESIAN_POINT('Ctrl Pts',(-35.956505064021,1.95286980787962,312.206563224833));
#16427=CARTESIAN_POINT('Ctrl Pts',(-35.8946223616222,2.0225955718749,312.201526939936));
#16428=CARTESIAN_POINT('Ctrl Pts',(-35.8293752012407,2.08942998886531,312.196490655039));
#16429=CARTESIAN_POINT('Ctrl Pts',(-35.7610690412033,2.15303774065748,312.191454370142));
#16430=CARTESIAN_POINT('Ctrl Pts',(-35.6927877190443,2.21662236303343,312.186419916568));
#16431=CARTESIAN_POINT('Ctrl Pts',(-35.6214499317837,2.27698234864377,312.181385462994));
#16432=CARTESIAN_POINT('Ctrl Pts',(-35.54739783171,2.33381937989027,312.17635100942));
#16433=CARTESIAN_POINT('Ctrl Pts',(-35.4733519433136,2.3906516435029,312.171316978149));
#16434=CARTESIAN_POINT('Ctrl Pts',(-35.3965925473205,2.44396126995869,312.166282946877));
#16435=CARTESIAN_POINT('Ctrl Pts',(-35.3174937834037,2.49349109614537,312.161248915606));
#16436=CARTESIAN_POINT('Ctrl Pts',(-35.23837952742,2.54303062310796,312.156213898383));
#16437=CARTESIAN_POINT('Ctrl Pts',(-35.156925370263,2.58878864411495,312.15117888116));
#16438=CARTESIAN_POINT('Ctrl Pts',(-35.0735322551215,2.63055269103797,312.146143863937));
#16439=CARTESIAN_POINT('Ctrl Pts',(-34.9900475092246,2.67236262749475,312.141103314334));
#16440=CARTESIAN_POINT('Ctrl Pts',(-34.9046199504724,2.71016963065511,312.136062764731));
#16441=CARTESIAN_POINT('Ctrl Pts',(-34.8176725397979,2.74380850653966,312.131022215127));
#16442=CARTESIAN_POINT('Ctrl Pts',(-34.7306717107299,2.77746804933875,312.125978568732));
#16443=CARTESIAN_POINT('Ctrl Pts',(-34.6421495919806,2.80695422652558,312.120934922336));
#16444=CARTESIAN_POINT('Ctrl Pts',(-34.5525443253081,2.83215174102311,312.115891275941));
#16445=CARTESIAN_POINT('Ctrl Pts',(-34.4627939708205,2.8573900550457,312.110839462931));
#16446=CARTESIAN_POINT('Ctrl Pts',(-34.3719573994857,2.8783257435797,312.105787649922));
#16447=CARTESIAN_POINT('Ctrl Pts',(-34.2804827733287,2.89489465256765,312.100735836912));
#16448=CARTESIAN_POINT('Ctrl Pts',(-34.2341803714899,2.90328146226802,312.098178722597));
#16449=CARTESIAN_POINT('Ctrl Pts',(-34.1877145737566,2.91055026154907,312.095621608282));
#16450=CARTESIAN_POINT('Ctrl Pts',(-34.141143718015,2.91669781538954,312.093064493968));
#16451=CARTESIAN_POINT('Ctrl Pts',(-34.0491301834323,2.92884399885327,312.088012211318));
#16452=CARTESIAN_POINT('Ctrl Pts',(-33.9563761616878,2.9366535656255,312.082959928669));
#16453=CARTESIAN_POINT('Ctrl Pts',(-33.8633257974159,2.94004633011926,312.077907646019));
#16454=CARTESIAN_POINT('Ctrl Pts',(-33.7704037643636,2.94343441545235,312.072862331269));
#16455=CARTESIAN_POINT('Ctrl Pts',(-33.6771866410364,2.94241778698686,312.067817016519));
#16456=CARTESIAN_POINT('Ctrl Pts',(-33.5841258298458,2.93696775412617,312.06277170177));
#16457=CARTESIAN_POINT('Ctrl Pts',(-33.4911646101603,2.93152355376327,312.057731786398));
#16458=CARTESIAN_POINT('Ctrl Pts',(-33.3983598112263,2.9216554052996,312.052691871026));
#16459=CARTESIAN_POINT('Ctrl Pts',(-33.3061638809911,2.90738665622614,312.047651955654));
#16460=CARTESIAN_POINT('Ctrl Pts',(-33.2140344058603,2.89312819211002,312.042615673068));
#16461=CARTESIAN_POINT('Ctrl Pts',(-33.12251336487,2.87447549986094,312.037579390482));
#16462=CARTESIAN_POINT('Ctrl Pts',(-33.0320480735983,2.85150375622477,312.032543107897));
#16463=CARTESIAN_POINT('Ctrl Pts',(-32.9416156761503,2.82854036527806,312.027508656539));
#16464=CARTESIAN_POINT('Ctrl Pts',(-32.8522386959621,2.80126115201499,312.022474205181));
#16465=CARTESIAN_POINT('Ctrl Pts',(-32.7643532173439,2.76979217883517,312.017439753824));
#16466=CARTESIAN_POINT('Ctrl Pts',(-32.6764751090773,2.73832584474201,312.012405724671));
#16467=CARTESIAN_POINT('Ctrl Pts',(-32.590088671878,2.70267059926534,312.007371695518));
#16468=CARTESIAN_POINT('Ctrl Pts',(-32.5056127178106,2.66300168360263,312.002337666366));
#16469=CARTESIAN_POINT('Ctrl Pts',(-32.4211202168114,2.62332499769509,311.99730265116));
#16470=CARTESIAN_POINT('Ctrl Pts',(-32.3385393440913,2.57963326938745,311.992267635955));
#16471=CARTESIAN_POINT('Ctrl Pts',(-32.2582658556418,2.53214847837903,311.98723262075));
#16472=CARTESIAN_POINT('Ctrl Pts',(-32.1779041615258,2.48461151039763,311.982192072997));
#16473=CARTESIAN_POINT('Ctrl Pts',(-32.0998552955712,2.43327338668277,311.977151525245));
#16474=CARTESIAN_POINT('Ctrl Pts',(-32.0244871976255,2.3784001991587,311.972110977492));
#16475=CARTESIAN_POINT('Ctrl Pts',(-31.9490727939409,2.32349329785444,311.967067332855));
#16476=CARTESIAN_POINT('Ctrl Pts',(-31.8763427832563,2.26504728694481,311.962023688218));
#16477=CARTESIAN_POINT('Ctrl Pts',(-31.8066313816548,2.20336804360359,311.956980043581));
#16478=CARTESIAN_POINT('Ctrl Pts',(-31.7368071018819,2.14158892793105,311.951928232168));
#16479=CARTESIAN_POINT('Ctrl Pts',(-31.6700115070096,2.07656643765146,311.946876420755));
#16480=CARTESIAN_POINT('Ctrl Pts',(-31.6065412469252,2.00864257188561,311.941824609342));
#16481=CARTESIAN_POINT('Ctrl Pts',(-31.5744137457052,1.97426073577267,311.939267473495));
#16482=CARTESIAN_POINT('Ctrl Pts',(-31.543137612452,1.93913602706984,311.936710337647));
#16483=CARTESIAN_POINT('Ctrl Pts',(-31.51274716265,1.90331573629989,311.934153201799));
#16484=CARTESIAN_POINT('Ctrl Pts',(-31.4527031003815,1.83254364232026,311.929100929619));
#16485=CARTESIAN_POINT('Ctrl Pts',(-31.3959035223174,1.7588004031586,311.924048657439));
#16486=CARTESIAN_POINT('Ctrl Pts',(-31.3426563804786,1.6824159553422,311.918996385259));
#16487=CARTESIAN_POINT('Ctrl Pts',(-31.2894826771468,1.60613685702646,311.913951081178));
#16488=CARTESIAN_POINT('Ctrl Pts',(-31.2398519259153,1.52722414995996,311.908905777096));
#16489=CARTESIAN_POINT('Ctrl Pts',(-31.1940327208393,1.44604176124601,311.903860473014));
#16490=CARTESIAN_POINT('Ctrl Pts',(-31.1482625521689,1.36494625515107,311.898820568494));
#16491=CARTESIAN_POINT('Ctrl Pts',(-31.1062960388672,1.28158628031752,311.893780663973));
#16492=CARTESIAN_POINT('Ctrl Pts',(-31.0683585959412,1.19635482628272,311.888740759452));
#16493=CARTESIAN_POINT('Ctrl Pts',(-31.0304485002042,1.11118481130409,311.883704487944));
#16494=CARTESIAN_POINT('Ctrl Pts',(-30.9965618821709,1.02414640325922,311.878668216436));
#16495=CARTESIAN_POINT('Ctrl Pts',(-30.966877807416,0.93565634758182,311.873631944928));
#16496=CARTESIAN_POINT('Ctrl Pts',(-30.9372045268311,0.847198469989997,
311.868597504785));
#16497=CARTESIAN_POINT('Ctrl Pts',(-30.9117308947555,0.757290414202034,
311.863563064642));
#16498=CARTESIAN_POINT('Ctrl Pts',(-30.890587117435,0.66636704350975,311.858528624498));
#16499=CARTESIAN_POINT('Ctrl Pts',(-30.869445113818,0.575451300173184,311.853494606683));
#16500=CARTESIAN_POINT('Ctrl Pts',(-30.8526323432332,0.483520844028177,
311.848460588868));
#16501=CARTESIAN_POINT('Ctrl Pts',(-30.8402283156891,0.391022653483081,
311.843426571052));
#16502=CARTESIAN_POINT('Ctrl Pts',(-30.82782185874,0.298506346598925,311.838391567294));
#16503=CARTESIAN_POINT('Ctrl Pts',(-30.8198259183807,0.20542252482137,311.833356563535));
#16504=CARTESIAN_POINT('Ctrl Pts',(-30.8162682273124,0.112224097876667,
311.828321559776));
#16505=CARTESIAN_POINT('Ctrl Pts',(-30.8127066270613,0.0189232647127285,
311.823281023567));
#16506=CARTESIAN_POINT('Ctrl Pts',(-30.8135930276215,-0.074491980364185,
311.818240487358));
#16507=CARTESIAN_POINT('Ctrl Pts',(-30.8189030141255,-0.167568220223843,
311.813199951148));
#16508=CARTESIAN_POINT('Ctrl Pts',(-30.8242162629871,-0.260701644404563,
311.808156318127));
#16509=CARTESIAN_POINT('Ctrl Pts',(-30.8339584619861,-0.353495207224369,
311.803112685105));
#16510=CARTESIAN_POINT('Ctrl Pts',(-30.8480534866068,-0.445502293820143,
311.798069052083));
#16511=CARTESIAN_POINT('Ctrl Pts',(-30.8621713342437,-0.537658360590239,
311.793017252285));
#16512=CARTESIAN_POINT('Ctrl Pts',(-30.880655990392,-0.629024973895696,
311.787965452487));
#16513=CARTESIAN_POINT('Ctrl Pts',(-30.9033806193877,-0.719167535276973,
311.782913652689));
#16514=CARTESIAN_POINT('Ctrl Pts',(-30.9148839463684,-0.764798174995941,
311.780356405002));
#16515=CARTESIAN_POINT('Ctrl Pts',(-30.9274729521898,-0.810115424651446,
311.777799157316));
#16516=CARTESIAN_POINT('Ctrl Pts',(-30.9411264644474,-0.855064817799336,
311.77524190963));
#16517=CARTESIAN_POINT('Ctrl Pts',(-30.9681013021196,-0.943869995599242,
311.770189631511));
#16518=CARTESIAN_POINT('Ctrl Pts',(-30.999331001575,-1.03155685611456,311.765137353392));
#16519=CARTESIAN_POINT('Ctrl Pts',(-31.0347049864818,-1.11768783068693,
311.760085075273));
#16520=CARTESIAN_POINT('Ctrl Pts',(-31.0700301841841,-1.20370001486903,
311.755039765171));
#16521=CARTESIAN_POINT('Ctrl Pts',(-31.1094881421484,-1.28816016980654,
311.749994455069));
#16522=CARTESIAN_POINT('Ctrl Pts',(-31.1529183942683,-1.37064540401327,
311.744949144967));
#16523=CARTESIAN_POINT('Ctrl Pts',(-31.196302167356,-1.45304236256733,311.739909234353));
#16524=CARTESIAN_POINT('Ctrl Pts',(-31.2436495789414,-1.53346821042311,
311.73486932374));
#16525=CARTESIAN_POINT('Ctrl Pts',(-31.2947523465011,-1.61152061444348,
311.729829413126));
#16526=CARTESIAN_POINT('Ctrl Pts',(-31.3458182775324,-1.68951675576551,
311.724793135443));
#16527=CARTESIAN_POINT('Ctrl Pts',(-31.4006339413852,-1.76514248320502,
311.719756857759));
#16528=CARTESIAN_POINT('Ctrl Pts',(-31.4589459829763,-1.83802156107686,
311.714720580076));
#16529=CARTESIAN_POINT('Ctrl Pts',(-31.5172368208559,-1.91087413829977,
311.709686133709));
#16530=CARTESIAN_POINT('Ctrl Pts',(-31.5790212334917,-1.98098170354263,
311.704651687342));
#16531=CARTESIAN_POINT('Ctrl Pts',(-31.6440041734869,-2.04799928198917,
311.699617240975));
#16532=CARTESIAN_POINT('Ctrl Pts',(-31.7089816627469,-2.11501123903607,
311.694583216894));
#16533=CARTESIAN_POINT('Ctrl Pts',(-31.7771568365523,-2.17893340579648,
311.689549192814));
#16534=CARTESIAN_POINT('Ctrl Pts',(-31.848197006501,-2.23945686351124,311.684515168734));
#16535=CARTESIAN_POINT('Ctrl Pts',(-31.9192510905571,-2.2999921755035,311.679480158677));
#16536=CARTESIAN_POINT('Ctrl Pts',(-31.9931709468047,-2.35712716860007,
311.67444514862));
#16537=CARTESIAN_POINT('Ctrl Pts',(-32.0695908586993,-2.41059323795842,
311.669410138563));
#16538=CARTESIAN_POINT('Ctrl Pts',(-32.1460947406996,-2.46411805576835,
311.664369596043));
#16539=CARTESIAN_POINT('Ctrl Pts',(-32.2251037972259,-2.51396564760069,
311.659329053523));
#16540=CARTESIAN_POINT('Ctrl Pts',(-32.3062236426284,-2.55991097131137,
311.654288511003));
#16541=CARTESIAN_POINT('Ctrl Pts',(-32.3873933267648,-2.60588452309317,
311.649244871654));
#16542=CARTESIAN_POINT('Ctrl Pts',(-32.470675985273,-2.64795083367218,311.644201232306));
#16543=CARTESIAN_POINT('Ctrl Pts',(-32.5556549453796,-2.68593201429846,
311.639157592957));
#16544=CARTESIAN_POINT('Ctrl Pts',(-32.6407715047558,-2.7239746946502,311.634105786868));
#16545=CARTESIAN_POINT('Ctrl Pts',(-32.7275894358986,-2.75791887803125,
311.62905398078));
#16546=CARTESIAN_POINT('Ctrl Pts',(-32.815674702911,-2.78763581362287,311.624002174691));
#16547=CARTESIAN_POINT('Ctrl Pts',(-32.8602627937985,-2.80267829995457,
311.621444988947));
#16548=CARTESIAN_POINT('Ctrl Pts',(-32.9051754117061,-2.81663844162384,
311.618887803204));
#16549=CARTESIAN_POINT('Ctrl Pts',(-32.95035530731,-2.82950453941247,311.61633061746));
#16550=CARTESIAN_POINT('Ctrl Pts',(-33.0396180316545,-2.85492431794327,
311.611278340046));
#16551=CARTESIAN_POINT('Ctrl Pts',(-33.1302450405338,-2.87616160923921,
311.606226062632));
#16552=CARTESIAN_POINT('Ctrl Pts',(-33.2218086080801,-2.89307238572852,
311.601173785217));
#16553=CARTESIAN_POINT('Ctrl Pts',(-33.3132458927251,-2.90995983916505,
311.596128475818));
#16554=CARTESIAN_POINT('Ctrl Pts',(-33.4056167362174,-2.92253255510562,
311.591083166418));
#16555=CARTESIAN_POINT('Ctrl Pts',(-33.4984787311459,-2.9306963944669,311.586037857018));
#16556=CARTESIAN_POINT('Ctrl Pts',(-33.5912413452703,-2.93885149689636,
311.580997947103));
#16557=CARTESIAN_POINT('Ctrl Pts',(-33.684493625891,-2.94260706253087,311.575958037187));
#16558=CARTESIAN_POINT('Ctrl Pts',(-33.7777845509332,-2.94192028300932,
311.570918127272));
#16559=CARTESIAN_POINT('Ctrl Pts',(-33.8710082290045,-2.94123399853959,
311.565881850279));
#16560=CARTESIAN_POINT('Ctrl Pts',(-33.9642700531627,-2.93611173695307,
311.560845573286));
#16561=CARTESIAN_POINT('Ctrl Pts',(-34.0571165291237,-2.92656271392951,
311.555809296293));
#16562=CARTESIAN_POINT('Ctrl Pts',(-34.1499292438889,-2.91701716315874,
311.55077485061));
#16563=CARTESIAN_POINT('Ctrl Pts',(-34.2423264690152,-2.90304809414868,
311.545740404928));
#16564=CARTESIAN_POINT('Ctrl Pts',(-34.3338584093083,-2.88471670149476,
311.540705959245));
#16565=CARTESIAN_POINT('Ctrl Pts',(-34.425382672065,-2.86638684644549,311.535671935843));
#16566=CARTESIAN_POINT('Ctrl Pts',(-34.5160413587211,-2.84369548267463,
311.530637912441));
#16567=CARTESIAN_POINT('Ctrl Pts',(-34.6053945983624,-2.81675497501515,
311.525603889039));
#16568=CARTESIAN_POINT('Ctrl Pts',(-34.6947653390869,-2.78980919068004,
311.520568879653));
#16569=CARTESIAN_POINT('Ctrl Pts',(-34.7828296997837,-2.75861273818651,
311.515533870266));
#16570=CARTESIAN_POINT('Ctrl Pts',(-34.8691638114394,-2.72332758084775,
311.51049886088));
#16571=CARTESIAN_POINT('Ctrl Pts',(-34.9555927871857,-2.68800365210917,
311.505458319016));
#16572=CARTESIAN_POINT('Ctrl Pts',(-35.0402873069962,-2.64858221894387,
311.500417777152));
#16573=CARTESIAN_POINT('Ctrl Pts',(-35.1228445956338,-2.60527293825904,
311.495377235287));
#16574=CARTESIAN_POINT('Ctrl Pts',(-35.2054526062804,-2.56193704897603,
311.490333596587));
#16575=CARTESIAN_POINT('Ctrl Pts',(-35.2859203888052,-2.51470878157065,
311.485289957886));
#16576=CARTESIAN_POINT('Ctrl Pts',(-35.3638727366605,-2.46384206625863,
311.480246319186));
#16577=CARTESIAN_POINT('Ctrl Pts',(-35.4419513064852,-2.41289298656428,
311.475194513727));
#16578=CARTESIAN_POINT('Ctrl Pts',(-35.5175059506873,-2.3582939572961,311.470142708267));
#16579=CARTESIAN_POINT('Ctrl Pts',(-35.5901933664827,-2.3003401174577,311.465090902808));
#16580=CARTESIAN_POINT('Ctrl Pts',(-35.6269872843073,-2.27100424415282,
311.462533710302));
#16581=CARTESIAN_POINT('Ctrl Pts',(-35.6630470935547,-2.24080936808293,
311.459976517797));
#16582=CARTESIAN_POINT('Ctrl Pts',(-35.6983319533873,-2.20979727965005,
311.457419325291));
#16583=CARTESIAN_POINT('Ctrl Pts',(-35.7670192133601,-2.14942760861852,
311.4524413674));
#16584=CARTESIAN_POINT('Ctrl Pts',(-35.8330298232882,-2.08572835462146,
311.447463409509));
#16585=CARTESIAN_POINT('Ctrl Pts',(-35.8960161596962,-2.01896966106762,
311.442485451618));
#16586=CARTESIAN_POINT('Ctrl Pts',(-35.959444480282,-1.95174251216369,311.43747256268));
#16587=CARTESIAN_POINT('Ctrl Pts',(-36.0198055125062,-1.88141306145673,
311.432459673743));
#16588=CARTESIAN_POINT('Ctrl Pts',(-36.0767772751384,-1.80829931640985,
311.427446784806));
#16589=CARTESIAN_POINT('Ctrl Pts',(-36.1332079540307,-1.73587996200101,
311.42248150529));
#16590=CARTESIAN_POINT('Ctrl Pts',(-36.1863131607934,-1.66072932853249,
311.417516225775));
#16591=CARTESIAN_POINT('Ctrl Pts',(-36.2358173502925,-1.58319294210419,
311.41255094626));
#16592=CARTESIAN_POINT('Ctrl Pts',(-36.2852909788572,-1.50570442201681,
311.407588732012));
#16593=CARTESIAN_POINT('Ctrl Pts',(-36.3311677570923,-1.42583345800156,
311.402626517764));
#16594=CARTESIAN_POINT('Ctrl Pts',(-36.3732143473538,-1.34395608132238,
311.397664303517));
#16595=CARTESIAN_POINT('Ctrl Pts',(-36.4152475509804,-1.26210477245377,
311.39270366912));
#16596=CARTESIAN_POINT('Ctrl Pts',(-36.4534527797942,-1.17824872743093,
311.387743034723));
#16597=CARTESIAN_POINT('Ctrl Pts',(-36.487642382713,-1.0927890244623,311.382782400327));
#16598=CARTESIAN_POINT('Ctrl Pts',(-36.5224515185249,-1.00578074846246,
311.377731876726));
#16599=CARTESIAN_POINT('Ctrl Pts',(-36.5530978472644,-0.917110563339265,
311.372681353126));
#16600=CARTESIAN_POINT('Ctrl Pts',(-36.5794349219442,-0.8272221711891,311.367630829525));
#16601=CARTESIAN_POINT('Ctrl Pts',(-36.6053216305679,-0.738870877640935,
311.362666670277));
#16602=CARTESIAN_POINT('Ctrl Pts',(-36.6270452419933,-0.649343179726609,
311.357702511029));
#16603=CARTESIAN_POINT('Ctrl Pts',(-36.6445177946938,-0.55907312852248,
311.352738351781));
#16604=CARTESIAN_POINT('Ctrl Pts',(-36.662446317566,-0.466447356808736,
311.347644646005));
#16605=CARTESIAN_POINT('Ctrl Pts',(-36.67589872875,-0.373040454094561,311.342550940228));
#16606=CARTESIAN_POINT('Ctrl Pts',(-36.6848366520725,-0.279327624487683,
311.337457234452));
#16607=CARTESIAN_POINT('Ctrl Pts',(-36.6937745753949,-0.185614794880804,
311.332363528675));
#16608=CARTESIAN_POINT('Ctrl Pts',(-36.6981980415015,-0.0915965565959887,
311.327269822898));
#16609=CARTESIAN_POINT('Ctrl Pts',(-36.6981261623761,0.00225326298871554,
311.322176117122));
#16610=CARTESIAN_POINT('',(-36.6981262001274,-0.00220342124124626,310.322176117056));
#16611=CARTESIAN_POINT('Ctrl Pts',(-36.6981261623756,0.00225326359443262,
311.322176117089));
#16612=CARTESIAN_POINT('Ctrl Pts',(-36.6980148327132,0.1476120984491,311.314286755767));
#16613=CARTESIAN_POINT('Ctrl Pts',(-36.6871291095033,0.29256686069583,311.306397394444));
#16614=CARTESIAN_POINT('Ctrl Pts',(-36.6656558427427,0.435896845852016,
311.298508033121));
#16615=CARTESIAN_POINT('Ctrl Pts',(-36.6519045529365,0.527684098614721,
311.29345575602));
#16616=CARTESIAN_POINT('Ctrl Pts',(-36.633780885816,0.618984748458059,311.288403478919));
#16617=CARTESIAN_POINT('Ctrl Pts',(-36.6113304995924,0.709349786879677,
311.283351201818));
#16618=CARTESIAN_POINT('Ctrl Pts',(-36.5889110766032,0.799590195202268,
311.278305892742));
#16619=CARTESIAN_POINT('Ctrl Pts',(-36.5621768985692,0.888897128846525,
311.273260583666));
#16620=CARTESIAN_POINT('Ctrl Pts',(-36.5312251193052,0.976828832709801,
311.268215274589));
#16621=CARTESIAN_POINT('Ctrl Pts',(-36.500306464662,1.06466643198808,311.263175365007));
#16622=CARTESIAN_POINT('Ctrl Pts',(-36.4651793271225,1.15113131005255,311.258135455425));
#16623=CARTESIAN_POINT('Ctrl Pts',(-36.4259911615463,1.23579508566736,311.253095545842));
#16624=CARTESIAN_POINT('Ctrl Pts',(-36.3868312441088,1.32039783280476,311.248059269195));
#16625=CARTESIAN_POINT('Ctrl Pts',(-36.3436163031757,1.40320165603155,311.243022992548));
#16626=CARTESIAN_POINT('Ctrl Pts',(-36.2965421869159,1.48379742768906,311.237986715901));
#16627=CARTESIAN_POINT('Ctrl Pts',(-36.2494851880039,1.56436389267091,311.232952270573));
#16628=CARTESIAN_POINT('Ctrl Pts',(-36.1985720253936,1.64272351790864,311.227917825244));
#16629=CARTESIAN_POINT('Ctrl Pts',(-36.1440443485017,1.71849203005162,311.222883379916));
#16630=CARTESIAN_POINT('Ctrl Pts',(-36.0895212453757,1.79425418675342,311.217849356875));
#16631=CARTESIAN_POINT('Ctrl Pts',(-36.0313844904188,1.86742530200637,311.212815333834));
#16632=CARTESIAN_POINT('Ctrl Pts',(-35.9699182246906,1.93765129094818,311.207781310794));
#16633=CARTESIAN_POINT('Ctrl Pts',(-35.908439920019,2.00789103453554,311.202746301776));
#16634=CARTESIAN_POINT('Ctrl Pts',(-35.8436311023061,2.07518417217566,311.197711292758));
#16635=CARTESIAN_POINT('Ctrl Pts',(-35.7758144608132,2.13921169187599,311.192676283741));
#16636=CARTESIAN_POINT('Ctrl Pts',(-35.7079233023717,2.20330956503658,311.187635742254));
#16637=CARTESIAN_POINT('Ctrl Pts',(-35.6370180465144,2.26413435220616,311.182595200767));
#16638=CARTESIAN_POINT('Ctrl Pts',(-35.5634560913953,2.32140596335365,311.177554659279));
#16639=CARTESIAN_POINT('Ctrl Pts',(-35.4898489409464,2.37871276129504,311.172511020961));
#16640=CARTESIAN_POINT('Ctrl Pts',(-35.4135822046436,2.43246178152501,311.167467382643));
#16641=CARTESIAN_POINT('Ctrl Pts',(-35.3350421986589,2.48241633800681,311.162423744325));
#16642=CARTESIAN_POINT('Ctrl Pts',(-35.2563750192213,2.53245178184475,311.157371939253));
#16643=CARTESIAN_POINT('Ctrl Pts',(-35.1754276068903,2.57868027601982,311.152320134181));
#16644=CARTESIAN_POINT('Ctrl Pts',(-35.0926106134532,2.62091121911518,311.147268329109));
#16645=CARTESIAN_POINT('Ctrl Pts',(-35.0506891050683,2.64228829115798,311.144711133057));
#16646=CARTESIAN_POINT('Ctrl Pts',(-35.0082888671287,2.66264182700462,311.142153937005));
#16647=CARTESIAN_POINT('Ctrl Pts',(-34.965464834845,2.68195191274982,311.139596740952));
#16648=CARTESIAN_POINT('Ctrl Pts',(-34.8808569799058,2.72010303599686,311.134544463969));
#16649=CARTESIAN_POINT('Ctrl Pts',(-34.7942901489513,2.75431501252286,311.129492186985));
#16650=CARTESIAN_POINT('Ctrl Pts',(-34.7061665257702,2.78438304611017,311.124439910002));
#16651=CARTESIAN_POINT('Ctrl Pts',(-34.6181644413726,2.8144096103151,311.119394601043));
#16652=CARTESIAN_POINT('Ctrl Pts',(-34.5286102481237,2.84030344632051,311.114349292085));
#16653=CARTESIAN_POINT('Ctrl Pts',(-34.437927921793,2.86190697568658,311.109303983126));
#16654=CARTESIAN_POINT('Ctrl Pts',(-34.3473426437734,2.88348738493516,311.104264073662));
#16655=CARTESIAN_POINT('Ctrl Pts',(-34.2556320622605,2.90078651142138,311.099224164198));
#16656=CARTESIAN_POINT('Ctrl Pts',(-34.1632361529169,2.91369630506964,311.094184254733));
#16657=CARTESIAN_POINT('Ctrl Pts',(-34.0709068456309,2.92659679290744,311.089147978204));
#16658=CARTESIAN_POINT('Ctrl Pts',(-33.9778936311397,2.93511417545618,311.084111701675));
#16659=CARTESIAN_POINT('Ctrl Pts',(-33.8846465090519,2.93919151167209,311.079075425146));
#16660=CARTESIAN_POINT('Ctrl Pts',(-33.7914332939919,2.94326736526473,311.074040979935));
#16661=CARTESIAN_POINT('Ctrl Pts',(-33.6979867836906,2.94290636054035,311.069006534724));
#16662=CARTESIAN_POINT('Ctrl Pts',(-33.6047608896535,2.93810351978828,311.063972089513));
#16663=CARTESIAN_POINT('Ctrl Pts',(-33.5115428153734,2.9333010818969,311.05893806659));
#16664=CARTESIAN_POINT('Ctrl Pts',(-33.4185457642236,2.92405757179316,311.053904043667));
#16665=CARTESIAN_POINT('Ctrl Pts',(-33.326221283017,2.9104200818419,311.048870020744));
#16666=CARTESIAN_POINT('Ctrl Pts',(-33.2338787188888,2.8967799208151,311.043835011843));
#16667=CARTESIAN_POINT('Ctrl Pts',(-33.1422094257301,2.87874413603304,311.038800002943));
#16668=CARTESIAN_POINT('Ctrl Pts',(-33.0516563439135,2.85641122024238,311.033764994042));
#16669=CARTESIAN_POINT('Ctrl Pts',(-32.9610037623138,2.83405376502985,311.028724452671));
#16670=CARTESIAN_POINT('Ctrl Pts',(-32.8714702722827,2.80738986029844,311.023683911299));
#16671=CARTESIAN_POINT('Ctrl Pts',(-32.7834848927091,2.77656825631777,311.018643369928));
#16672=CARTESIAN_POINT('Ctrl Pts',(-32.6954454562649,2.74572771601533,311.013599731725));
#16673=CARTESIAN_POINT('Ctrl Pts',(-32.6089564353067,2.71072455764135,311.008556093522));
#16674=CARTESIAN_POINT('Ctrl Pts',(-32.5244260231715,2.67175534835436,311.003512455319));
#16675=CARTESIAN_POINT('Ctrl Pts',(-32.4397587377679,2.63272303937452,310.99846065036));
#16676=CARTESIAN_POINT('Ctrl Pts',(-32.3570567861788,2.58971206365978,310.993408845401));
#16677=CARTESIAN_POINT('Ctrl Pts',(-32.2767028009575,2.54296440489324,310.988357040442));
#16678=CARTESIAN_POINT('Ctrl Pts',(-32.2360280343565,2.51930098478736,310.985799843223));
#16679=CARTESIAN_POINT('Ctrl Pts',(-32.195954421594,2.49468078637952,310.983242646003));
#16680=CARTESIAN_POINT('Ctrl Pts',(-32.1565284555702,2.46913920544266,310.980685448783));
#16681=CARTESIAN_POINT('Ctrl Pts',(-32.0786342298843,2.41867648073303,310.975633171884));
#16682=CARTESIAN_POINT('Ctrl Pts',(-32.0029904579736,2.36443355494242,310.970580894984));
#16683=CARTESIAN_POINT('Ctrl Pts',(-31.9299871189817,2.30663760541324,310.965528618085));
#16684=CARTESIAN_POINT('Ctrl Pts',(-31.8570844651319,2.2489213672161,310.960483309213));
#16685=CARTESIAN_POINT('Ctrl Pts',(-31.7868153530777,2.18766211611815,310.95543800034));
#16686=CARTESIAN_POINT('Ctrl Pts',(-31.719541870994,2.12313092140667,310.950392691468));
#16687=CARTESIAN_POINT('Ctrl Pts',(-31.6523403850784,2.05866878806375,310.945352782092));
#16688=CARTESIAN_POINT('Ctrl Pts',(-31.5881284757504,1.99094197702334,310.940312872715));
#16689=CARTESIAN_POINT('Ctrl Pts',(-31.5272352609016,1.92026183183079,310.935272963339));
#16690=CARTESIAN_POINT('Ctrl Pts',(-31.4663859399434,1.84963263527946,310.9302366869));
#16691=CARTESIAN_POINT('Ctrl Pts',(-31.4088508477137,1.77605467159468,310.925200410461));
#16692=CARTESIAN_POINT('Ctrl Pts',(-31.3549215665312,1.69987539101623,310.920164134022));
#16693=CARTESIAN_POINT('Ctrl Pts',(-31.3010118954231,1.62372381118455,310.915129688903));
#16694=CARTESIAN_POINT('Ctrl Pts',(-31.2507056870232,1.54497315582983,310.910095243784));
#16695=CARTESIAN_POINT('Ctrl Pts',(-31.2042529596907,1.46400230651697,310.905060798664));
#16696=CARTESIAN_POINT('Ctrl Pts',(-31.1578041288089,1.38303824903183,310.900026775834));
#16697=CARTESIAN_POINT('Ctrl Pts',(-31.1152083572513,1.29985475329337,310.894992753003));
#16698=CARTESIAN_POINT('Ctrl Pts',(-31.076670610348,1.21485691363216,310.889958730173));
#16699=CARTESIAN_POINT('Ctrl Pts',(-31.0381253153461,1.12984242608344,310.884923721366));
#16700=CARTESIAN_POINT('Ctrl Pts',(-31.0036398066047,1.04301329360174,310.87988871256));
#16701=CARTESIAN_POINT('Ctrl Pts',(-30.9733711789297,0.954795213502898,
310.874853703753));
#16702=CARTESIAN_POINT('Ctrl Pts',(-30.9430692920738,0.866480199340128,
310.869813162476));
#16703=CARTESIAN_POINT('Ctrl Pts',(-30.9169936797229,0.776773611991706,
310.8647726212));
#16704=CARTESIAN_POINT('Ctrl Pts',(-30.8952516483215,0.686116664745062,
310.859732079923));
#16705=CARTESIAN_POINT('Ctrl Pts',(-30.8734962589519,0.595404019270442,
310.854688441816));
#16706=CARTESIAN_POINT('Ctrl Pts',(-30.8560798338832,0.503740287619101,
310.849644803709));
#16707=CARTESIAN_POINT('Ctrl Pts',(-30.843058203726,0.41157507337135,310.844601165602));
#16708=CARTESIAN_POINT('Ctrl Pts',(-30.8300154886953,0.319260623439119,
310.839549360739));
#16709=CARTESIAN_POINT('Ctrl Pts',(-30.8213818161632,0.226443511624768,
310.834497555876));
#16710=CARTESIAN_POINT('Ctrl Pts',(-30.8171609942021,0.133576451149687,
310.829445751013));
#16711=CARTESIAN_POINT('Ctrl Pts',(-30.8150244354211,0.0865676136897683,
310.82688855288));
#16712=CARTESIAN_POINT('Ctrl Pts',(-30.8140177651276,0.0395459504315597,
310.824331354747));
#16713=CARTESIAN_POINT('Ctrl Pts',(-30.8141364081974,-0.00743028464432902,
310.821774156614));
#16714=CARTESIAN_POINT('Ctrl Pts',(-30.814370812267,-0.100241611016934,
310.816721879646));
#16715=CARTESIAN_POINT('Ctrl Pts',(-30.8190018384742,-0.19320842813451,
310.811669602677));
#16716=CARTESIAN_POINT('Ctrl Pts',(-30.8280497205578,-0.285879865856423,
310.806617325709));
#16717=CARTESIAN_POINT('Ctrl Pts',(-30.8370851239363,-0.378423492501761,
310.801572016766));
#16718=CARTESIAN_POINT('Ctrl Pts',(-30.850525235491,-0.470672110956442,
310.796526707824));
#16719=CARTESIAN_POINT('Ctrl Pts',(-30.8683382860445,-0.562174525991569,
310.791481398881));
#16720=CARTESIAN_POINT('Ctrl Pts',(-30.8861322730517,-0.653579015041502,
310.786441489434));
#16721=CARTESIAN_POINT('Ctrl Pts',(-30.9082898125679,-0.74423845425817,
310.781401579986));
#16722=CARTESIAN_POINT('Ctrl Pts',(-30.934727422777,-0.833707552516224,
310.776361670539));
#16723=CARTESIAN_POINT('Ctrl Pts',(-30.9611459758679,-0.923112158440201,
310.771325394027));
#16724=CARTESIAN_POINT('Ctrl Pts',(-30.9918383418163,-1.01132770405547,
310.766289117516));
#16725=CARTESIAN_POINT('Ctrl Pts',(-31.0266703570855,-1.09792089722844,
310.761252841005));
#16726=CARTESIAN_POINT('Ctrl Pts',(-31.0614897065423,-1.1844826028998,310.756218395812));
#16727=CARTESIAN_POINT('Ctrl Pts',(-31.1004455492921,-1.26942271633927,
310.75118395062));
#16728=CARTESIAN_POINT('Ctrl Pts',(-31.1433547886595,-1.35232586297179,
310.746149505428));
#16729=CARTESIAN_POINT('Ctrl Pts',(-31.1862604288087,-1.43522205570513,
310.741115482524));
#16730=CARTESIAN_POINT('Ctrl Pts',(-31.2331186018868,-1.5160812268844,310.73608145962));
#16731=CARTESIAN_POINT('Ctrl Pts',(-31.2836997753803,-1.59451167887353,
310.731047436716));
#16732=CARTESIAN_POINT('Ctrl Pts',(-31.3342908558324,-1.67295749245256,
310.726012427835));
#16733=CARTESIAN_POINT('Ctrl Pts',(-31.3886061438107,-1.7489732689834,310.720977418954));
#16734=CARTESIAN_POINT('Ctrl Pts',(-31.4463728608584,-1.82219639447585,
310.715942410074));
#16735=CARTESIAN_POINT('Ctrl Pts',(-31.5042030520017,-1.89549997757259,
310.710901868723));
#16736=CARTESIAN_POINT('Ctrl Pts',(-31.5654919667713,-1.96600443508492,
310.705861327372));
#16737=CARTESIAN_POINT('Ctrl Pts',(-31.6299268184473,-2.03338060395983,
310.700820786021));
#16738=CARTESIAN_POINT('Ctrl Pts',(-31.6944012579037,-2.10079816771507,
310.695777147839));
#16739=CARTESIAN_POINT('Ctrl Pts',(-31.7620251603763,-2.16508331070172,
310.690733509658));
#16740=CARTESIAN_POINT('Ctrl Pts',(-31.8324508071149,-2.22594559856081,
310.685689871476));
#16741=CARTESIAN_POINT('Ctrl Pts',(-31.9029904884068,-2.28690643579974,
310.680638066539));
#16742=CARTESIAN_POINT('Ctrl Pts',(-31.9763406216714,-2.34443307946837,
310.675586261602));
#16743=CARTESIAN_POINT('Ctrl Pts',(-32.0521226991807,-2.39827714343257,
310.670534456665));
#16744=CARTESIAN_POINT('Ctrl Pts',(-32.0904831930016,-2.42553272880159,
310.667977259258));
#16745=CARTESIAN_POINT('Ctrl Pts',(-32.1294664045489,-2.45184542834957,
310.665420061851));
#16746=CARTESIAN_POINT('Ctrl Pts',(-32.1690208852344,-2.4771875383791,310.662862864445));
#16747=CARTESIAN_POINT('Ctrl Pts',(-32.2471690135683,-2.52725616353908,
310.657810587493));
#16748=CARTESIAN_POINT('Ctrl Pts',(-32.3278290201464,-2.57371301198809,
310.652758310541));
#16749=CARTESIAN_POINT('Ctrl Pts',(-32.4106328426013,-2.61629688767119,
310.647706033589));
#16750=CARTESIAN_POINT('Ctrl Pts',(-32.4933224632462,-2.6588220323014,310.642660724663));
#16751=CARTESIAN_POINT('Ctrl Pts',(-32.578149632747,-2.69748461708396,310.637615415737));
#16752=CARTESIAN_POINT('Ctrl Pts',(-32.6647178511997,-2.73206698577875,
310.632570106811));
#16753=CARTESIAN_POINT('Ctrl Pts',(-32.7511934242478,-2.76661234438375,
310.627530197381));
#16754=CARTESIAN_POINT('Ctrl Pts',(-32.8394059323737,-2.79708600235729,
310.62249028795));
#16755=CARTESIAN_POINT('Ctrl Pts',(-32.9289358318737,-2.82331697292177,
310.617450378519));
#16756=CARTESIAN_POINT('Ctrl Pts',(-33.0184011952104,-2.84952903532029,
310.612414102025));
#16757=CARTESIAN_POINT('Ctrl Pts',(-33.10918163731,-2.87150436450134,310.60737782553));
#16758=CARTESIAN_POINT('Ctrl Pts',(-33.2008402526277,-2.88912107744592,
310.602341549036));
#16759=CARTESIAN_POINT('Ctrl Pts',(-33.2924655385258,-2.90673138450256,
310.59730710386));
#16760=CARTESIAN_POINT('Ctrl Pts',(-33.3849679274346,-2.91998614013725,
310.592272658685));
#16761=CARTESIAN_POINT('Ctrl Pts',(-33.4778990743842,-2.9288143005921,310.58723821351));
#16762=CARTESIAN_POINT('Ctrl Pts',(-33.5708224262876,-2.9376417205426,310.582204190623));
#16763=CARTESIAN_POINT('Ctrl Pts',(-33.6641740224438,-2.94204324171661,
310.577170167736));
#16764=CARTESIAN_POINT('Ctrl Pts',(-33.7575002725516,-2.94199967950234,
310.572136144848));
#16765=CARTESIAN_POINT('Ctrl Pts',(-33.8508448017788,-2.94195610875586,
310.567101135985));
#16766=CARTESIAN_POINT('Ctrl Pts',(-33.9441635308687,-2.93746572613335,
310.562066127121));
#16767=CARTESIAN_POINT('Ctrl Pts',(-34.0370038969137,-2.92856145282435,
310.557031118257));
#16768=CARTESIAN_POINT('Ctrl Pts',(-34.1299462759984,-2.91964739549548,
310.551990576923));
#16769=CARTESIAN_POINT('Ctrl Pts',(-34.2224087999158,-2.90630980881408,
310.546950035589));
#16770=CARTESIAN_POINT('Ctrl Pts',(-34.3139453579785,-2.88863336331914,
310.541909494255));
#16771=CARTESIAN_POINT('Ctrl Pts',(-34.4055381546934,-2.87094605768821,
310.53686585609));
#16772=CARTESIAN_POINT('Ctrl Pts',(-34.4962034216126,-2.84891469112421,
310.531822217925));
#16773=CARTESIAN_POINT('Ctrl Pts',(-34.5855086862144,-2.82267427459644,
310.52677857976));
#16774=CARTESIAN_POINT('Ctrl Pts',(-34.674958555612,-2.79639136908337,310.52172677484));
#16775=CARTESIAN_POINT('Ctrl Pts',(-34.7630436071173,-2.76588595274888,
310.516674969919));
#16776=CARTESIAN_POINT('Ctrl Pts',(-34.8493500407492,-2.7313416919894,310.511623164999));
#16777=CARTESIAN_POINT('Ctrl Pts',(-34.8930379119615,-2.71385556550174,
310.509065967424));
#16778=CARTESIAN_POINT('Ctrl Pts',(-34.9362704105143,-2.69533529825263,
310.50650876985));
#16779=CARTESIAN_POINT('Ctrl Pts',(-34.9789963834475,-2.67580913609329,
310.503951572275));
#16780=CARTESIAN_POINT('Ctrl Pts',(-35.0634104506821,-2.63723113184438,
310.49889929533));
#16781=CARTESIAN_POINT('Ctrl Pts',(-35.1461487115125,-2.59458543339695,
310.493847018385));
#16782=CARTESIAN_POINT('Ctrl Pts',(-35.2267922544889,-2.54803998860497,
310.48879474144));
#16783=CARTESIAN_POINT('Ctrl Pts',(-35.3073245750781,-2.5015587386052,310.483749432521));
#16784=CARTESIAN_POINT('Ctrl Pts',(-35.3857675372035,-2.45118865011851,
310.478704123603));
#16785=CARTESIAN_POINT('Ctrl Pts',(-35.4617234293671,-2.39714515753402,
310.473658814684));
#16786=CARTESIAN_POINT('Ctrl Pts',(-35.5375980334471,-2.34315950235777,
310.46861890526));
#16787=CARTESIAN_POINT('Ctrl Pts',(-35.6109904979903,-2.28550851326761,
310.463578995837));
#16788=CARTESIAN_POINT('Ctrl Pts',(-35.6815298635595,-2.22445227196699,
310.458539086413));
#16789=CARTESIAN_POINT('Ctrl Pts',(-35.7520183819782,-2.16344004206148,
310.453502809926));
#16790=CARTESIAN_POINT('Ctrl Pts',(-35.8196575542849,-2.09902772875571,
310.44846653344));
#16791=CARTESIAN_POINT('Ctrl Pts',(-35.8841082967683,-2.03151660295942,
310.443430256953));
#16792=CARTESIAN_POINT('Ctrl Pts',(-35.9485356033097,-1.96403002593893,
310.438395811785));
#16793=CARTESIAN_POINT('Ctrl Pts',(-36.0097764768289,-1.89344719596275,
310.433361366617));
#16794=CARTESIAN_POINT('Ctrl Pts',(-36.0675283757988,-1.82010653444136,
310.428326921449));
#16795=CARTESIAN_POINT('Ctrl Pts',(-36.1252754305495,-1.74677202472187,
310.42329289857));
#16796=CARTESIAN_POINT('Ctrl Pts',(-36.1795338179152,-1.67068049253444,
310.418258875691));
#16797=CARTESIAN_POINT('Ctrl Pts',(-36.2300417505706,-1.59220285512856,
310.413224852811));
#16798=CARTESIAN_POINT('Ctrl Pts',(-36.2805595758385,-1.51370984689249,
310.408189843955));
#16799=CARTESIAN_POINT('Ctrl Pts',(-36.3273252474256,-1.43283017903317,
310.403154835099));
#16800=CARTESIAN_POINT('Ctrl Pts',(-36.3701213368016,-1.34996212510415,
310.398119826244));
#16801=CARTESIAN_POINT('Ctrl Pts',(-36.4129644505407,-1.26700301571866,
310.393079284918));
#16802=CARTESIAN_POINT('Ctrl Pts',(-36.4518290712748,-1.18205155440164,
310.388038743592));
#16803=CARTESIAN_POINT('Ctrl Pts',(-36.4865447676517,-1.09552861761781,
310.382998202266));
#16804=CARTESIAN_POINT('Ctrl Pts',(-36.5212817928175,-1.00895252247476,
310.377954564109));
#16805=CARTESIAN_POINT('Ctrl Pts',(-36.551864673487,-0.920803449165568,
310.372910925952));
#16806=CARTESIAN_POINT('Ctrl Pts',(-36.5781726829229,-0.831518073196525,
310.367867287795));
#16807=CARTESIAN_POINT('Ctrl Pts',(-36.6045232907916,-0.742088124636358,
310.362815482882));
#16808=CARTESIAN_POINT('Ctrl Pts',(-36.6265851035865,-0.651518631330701,
310.35776367797));
#16809=CARTESIAN_POINT('Ctrl Pts',(-36.6442884092663,-0.560256923135343,
310.352711873057));
#16810=CARTESIAN_POINT('Ctrl Pts',(-36.6532497315015,-0.514060716072903,
310.350154675407));
#16811=CARTESIAN_POINT('Ctrl Pts',(-36.6610950854093,-0.467687234593608,
310.347597477756));
#16812=CARTESIAN_POINT('Ctrl Pts',(-36.6678205117366,-0.421194777740095,
310.345040280106));
#16813=CARTESIAN_POINT('Ctrl Pts',(-36.6878647509024,-0.282630190273806,
310.337418892434));
#16814=CARTESIAN_POINT('Ctrl Pts',(-36.6980210483658,-0.14260159061453,
310.329797504762));
#16815=CARTESIAN_POINT('Ctrl Pts',(-36.698126200127,-0.00220342186298763,
310.32217611709));
#16816=CARTESIAN_POINT('',(-36.6981268542406,-0.00100312718013536,309.322176117137));
#16817=CARTESIAN_POINT('Ctrl Pts',(-36.6981262001274,-0.00220342124124822,
310.322176117056));
#16818=CARTESIAN_POINT('Ctrl Pts',(-36.6981948132346,0.0894085233407486,
310.317203045461));
#16819=CARTESIAN_POINT('Ctrl Pts',(-36.6939801246682,0.181182574134905,
310.312229973866));
#16820=CARTESIAN_POINT('Ctrl Pts',(-36.6854632440038,0.272678047413998,
310.30725690227));
#16821=CARTESIAN_POINT('Ctrl Pts',(-36.6768197596925,0.365533603222195,
310.30220990584));
#16822=CARTESIAN_POINT('Ctrl Pts',(-36.6637450630147,0.458101758252811,
310.297162909409));
#16823=CARTESIAN_POINT('Ctrl Pts',(-36.6462743635366,0.549920324264078,
310.292115912979));
#16824=CARTESIAN_POINT('Ctrl Pts',(-36.6290924162591,0.640221331518039,
310.287152332288));
#16825=CARTESIAN_POINT('Ctrl Pts',(-36.6076587613469,0.729796870639183,
310.282188751598));
#16826=CARTESIAN_POINT('Ctrl Pts',(-36.5820590621694,0.818212761300913,
310.277225170907));
#16827=CARTESIAN_POINT('Ctrl Pts',(-36.5564689397755,0.906595575798285,
310.27226344708));
#16828=CARTESIAN_POINT('Ctrl Pts',(-36.5267159943775,0.99381916317762,310.267301723252));
#16829=CARTESIAN_POINT('Ctrl Pts',(-36.4929364206862,1.0794620572737,310.262339999425));
#16830=CARTESIAN_POINT('Ctrl Pts',(-36.4591593905128,1.16509850267292,310.257378649203));
#16831=CARTESIAN_POINT('Ctrl Pts',(-36.4213565034685,1.24915406511091,310.252417298981));
#16832=CARTESIAN_POINT('Ctrl Pts',(-36.3797125300232,1.33122616379923,310.247455948759));
#16833=CARTESIAN_POINT('Ctrl Pts',(-36.3368159693807,1.41576686602291,310.242345368691));
#16834=CARTESIAN_POINT('Ctrl Pts',(-36.289843781522,1.49820241227349,310.237234788622));
#16835=CARTESIAN_POINT('Ctrl Pts',(-36.2390485695323,1.57812059265973,310.232124208554));
#16836=CARTESIAN_POINT('Ctrl Pts',(-36.189671218157,1.6558079950668,310.227156281501));
#16837=CARTESIAN_POINT('Ctrl Pts',(-36.1366817872867,1.73111637604713,310.222188354449));
#16838=CARTESIAN_POINT('Ctrl Pts',(-36.0803549698273,1.80369855066789,310.217220427397));
#16839=CARTESIAN_POINT('Ctrl Pts',(-36.0216020326857,1.87940699888914,310.21203852082));
#16840=CARTESIAN_POINT('Ctrl Pts',(-35.9592181044242,1.95214867708126,310.206856614243));
#16841=CARTESIAN_POINT('Ctrl Pts',(-35.8935582465988,2.02157160992029,310.201674707667));
#16842=CARTESIAN_POINT('Ctrl Pts',(-35.8278983887735,2.09099454275932,310.19649280109));
#16843=CARTESIAN_POINT('Ctrl Pts',(-35.7589630590051,2.15709840293153,310.191310894513));
#16844=CARTESIAN_POINT('Ctrl Pts',(-35.6871451388127,2.21957947483799,310.186128987937));
#16845=CARTESIAN_POINT('Ctrl Pts',(-35.6171238025698,2.28049753168308,310.181076710987));
#16846=CARTESIAN_POINT('Ctrl Pts',(-35.5440912695704,2.33820822865127,310.176024434037));
#16847=CARTESIAN_POINT('Ctrl Pts',(-35.4683736292143,2.39239954172348,310.170972157087));
#16848=CARTESIAN_POINT('Ctrl Pts',(-35.3927604175115,2.44651611493563,310.165926848163));
#16849=CARTESIAN_POINT('Ctrl Pts',(-35.3144698154288,2.49712269321811,310.160881539239));
#16850=CARTESIAN_POINT('Ctrl Pts',(-35.2338623888242,2.54394618560706,310.155836230315));
#16851=CARTESIAN_POINT('Ctrl Pts',(-35.1533412283792,2.59071956744122,310.150796320886));
#16852=CARTESIAN_POINT('Ctrl Pts',(-35.0705085538136,2.63371768876335,310.145756411457));
#16853=CARTESIAN_POINT('Ctrl Pts',(-34.9857545271178,2.67271027361161,310.140716502029));
#16854=CARTESIAN_POINT('Ctrl Pts',(-34.9010615939771,2.71167475129226,310.135680225536));
#16855=CARTESIAN_POINT('Ctrl Pts',(-34.8144504639697,2.7466392463159,310.130643949044));
#16856=CARTESIAN_POINT('Ctrl Pts',(-34.7263356284558,2.77741953371835,310.125607672552));
#16857=CARTESIAN_POINT('Ctrl Pts',(-34.6382528337535,2.80818862861973,310.120573227378));
#16858=CARTESIAN_POINT('Ctrl Pts',(-34.548667838774,2.83477639213302,310.115538782205));
#16859=CARTESIAN_POINT('Ctrl Pts',(-34.4580138578032,2.85704722997347,310.110504337032));
#16860=CARTESIAN_POINT('Ctrl Pts',(-34.3673674808716,2.87931619974016,310.105470314147));
#16861=CARTESIAN_POINT('Ctrl Pts',(-34.2756527276982,2.89726885796853,310.100436291262));
#16862=CARTESIAN_POINT('Ctrl Pts',(-34.1833155560286,2.91082015232438,310.095402268377));
#16863=CARTESIAN_POINT('Ctrl Pts',(-34.0909602989637,2.92437410087151,310.090367259516));
#16864=CARTESIAN_POINT('Ctrl Pts',(-33.9979828208674,2.93352490934959,310.085332250654));
#16865=CARTESIAN_POINT('Ctrl Pts',(-33.9048356530551,2.93823922511741,310.080297241793));
#16866=CARTESIAN_POINT('Ctrl Pts',(-33.8115861350909,2.94295872097762,310.075256700461));
#16867=CARTESIAN_POINT('Ctrl Pts',(-33.7181669995994,2.94323197091792,310.070216159129));
#16868=CARTESIAN_POINT('Ctrl Pts',(-33.6250319325769,2.93907775954891,310.065175617798));
#16869=CARTESIAN_POINT('Ctrl Pts',(-33.531839644804,2.93492099589643,310.060131979635));
#16870=CARTESIAN_POINT('Ctrl Pts',(-33.4389322149921,2.92633139648946,310.055088341473));
#16871=CARTESIAN_POINT('Ctrl Pts',(-33.3467571692897,2.9133795360414,310.05004470331));
#16872=CARTESIAN_POINT('Ctrl Pts',(-33.2544328719875,2.9004067036928,310.044992898392));
#16873=CARTESIAN_POINT('Ctrl Pts',(-33.1628437622273,2.88305759155797,310.039941093474));
#16874=CARTESIAN_POINT('Ctrl Pts',(-33.0724259801845,2.86145363075587,310.034889288556));
#16875=CARTESIAN_POINT('Ctrl Pts',(-33.0266569652171,2.85051781721382,310.03233209096));
#16876=CARTESIAN_POINT('Ctrl Pts',(-32.9811878275027,2.83849256113045,310.029774893363));
#16877=CARTESIAN_POINT('Ctrl Pts',(-32.9360732888412,2.82539835587649,310.027217695767));
#16878=CARTESIAN_POINT('Ctrl Pts',(-32.846940112708,2.79952802365425,310.022165418817));
#16879=CARTESIAN_POINT('Ctrl Pts',(-32.7588723470157,2.76938927675331,310.017113141868));
#16880=CARTESIAN_POINT('Ctrl Pts',(-32.6723088992443,2.73508725084322,310.012060864919));
#16881=CARTESIAN_POINT('Ctrl Pts',(-32.585864838504,2.70083253378158,310.007015555995));
#16882=CARTESIAN_POINT('Ctrl Pts',(-32.5009213823539,2.6624261099013,310.001970247071));
#16883=CARTESIAN_POINT('Ctrl Pts',(-32.4179033815805,2.62002318300882,309.996924938148));
#16884=CARTESIAN_POINT('Ctrl Pts',(-32.3349742267663,2.57766563577707,309.99188502872));
#16885=CARTESIAN_POINT('Ctrl Pts',(-32.2539668250374,2.53132028783144,309.986845119292));
#16886=CARTESIAN_POINT('Ctrl Pts',(-32.1752860640212,2.48119041092724,309.981805209864));
#16887=CARTESIAN_POINT('Ctrl Pts',(-32.0966620187463,2.43109666932591,309.976768933372));
#16888=CARTESIAN_POINT('Ctrl Pts',(-32.0203616542664,2.37722405910684,309.97173265688));
#16889=CARTESIAN_POINT('Ctrl Pts',(-31.9467643223076,2.31982124509054,309.966696380388));
#16890=CARTESIAN_POINT('Ctrl Pts',(-31.8731937522243,2.26243930420819,309.961661935216));
#16891=CARTESIAN_POINT('Ctrl Pts',(-31.8023246119943,2.20152998262774,309.956627490043));
#16892=CARTESIAN_POINT('Ctrl Pts',(-31.7345055124579,2.13738402234726,309.95159304487));
#16893=CARTESIAN_POINT('Ctrl Pts',(-31.6666921015751,2.07324344261824,309.946559021986));
#16894=CARTESIAN_POINT('Ctrl Pts',(-31.6019285453523,2.00586706937989,309.941524999102));
#16895=CARTESIAN_POINT('Ctrl Pts',(-31.5405278686293,1.93558373033768,309.936490976218));
#16896=CARTESIAN_POINT('Ctrl Pts',(-31.4791151658125,1.86528662542069,309.931455967357));
#16897=CARTESIAN_POINT('Ctrl Pts',(-31.4210669425874,1.79208175872728,309.926420958496));
#16898=CARTESIAN_POINT('Ctrl Pts',(-31.3666563229955,1.71633148401794,309.921385949635));
#16899=CARTESIAN_POINT('Ctrl Pts',(-31.3121859169892,1.64049797487098,309.916345408304));
#16900=CARTESIAN_POINT('Ctrl Pts',(-31.2613613526787,1.56211383615331,309.911304866973));
#16901=CARTESIAN_POINT('Ctrl Pts',(-31.2144125506615,1.48157062930825,309.906264325642));
#16902=CARTESIAN_POINT('Ctrl Pts',(-31.1674349040235,1.40097793795746,309.90122068748));
#16903=CARTESIAN_POINT('Ctrl Pts',(-31.1243379652487,1.31822393141491,309.896177049318));
#16904=CARTESIAN_POINT('Ctrl Pts',(-31.0853047818433,1.23372304188724,309.891133411156));
#16905=CARTESIAN_POINT('Ctrl Pts',(-31.0462083951598,1.14908532690086,309.886081606239));
#16906=CARTESIAN_POINT('Ctrl Pts',(-31.0111890669144,1.06269549320429,309.881029801322));
#16907=CARTESIAN_POINT('Ctrl Pts',(-30.980380926012,0.974985944782278,309.875977996404));
#16908=CARTESIAN_POINT('Ctrl Pts',(-30.9647860039348,0.930587823603603,
309.873420798802));
#16909=CARTESIAN_POINT('Ctrl Pts',(-30.9502693244297,0.885851761032472,
309.8708636012));
#16910=CARTESIAN_POINT('Ctrl Pts',(-30.9368432966644,0.840834857561148,
309.868306403598));
#16911=CARTESIAN_POINT('Ctrl Pts',(-30.9103173799509,0.751894580283191,
309.863254126648));
#16912=CARTESIAN_POINT('Ctrl Pts',(-30.8879566910281,0.661538202464539,
309.858201849698));
#16913=CARTESIAN_POINT('Ctrl Pts',(-30.8699105561981,0.570191628954484,
309.853149572748));
#16914=CARTESIAN_POINT('Ctrl Pts',(-30.8518893103312,0.478971039291871,
309.848104263823));
#16915=CARTESIAN_POINT('Ctrl Pts',(-30.8381708793757,0.386763399734169,
309.843058954899));
#16916=CARTESIAN_POINT('Ctrl Pts',(-30.8288548872494,0.294009914868297,
309.838013645975));
#16917=CARTESIAN_POINT('Ctrl Pts',(-30.8195488651085,0.201355694887732,
309.832973736546));
#16918=CARTESIAN_POINT('Ctrl Pts',(-30.8146359611485,0.108157230370923,
309.827933827117));
#16919=CARTESIAN_POINT('Ctrl Pts',(-30.8141645794648,0.0148649771324433,
309.822893917688));
#16920=CARTESIAN_POINT('Ctrl Pts',(-30.813693537569,-0.0783600279098104,
309.817857641196));
#16921=CARTESIAN_POINT('Ctrl Pts',(-30.8176576565629,-0.171678244323985,
309.812821364703));
#16922=CARTESIAN_POINT('Ctrl Pts',(-30.8260533512008,-0.264636098443424,
309.80778508821));
#16923=CARTESIAN_POINT('Ctrl Pts',(-30.834445992949,-0.357560150705554,
309.802750643037));
#16924=CARTESIAN_POINT('Ctrl Pts',(-30.8472669691344,-0.450123658982208,
309.797716197864));
#16925=CARTESIAN_POINT('Ctrl Pts',(-30.8644606736798,-0.541876103138771,
309.79268175269));
#16926=CARTESIAN_POINT('Ctrl Pts',(-30.8816529360205,-0.633620851117278,
309.787647729805));
#16927=CARTESIAN_POINT('Ctrl Pts',(-30.9032171154638,-0.724554233616771,
309.78261370692));
#16928=CARTESIAN_POINT('Ctrl Pts',(-30.9290463164374,-0.814235018785542,
309.777579684035));
#16929=CARTESIAN_POINT('Ctrl Pts',(-30.9548805763844,-0.903933369062518,
309.772544675173));
#16930=CARTESIAN_POINT('Ctrl Pts',(-30.9849813935838,-0.992378207993662,
309.767509666312));
#16931=CARTESIAN_POINT('Ctrl Pts',(-31.0191920791562,-1.07914368867578,
309.76247465745));
#16932=CARTESIAN_POINT('Ctrl Pts',(-31.053440355446,-1.16600450730914,309.757434116118));
#16933=CARTESIAN_POINT('Ctrl Pts',(-31.0918073512228,-1.25118187036631,
309.752393574786));
#16934=CARTESIAN_POINT('Ctrl Pts',(-31.1340884258291,-1.33427043102484,
309.747353033455));
#16935=CARTESIAN_POINT('Ctrl Pts',(-31.1763954772765,-1.41741004001541,
309.742309395292));
#16936=CARTESIAN_POINT('Ctrl Pts',(-31.2226211750026,-1.49845790613682,
309.737265757129));
#16937=CARTESIAN_POINT('Ctrl Pts',(-31.2725162662144,-1.57703569952134,
309.732222118966));
#16938=CARTESIAN_POINT('Ctrl Pts',(-31.3224921485133,-1.6557407275737,309.727170314048));
#16939=CARTESIAN_POINT('Ctrl Pts',(-31.3761490304801,-1.73196733537553,
309.72211850913));
#16940=CARTESIAN_POINT('Ctrl Pts',(-31.4331960576555,-1.80536858279825,
309.717066704211));
#16941=CARTESIAN_POINT('Ctrl Pts',(-31.4620729685833,-1.84252391566604,
309.714509506617));
#16942=CARTESIAN_POINT('Ctrl Pts',(-31.4918179327893,-1.87895585727067,
309.711952309023));
#16943=CARTESIAN_POINT('Ctrl Pts',(-31.5223896698333,-1.91462305088546,
309.709395111429));
#16944=CARTESIAN_POINT('Ctrl Pts',(-31.5827905096962,-1.98509102746098,
309.704342834479));
#16945=CARTESIAN_POINT('Ctrl Pts',(-31.6466376295842,-2.0528244808105,309.699290557529));
#16946=CARTESIAN_POINT('Ctrl Pts',(-31.7136538692465,-2.11746721508837,
309.694238280579));
#16947=CARTESIAN_POINT('Ctrl Pts',(-31.780577681099,-2.18202079506008,309.689192971655));
#16948=CARTESIAN_POINT('Ctrl Pts',(-31.8506616104126,-2.24349182068772,
309.684147662731));
#16949=CARTESIAN_POINT('Ctrl Pts',(-31.9235887170129,-2.30155759189633,
309.679102353807));
#16950=CARTESIAN_POINT('Ctrl Pts',(-31.9964377769405,-2.35956122105036,
309.674062444378));
#16951=CARTESIAN_POINT('Ctrl Pts',(-32.0721236205085,-2.4141665641599,309.669022534949));
#16952=CARTESIAN_POINT('Ctrl Pts',(-32.1502937904264,-2.46508896835621,
309.663982625521));
#16953=CARTESIAN_POINT('Ctrl Pts',(-32.2284076126545,-2.51597466596951,
309.658946349028));
#16954=CARTESIAN_POINT('Ctrl Pts',(-32.3090018306251,-2.56318245963682,
309.653910072536));
#16955=CARTESIAN_POINT('Ctrl Pts',(-32.3916932091461,-2.60646971236028,
309.648873796044));
#16956=CARTESIAN_POINT('Ctrl Pts',(-32.4743545189634,-2.64974122472964,
309.643839350871));
#16957=CARTESIAN_POINT('Ctrl Pts',(-32.5591110811894,-2.68909482245053,
309.638804905698));
#16958=CARTESIAN_POINT('Ctrl Pts',(-32.6455540536062,-2.72433325322679,
309.633770460524));
#16959=CARTESIAN_POINT('Ctrl Pts',(-32.7319897752024,-2.75956872821,309.62873643764));
#16960=CARTESIAN_POINT('Ctrl Pts',(-32.8201112142855,-2.79068955501337,
309.623702414755));
#16961=CARTESIAN_POINT('Ctrl Pts',(-32.9094895588942,-2.81754662792824,
309.61866839187));
#16962=CARTESIAN_POINT('Ctrl Pts',(-32.9988854093746,-2.84440896113825,
309.613633383009));
#16963=CARTESIAN_POINT('Ctrl Pts',(-33.0895382287521,-2.8670057544445,309.608598374147));
#16964=CARTESIAN_POINT('Ctrl Pts',(-33.1810051707611,-2.88523809285828,
309.603563365286));
#16965=CARTESIAN_POINT('Ctrl Pts',(-33.272572616689,-2.9034904649741,309.598522823954));
#16966=CARTESIAN_POINT('Ctrl Pts',(-33.3649555345335,-2.91736872250081,
309.593482282623));
#16967=CARTESIAN_POINT('Ctrl Pts',(-33.4577023410775,-2.92682536340521,
309.588441741291));
#16968=CARTESIAN_POINT('Ctrl Pts',(-33.5505061298309,-2.93628781432411,
309.583398103129));
#16969=CARTESIAN_POINT('Ctrl Pts',(-33.6436738090824,-2.94132321649817,
309.578354464966));
#16970=CARTESIAN_POINT('Ctrl Pts',(-33.7367523457436,-2.94193620287622,
309.573310826804));
#16971=CARTESIAN_POINT('Ctrl Pts',(-33.8299815969541,-2.94255018181355,
309.568259021886));
#16972=CARTESIAN_POINT('Ctrl Pts',(-33.9231209740874,-2.9387274673719,309.563207216968));
#16973=CARTESIAN_POINT('Ctrl Pts',(-34.0157213005729,-2.93052466500855,
309.55815541205));
#16974=CARTESIAN_POINT('Ctrl Pts',(-34.0625951082925,-2.92637244875475,
309.555598214453));
#16975=CARTESIAN_POINT('Ctrl Pts',(-34.1093309311938,-2.9210987283285,309.553041016856));
#16976=CARTESIAN_POINT('Ctrl Pts',(-34.1558716459712,-2.914715807452,309.550483819259));
#16977=CARTESIAN_POINT('Ctrl Pts',(-34.2478225303235,-2.90210501661753,
309.545431542309));
#16978=CARTESIAN_POINT('Ctrl Pts',(-34.33934112768,-2.88511614501201,309.540379265359));
#16979=CARTESIAN_POINT('Ctrl Pts',(-34.4299778973623,-2.86378927335161,
309.535326988409));
#16980=CARTESIAN_POINT('Ctrl Pts',(-34.5204896621479,-2.84249181539825,
309.530281679485));
#16981=CARTESIAN_POINT('Ctrl Pts',(-34.6101215873175,-2.81686834705408,
309.525236370561));
#16982=CARTESIAN_POINT('Ctrl Pts',(-34.6984307457689,-2.78701053071398,
309.520191061637));
#16983=CARTESIAN_POINT('Ctrl Pts',(-34.7866453956583,-2.75718466824293,
309.515151152209));
#16984=CARTESIAN_POINT('Ctrl Pts',(-34.8735396740097,-2.72313360655017,
309.51011124278));
#16985=CARTESIAN_POINT('Ctrl Pts',(-34.9586834021217,-2.68499947122222,
309.505071333352));
#16986=CARTESIAN_POINT('Ctrl Pts',(-35.0437657557684,-2.64689282426267,
309.500035056859));
#16987=CARTESIAN_POINT('Ctrl Pts',(-35.1270996630077,-2.60470913479231,
309.494998780367));
#16988=CARTESIAN_POINT('Ctrl Pts',(-35.2082735964798,-2.55863915699102,
309.489962503875));
#16989=CARTESIAN_POINT('Ctrl Pts',(-35.28941801303,-2.51258593141394,309.484928058702));
#16990=CARTESIAN_POINT('Ctrl Pts',(-35.3684036301592,-2.46264944394667,
309.479893613529));
#16991=CARTESIAN_POINT('Ctrl Pts',(-35.444843204326,-2.4090665550276,309.474859168356));
#16992=CARTESIAN_POINT('Ctrl Pts',(-35.5212763667557,-2.35548816063126,
309.469825145471));
#16993=CARTESIAN_POINT('Ctrl Pts',(-35.5951635471574,-2.29826422805756,
309.464791122586));
#16994=CARTESIAN_POINT('Ctrl Pts',(-35.6661471606637,-2.23767448087141,
309.459757099701));
#16995=CARTESIAN_POINT('Ctrl Pts',(-35.7371446772024,-2.1770728664222,309.45472209084));
#16996=CARTESIAN_POINT('Ctrl Pts',(-35.8052371597658,-2.1131044168001,309.449687081979));
#16997=CARTESIAN_POINT('Ctrl Pts',(-35.870101615119,-2.04608783619383,309.444652073117));
#16998=CARTESIAN_POINT('Ctrl Pts',(-35.9350373435661,-1.97899761773734,
309.439611531786));
#16999=CARTESIAN_POINT('Ctrl Pts',(-35.9967376552072,-1.90885290243591,
309.434570990454));
#17000=CARTESIAN_POINT('Ctrl Pts',(-36.0549180448958,-1.83600758387068,
309.429530449123));
#17001=CARTESIAN_POINT('Ctrl Pts',(-36.1131341797196,-1.76311751026394,
309.42448681096));
#17002=CARTESIAN_POINT('Ctrl Pts',(-36.1678258270901,-1.6875238898987,309.419443172798));
#17003=CARTESIAN_POINT('Ctrl Pts',(-36.2187515235251,-1.60961007095911,
309.414399534635));
#17004=CARTESIAN_POINT('Ctrl Pts',(-36.2697596798232,-1.53157009247136,
309.409347729718));
#17005=CARTESIAN_POINT('Ctrl Pts',(-36.3169894866719,-1.45120279773392,
309.4042959248));
#17006=CARTESIAN_POINT('Ctrl Pts',(-36.3602452595575,-1.36891644076131,
309.399244119882));
#17007=CARTESIAN_POINT('Ctrl Pts',(-36.382141108722,-1.32726351121299,309.396686922284));
#17008=CARTESIAN_POINT('Ctrl Pts',(-36.4030194422427,-1.28511918230115,
309.394129724687));
#17009=CARTESIAN_POINT('Ctrl Pts',(-36.4228596657514,-1.24253813789557,
309.39157252709));
#17010=CARTESIAN_POINT('Ctrl Pts',(-36.4654479700165,-1.15113521220403,
309.386083339466));
#17011=CARTESIAN_POINT('Ctrl Pts',(-36.5033835448867,-1.05743256682659,
309.380594151842));
#17012=CARTESIAN_POINT('Ctrl Pts',(-36.5364336150382,-0.961903980042877,
309.375104964218));
#17013=CARTESIAN_POINT('Ctrl Pts',(-36.5693605733763,-0.866731238118326,
309.369636223868));
#17014=CARTESIAN_POINT('Ctrl Pts',(-36.5974381969507,-0.76974641445008,
309.364167483518));
#17015=CARTESIAN_POINT('Ctrl Pts',(-36.6204819709492,-0.671442287238291,
309.358698743169));
#17016=CARTESIAN_POINT('Ctrl Pts',(-36.6434698437343,-0.573376633116905,
309.353243269275));
#17017=CARTESIAN_POINT('Ctrl Pts',(-36.6614481150749,-0.473998359607168,
309.347787795382));
#17018=CARTESIAN_POINT('Ctrl Pts',(-36.6742814338892,-0.373816595918416,
309.342332321488));
#17019=CARTESIAN_POINT('Ctrl Pts',(-36.6870702578002,-0.273982176353674,
309.336895762483));
#17020=CARTESIAN_POINT('Ctrl Pts',(-36.6947496328921,-0.173350134536088,
309.331459203477));
#17021=CARTESIAN_POINT('Ctrl Pts',(-36.6972350637744,-0.0724396698782973,
309.326022644471));
#17022=CARTESIAN_POINT('Ctrl Pts',(-36.6978212358865,-0.0486406173166869,
309.324740468693));
#17023=CARTESIAN_POINT('Ctrl Pts',(-36.6981187313625,-0.0248261341478378,
309.323458292915));
#17024=CARTESIAN_POINT('Ctrl Pts',(-36.6981268542406,-0.00100312718012004,
309.322176117137));
#17025=CARTESIAN_POINT('',(-36.6981258228997,0.00265982559600335,308.322176117063));
#17026=CARTESIAN_POINT('Ctrl Pts',(-36.6981268542409,-0.00100312630173672,
309.32217611709));
#17027=CARTESIAN_POINT('Ctrl Pts',(-36.6981595100368,0.094770801544592,
309.317021477685));
#17028=CARTESIAN_POINT('Ctrl Pts',(-36.6935110801844,0.190508962578298,
309.311866838281));
#17029=CARTESIAN_POINT('Ctrl Pts',(-36.6842182670738,0.28573708124698,309.306712198876));
#17030=CARTESIAN_POINT('Ctrl Pts',(-36.6749193130744,0.381028128683565,
309.301554153176));
#17031=CARTESIAN_POINT('Ctrl Pts',(-36.6609699063463,0.475808051227989,
309.296396107476));
#17032=CARTESIAN_POINT('Ctrl Pts',(-36.6424583567241,0.569609905983874,
309.291238061776));
#17033=CARTESIAN_POINT('Ctrl Pts',(-36.623914852552,0.663573681060037,309.286071112282));
#17034=CARTESIAN_POINT('Ctrl Pts',(-36.6007935554482,0.756555609160315,
309.280904162788));
#17035=CARTESIAN_POINT('Ctrl Pts',(-36.5732335547574,0.848100702422635,
309.275737213293));
#17036=CARTESIAN_POINT('Ctrl Pts',(-36.54564865705,0.939728495236683,309.270565596106));
#17037=CARTESIAN_POINT('Ctrl Pts',(-36.5136172032491,1.02991647685934,309.265393978919));
#17038=CARTESIAN_POINT('Ctrl Pts',(-36.4773268787502,1.11822866952695,309.260222361731));
#17039=CARTESIAN_POINT('Ctrl Pts',(-36.4409596088543,1.20672810815648,309.255039779303));
#17040=CARTESIAN_POINT('Ctrl Pts',(-36.4003155984257,1.29334343468067,309.249857196875));
#17041=CARTESIAN_POINT('Ctrl Pts',(-36.355629286909,1.37766178420867,309.244674614448));
#17042=CARTESIAN_POINT('Ctrl Pts',(-36.3211012224824,1.44281259451377,309.240670154605));
#17043=CARTESIAN_POINT('Ctrl Pts',(-36.2841607426211,1.50659252353378,309.236665694763));
#17044=CARTESIAN_POINT('Ctrl Pts',(-36.2449332443537,1.5688236369295,309.232661234921));
#17045=CARTESIAN_POINT('Ctrl Pts',(-36.1954413795066,1.64733830111892,309.227608957971));
#17046=CARTESIAN_POINT('Ctrl Pts',(-36.1421416678632,1.72364961194115,309.222556681021));
#17047=CARTESIAN_POINT('Ctrl Pts',(-36.0852564281067,1.79736480014044,309.217504404071));
#17048=CARTESIAN_POINT('Ctrl Pts',(-36.0284496436342,1.87097832143883,309.212459095147));
#17049=CARTESIAN_POINT('Ctrl Pts',(-35.9680674266596,1.94200248643215,309.207413786223));
#17050=CARTESIAN_POINT('Ctrl Pts',(-35.9043763306642,2.0100718698146,309.202368477299));
#17051=CARTESIAN_POINT('Ctrl Pts',(-35.8407533969525,2.07806840526525,309.19732856787));
#17052=CARTESIAN_POINT('Ctrl Pts',(-35.7738289247213,2.14311612182233,309.192288658442));
#17053=CARTESIAN_POINT('Ctrl Pts',(-35.7039101478962,2.20488206196257,309.187248749013));
#17054=CARTESIAN_POINT('Ctrl Pts',(-35.6340417708788,2.26660347913421,309.182212472521));
#17055=CARTESIAN_POINT('Ctrl Pts',(-35.5611837113706,2.32504752860001,309.177176196028));
#17056=CARTESIAN_POINT('Ctrl Pts',(-35.4856797731719,2.3799183372927,309.172139919536));
#17057=CARTESIAN_POINT('Ctrl Pts',(-35.4102032901396,2.43476919355355,309.167105474363));
#17058=CARTESIAN_POINT('Ctrl Pts',(-35.3320831987663,2.4860491293745,309.16207102919));
#17059=CARTESIAN_POINT('Ctrl Pts',(-35.2516952477261,2.53350344225983,309.157036584017));
#17060=CARTESIAN_POINT('Ctrl Pts',(-35.1713140396124,2.58095377468617,309.152002561132));
#17061=CARTESIAN_POINT('Ctrl Pts',(-35.0886657327134,2.62457889650561,309.146968538247));
#17062=CARTESIAN_POINT('Ctrl Pts',(-35.0041528457329,2.66416882937757,309.141934515362));
#17063=CARTESIAN_POINT('Ctrl Pts',(-34.9196234058418,2.70376651643519,309.136899506501));
#17064=CARTESIAN_POINT('Ctrl Pts',(-34.8332290630134,2.73932725681085,309.131864497639));
#17065=CARTESIAN_POINT('Ctrl Pts',(-34.7453935316089,2.7706886832359,309.126829488778));
#17066=CARTESIAN_POINT('Ctrl Pts',(-34.6574614864811,2.80208456961111,309.121788947446));
#17067=CARTESIAN_POINT('Ctrl Pts',(-34.5680855108015,2.82927178191396,309.116748406114));
#17068=CARTESIAN_POINT('Ctrl Pts',(-34.4777054517754,2.85213754478709,309.111707864783));
#17069=CARTESIAN_POINT('Ctrl Pts',(-34.3872698646333,2.87501735603268,309.10666422662));
#17070=CARTESIAN_POINT('Ctrl Pts',(-34.2958294010936,2.89357034392742,309.101620588458));
#17071=CARTESIAN_POINT('Ctrl Pts',(-34.2038329370239,2.90773510082495,309.096576950295));
#17072=CARTESIAN_POINT('Ctrl Pts',(-34.1116875105174,2.92192279356818,309.091525145377));
#17073=CARTESIAN_POINT('Ctrl Pts',(-34.0189847274179,2.93170802346463,309.086473340459));
#17074=CARTESIAN_POINT('Ctrl Pts',(-33.9261772187974,2.93708136279489,309.081421535541));
#17075=CARTESIAN_POINT('Ctrl Pts',(-33.879198536551,2.93980131945303,309.078864337944));
#17076=CARTESIAN_POINT('Ctrl Pts',(-33.8321930031777,2.94139163438225,309.076307140348));
#17077=CARTESIAN_POINT('Ctrl Pts',(-33.7852189249271,2.94185615919161,309.073749942751));
#17078=CARTESIAN_POINT('Ctrl Pts',(-33.6924118406872,2.9427739247917,309.068697665801));
#17079=CARTESIAN_POINT('Ctrl Pts',(-33.5993946983949,2.93929733732224,309.063645388851));
#17080=CARTESIAN_POINT('Ctrl Pts',(-33.5066180822657,2.93140056753885,309.058593111901));
#17081=CARTESIAN_POINT('Ctrl Pts',(-33.4139694222777,2.92351468886392,309.053547802977));
#17082=CARTESIAN_POINT('Ctrl Pts',(-33.3215610680768,2.91122077924754,309.048502494053));
#17083=CARTESIAN_POINT('Ctrl Pts',(-33.2298445745017,2.89454500431871,309.043457185129));
#17084=CARTESIAN_POINT('Ctrl Pts',(-33.138226236023,2.87788707582326,309.0384172757));
#17085=CARTESIAN_POINT('Ctrl Pts',(-33.0472987211957,2.8568566821027,309.033377366272));
#17086=CARTESIAN_POINT('Ctrl Pts',(-32.9575083231665,2.83153177073301,309.028337456843));
#17087=CARTESIAN_POINT('Ctrl Pts',(-32.8677826490785,2.80622511441183,309.023301180351));
#17088=CARTESIAN_POINT('Ctrl Pts',(-32.7791928889215,2.77663021369273,309.018264903859));
#17089=CARTESIAN_POINT('Ctrl Pts',(-32.6921739669336,2.74287584292164,309.013228627366));
#17090=CARTESIAN_POINT('Ctrl Pts',(-32.6051866872551,2.70913374610451,309.008194182193));
#17091=CARTESIAN_POINT('Ctrl Pts',(-32.5197695247725,2.67123534445736,309.00315973702));
#17092=CARTESIAN_POINT('Ctrl Pts',(-32.4363400949979,2.62935856412087,308.998125291847));
#17093=CARTESIAN_POINT('Ctrl Pts',(-32.3529176632685,2.58748529640099,308.993091268962));
#17094=CARTESIAN_POINT('Ctrl Pts',(-32.2714830297116,2.54163451293453,308.988057246077));
#17095=CARTESIAN_POINT('Ctrl Pts',(-32.1924307111754,2.49203086604598,308.983023223193));
#17096=CARTESIAN_POINT('Ctrl Pts',(-32.1133629092499,2.44241750366028,308.977988214331));
#17097=CARTESIAN_POINT('Ctrl Pts',(-32.0366787251165,2.3890500544749,308.97295320547));
#17098=CARTESIAN_POINT('Ctrl Pts',(-31.96274413107,2.33219677446722,308.967918196608));
#17099=CARTESIAN_POINT('Ctrl Pts',(-31.8887282976564,2.27528102404845,308.962877655277));
#17100=CARTESIAN_POINT('Ctrl Pts',(-31.8174684378227,2.21487206843789,308.957837113945));
#17101=CARTESIAN_POINT('Ctrl Pts',(-31.7492975721632,2.1512785840502,308.952796572614));
#17102=CARTESIAN_POINT('Ctrl Pts',(-31.681084823374,2.08764602880528,308.947752934452));
#17103=CARTESIAN_POINT('Ctrl Pts',(-31.6159651567989,2.02082536764919,308.942709296289));
#17104=CARTESIAN_POINT('Ctrl Pts',(-31.5542333009654,1.95116068710975,308.937665658127));
#17105=CARTESIAN_POINT('Ctrl Pts',(-31.4924014877286,1.88138320418524,308.932613853209));
#17106=CARTESIAN_POINT('Ctrl Pts',(-31.4339687147059,1.80875285408697,308.927562048291));
#17107=CARTESIAN_POINT('Ctrl Pts',(-31.379188047652,1.73364503193103,308.922510243373));
#17108=CARTESIAN_POINT('Ctrl Pts',(-31.3514583564981,1.69562583969344,308.919953045776));
#17109=CARTESIAN_POINT('Ctrl Pts',(-31.3246637482859,1.65697227271581,308.917395848179));
#17110=CARTESIAN_POINT('Ctrl Pts',(-31.2988325632628,1.61773543172227,308.914838650582));
#17111=CARTESIAN_POINT('Ctrl Pts',(-31.2477976722396,1.54021487266135,308.909786373632));
#17112=CARTESIAN_POINT('Ctrl Pts',(-31.2003430973805,1.46013779263423,308.904734096682));
#17113=CARTESIAN_POINT('Ctrl Pts',(-31.1567345837079,1.37786898318173,308.899681819732));
#17114=CARTESIAN_POINT('Ctrl Pts',(-31.1131862142546,1.29571363765866,308.894636510808));
#17115=CARTESIAN_POINT('Ctrl Pts',(-31.0734735716699,1.21137295851321,308.889591201884));
#17116=CARTESIAN_POINT('Ctrl Pts',(-31.0378192175375,1.12524071313107,308.88454589296));
#17117=CARTESIAN_POINT('Ctrl Pts',(-31.0022030207353,1.03920064657573,308.879505983532));
#17118=CARTESIAN_POINT('Ctrl Pts',(-30.9706366486545,0.951373233050796,
308.874466074103));
#17119=CARTESIAN_POINT('Ctrl Pts',(-30.9432962830758,0.862175861316719,
308.869426164674));
#17120=CARTESIAN_POINT('Ctrl Pts',(-30.9159756253531,0.773042786050787,
308.864389888182));
#17121=CARTESIAN_POINT('Ctrl Pts',(-30.8928750491081,0.682542138923517,
308.85935361169));
#17122=CARTESIAN_POINT('Ctrl Pts',(-30.8741218516755,0.591109278768155,
308.854317335197));
#17123=CARTESIAN_POINT('Ctrl Pts',(-30.8553754733859,0.499709665943331,
308.849282890024));
#17124=CARTESIAN_POINT('Ctrl Pts',(-30.8409734226155,0.407378948261623,
308.844248444851));
#17125=CARTESIAN_POINT('Ctrl Pts',(-30.8309923033632,0.314564554214339,
308.839213999678));
#17126=CARTESIAN_POINT('Ctrl Pts',(-30.8210120213254,0.221757945421204,
308.834179976793));
#17127=CARTESIAN_POINT('Ctrl Pts',(-30.815451980834,0.128468182655901,308.829145953908));
#17128=CARTESIAN_POINT('Ctrl Pts',(-30.8143369958528,0.035148583111494,
308.824111931023));
#17129=CARTESIAN_POINT('Ctrl Pts',(-30.8132217924879,-0.0581892942482417,
308.819076922162));
#17130=CARTESIAN_POINT('Ctrl Pts',(-30.8165533786246,-0.151556575790484,
308.814041913301));
#17131=CARTESIAN_POINT('Ctrl Pts',(-30.8243044536866,-0.244500324799556,
308.809006904439));
#17132=CARTESIAN_POINT('Ctrl Pts',(-30.8320640456337,-0.337546200444327,
308.803966363108));
#17133=CARTESIAN_POINT('Ctrl Pts',(-30.8442527829522,-0.430167171201971,
308.798925821776));
#17134=CARTESIAN_POINT('Ctrl Pts',(-30.8607915396068,-0.521916109668268,
308.793885280444));
#17135=CARTESIAN_POINT('Ctrl Pts',(-30.8773404574187,-0.613721417268895,
308.788841642282));
#17136=CARTESIAN_POINT('Ctrl Pts',(-30.8982446156997,-0.70465319333625,
308.783798004119));
#17137=CARTESIAN_POINT('Ctrl Pts',(-30.9233743825601,-0.794277322658978,
308.778754365957));
#17138=CARTESIAN_POINT('Ctrl Pts',(-30.9485448400204,-0.884046573088771,
308.773702561039));
#17139=CARTESIAN_POINT('Ctrl Pts',(-30.9779544256604,-0.972503528671947,
308.768650756121));
#17140=CARTESIAN_POINT('Ctrl Pts',(-31.0114246241131,-1.05923214129474,
308.763598951203));
#17141=CARTESIAN_POINT('Ctrl Pts',(-31.0283670659601,-1.1031337177347,308.761041753606));
#17142=CARTESIAN_POINT('Ctrl Pts',(-31.0463492218567,-1.14659279432876,
308.758484556009));
#17143=CARTESIAN_POINT('Ctrl Pts',(-31.0653434831359,-1.18955787141558,
308.755927358413));
#17144=CARTESIAN_POINT('Ctrl Pts',(-31.1028706060156,-1.27444433810585,
308.750875081463));
#17145=CARTESIAN_POINT('Ctrl Pts',(-31.1444859129757,-1.35770562351071,
308.745822804513));
#17146=CARTESIAN_POINT('Ctrl Pts',(-31.190026669432,-1.43892076356962,308.740770527563));
#17147=CARTESIAN_POINT('Ctrl Pts',(-31.2355046167484,-1.52002389290471,
308.735725218639));
#17148=CARTESIAN_POINT('Ctrl Pts',(-31.2848970400129,-1.59908610046196,
308.730679909715));
#17149=CARTESIAN_POINT('Ctrl Pts',(-31.3379934585911,-1.67570703100534,
308.725634600791));
#17150=CARTESIAN_POINT('Ctrl Pts',(-31.3910330533219,-1.75224596174191,
308.720594691362));
#17151=CARTESIAN_POINT('Ctrl Pts',(-31.4477685125986,-1.82634844532714,
308.715554781933));
#17152=CARTESIAN_POINT('Ctrl Pts',(-31.507944379815,-1.89764032227676,308.710514872505));
#17153=CARTESIAN_POINT('Ctrl Pts',(-31.5680768702405,-1.9688808096414,308.705478596012));
#17154=CARTESIAN_POINT('Ctrl Pts',(-31.6316445536061,-2.03731437877803,
308.70044231952));
#17155=CARTESIAN_POINT('Ctrl Pts',(-31.698350391571,-2.10259823215311,308.695406043028));
#17156=CARTESIAN_POINT('Ctrl Pts',(-31.7650319735841,-2.16785834664651,
308.690371597855));
#17157=CARTESIAN_POINT('Ctrl Pts',(-31.8348491260709,-2.2299707102517,308.685337152681));
#17158=CARTESIAN_POINT('Ctrl Pts',(-31.9074672094207,-2.28862860362045,
308.680302707508));
#17159=CARTESIAN_POINT('Ctrl Pts',(-31.9800792015791,-2.34728157677604,
308.675268684623));
#17160=CARTESIAN_POINT('Ctrl Pts',(-32.0554913117727,-2.40248037679197,
308.670234661739));
#17161=CARTESIAN_POINT('Ctrl Pts',(-32.133335901137,-2.45395863198124,308.665200638854));
#17162=CARTESIAN_POINT('Ctrl Pts',(-32.2111957373415,-2.50544696983323,
308.660165629992));
#17163=CARTESIAN_POINT('Ctrl Pts',(-32.2914886281697,-2.5532130709011,308.655130621131));
#17164=CARTESIAN_POINT('Ctrl Pts',(-32.3738190298947,-2.59703457927613,
308.65009561227));
#17165=CARTESIAN_POINT('Ctrl Pts',(-32.4562398963043,-2.64090423874534,
308.645055070938));
#17166=CARTESIAN_POINT('Ctrl Pts',(-32.5407023497848,-2.6808204446462,308.640014529606));
#17167=CARTESIAN_POINT('Ctrl Pts',(-32.6267876620212,-2.7166075540359,308.634973988275));
#17168=CARTESIAN_POINT('Ctrl Pts',(-32.7129258637477,-2.7524166504744,308.629930350112));
#17169=CARTESIAN_POINT('Ctrl Pts',(-32.800688491616,-2.78409144931917,308.62488671195));
#17170=CARTESIAN_POINT('Ctrl Pts',(-32.8896404024585,-2.81150581228461,
308.619843073787));
#17171=CARTESIAN_POINT('Ctrl Pts',(-32.9787363459386,-2.83896456511163,
308.614791268869));
#17172=CARTESIAN_POINT('Ctrl Pts',(-33.0690249870781,-2.86214899953888,
308.609739463951));
#17173=CARTESIAN_POINT('Ctrl Pts',(-33.1600598958886,-2.8809838557836,308.604687659033));
#17174=CARTESIAN_POINT('Ctrl Pts',(-33.2061412972523,-2.89051796288145,
308.602130461437));
#17175=CARTESIAN_POINT('Ctrl Pts',(-33.2524138128963,-2.89893838835933,
308.59957326384));
#17176=CARTESIAN_POINT('Ctrl Pts',(-33.2988191974236,-2.9062404495502,308.597016066243));
#17177=CARTESIAN_POINT('Ctrl Pts',(-33.3905027086586,-2.92066719368886,
308.591963789293));
#17178=CARTESIAN_POINT('Ctrl Pts',(-33.4830341420085,-2.93077705337546,
308.586911512343));
#17179=CARTESIAN_POINT('Ctrl Pts',(-33.5759714816422,-2.93647884039791,
308.581859235393));
#17180=CARTESIAN_POINT('Ctrl Pts',(-33.668780643467,-2.94217276359974,308.576813926469));
#17181=CARTESIAN_POINT('Ctrl Pts',(-33.7619941595681,-2.9434706680037,308.571768617545));
#17182=CARTESIAN_POINT('Ctrl Pts',(-33.8551614799973,-2.94033266430423,
308.566723308621));
#17183=CARTESIAN_POINT('Ctrl Pts',(-33.9482290926541,-2.93719801889989,
308.561683399192));
#17184=CARTESIAN_POINT('Ctrl Pts',(-34.0412501662869,-2.9296369162686,308.556643489764));
#17185=CARTESIAN_POINT('Ctrl Pts',(-34.1337718136874,-2.91766146318791,
308.551603580335));
#17186=CARTESIAN_POINT('Ctrl Pts',(-34.2262267683699,-2.90569464241692,
308.546567303843));
#17187=CARTESIAN_POINT('Ctrl Pts',(-34.3181825730628,-2.88931985275281,
308.541531027351));
#17188=CARTESIAN_POINT('Ctrl Pts',(-34.4091901845105,-2.86860114167632,
308.536494750858));
#17189=CARTESIAN_POINT('Ctrl Pts',(-34.5001647032592,-2.84788996445394,
308.531460305685));
#17190=CARTESIAN_POINT('Ctrl Pts',(-34.5901912809832,-2.82283810230144,
308.526425860512));
#17191=CARTESIAN_POINT('Ctrl Pts',(-34.6788308388284,-2.79356075151802,
308.521391415339));
#17192=CARTESIAN_POINT('Ctrl Pts',(-34.7674629616039,-2.76428585651336,
308.516357392454));
#17193=CARTESIAN_POINT('Ctrl Pts',(-34.8547078740335,-2.7307863170804,308.511323369569));
#17194=CARTESIAN_POINT('Ctrl Pts',(-34.9401425431737,-2.69322692199041,
308.506289346685));
#17195=CARTESIAN_POINT('Ctrl Pts',(-35.0255939457665,-2.6556601704213,308.501254337823));
#17196=CARTESIAN_POINT('Ctrl Pts',(-35.1092339943976,-2.61403216309768,
308.496219328962));
#17197=CARTESIAN_POINT('Ctrl Pts',(-35.1906615446817,-2.56855498531383,
308.4911843201));
#17198=CARTESIAN_POINT('Ctrl Pts',(-35.2721785675969,-2.52302783718539,
308.486143778769));
#17199=CARTESIAN_POINT('Ctrl Pts',(-35.351477850948,-2.4736432930296,308.481103237437));
#17200=CARTESIAN_POINT('Ctrl Pts',(-35.4281849627321,-2.42065822736884,
308.476062696106));
#17201=CARTESIAN_POINT('Ctrl Pts',(-35.5049392021843,-2.36764060849984,
308.471019057943));
#17202=CARTESIAN_POINT('Ctrl Pts',(-35.5790977466969,-2.3110183336604,308.465975419781));
#17203=CARTESIAN_POINT('Ctrl Pts',(-35.6503188898848,-2.25108888762307,
308.460931781618));
#17204=CARTESIAN_POINT('Ctrl Pts',(-35.7216553557119,-2.19106240267892,
308.4558799767));
#17205=CARTESIAN_POINT('Ctrl Pts',(-35.7900445993316,-2.12771835737363,
308.450828171782));
#17206=CARTESIAN_POINT('Ctrl Pts',(-35.8551815721807,-2.061391279947,308.445776366864));
#17207=CARTESIAN_POINT('Ctrl Pts',(-35.8881535719188,-2.02781685540921,
308.443219169268));
#17208=CARTESIAN_POINT('Ctrl Pts',(-35.9202928687287,-1.99347861331989,
308.440661971671));
#17209=CARTESIAN_POINT('Ctrl Pts',(-35.9515639810421,-1.95842298117019,
308.438104774074));
#17210=CARTESIAN_POINT('Ctrl Pts',(-36.0127391832395,-1.88984418028136,
308.433102167244));
#17211=CARTESIAN_POINT('Ctrl Pts',(-36.0708188799458,-1.81826049345026,
308.428099560414));
#17212=CARTESIAN_POINT('Ctrl Pts',(-36.1254893538265,-1.74398570979198,
308.423096953584));
#17213=CARTESIAN_POINT('Ctrl Pts',(-36.1800900864435,-1.66980567594839,
308.418100728409));
#17214=CARTESIAN_POINT('Ctrl Pts',(-36.231289962854,-1.59294172082055,308.413104503234));
#17215=CARTESIAN_POINT('Ctrl Pts',(-36.2788132813222,-1.51374306058289,
308.408108278059));
#17216=CARTESIAN_POINT('Ctrl Pts',(-36.3262899036055,-1.43462222056899,
308.403116962152));
#17217=CARTESIAN_POINT('Ctrl Pts',(-36.3700969090617,-1.35317161692577,
308.398125646244));
#17218=CARTESIAN_POINT('Ctrl Pts',(-36.4100007259876,-1.26977099532699,
308.393134330336));
#17219=CARTESIAN_POINT('Ctrl Pts',(-36.4498770232938,-1.18642789086733,
308.388146456683));
#17220=CARTESIAN_POINT('Ctrl Pts',(-36.485855284119,-1.10113784771177,308.38315858303));
#17221=CARTESIAN_POINT('Ctrl Pts',(-36.517747532237,-1.01430576032625,308.378170709378));
#17222=CARTESIAN_POINT('Ctrl Pts',(-36.5496347291478,-0.927487425714,308.373183625722));
#17223=CARTESIAN_POINT('Ctrl Pts',(-36.5774370308001,-0.839127953048225,
308.368196542066));
#17224=CARTESIAN_POINT('Ctrl Pts',(-36.6010147219531,-0.749651914684957,
308.36320945841));
#17225=CARTESIAN_POINT('Ctrl Pts',(-36.6245894474414,-0.66018713085516,
308.358223002043));
#17226=CARTESIAN_POINT('Ctrl Pts',(-36.6439405088105,-0.569606500767948,
308.353236545676));
#17227=CARTESIAN_POINT('Ctrl Pts',(-36.6589786081074,-0.478347873358279,
308.348250089309));
#17228=CARTESIAN_POINT('Ctrl Pts',(-36.6740264570508,-0.38703008026958,
308.343260400074));
#17229=CARTESIAN_POINT('Ctrl Pts',(-36.6847556896895,-0.295033860820404,
308.33827071084));
#17230=CARTESIAN_POINT('Ctrl Pts',(-36.691128602081,-0.202804694334924,
308.333281021605));
#17231=CARTESIAN_POINT('Ctrl Pts',(-36.6958563904099,-0.134383860953072,
308.329579386766));
#17232=CARTESIAN_POINT('Ctrl Pts',(-36.6981877482332,-0.0658350003864118,
308.325877751928));
#17233=CARTESIAN_POINT('Ctrl Pts',(-36.6981258229002,0.00265982508757234,
308.32217611709));
#17234=CARTESIAN_POINT('',(-36.6981269972619,-0.000405865267969561,307.322176117036));
#17235=CARTESIAN_POINT('Ctrl Pts',(-36.6981258228997,0.00265982559600865,
308.322176117062));
#17236=CARTESIAN_POINT('Ctrl Pts',(-36.6980207165872,0.118916562715971,
308.31589330686));
#17237=CARTESIAN_POINT('Ctrl Pts',(-36.6910209105583,0.234866416982035,
308.309610496657));
#17238=CARTESIAN_POINT('Ctrl Pts',(-36.6772570076419,0.349805125770544,
308.303327686454));
#17239=CARTESIAN_POINT('Ctrl Pts',(-36.6632385686633,0.46686939781797,308.296928688149));
#17240=CARTESIAN_POINT('Ctrl Pts',(-36.6422035725581,0.582884936325711,
308.290529689843));
#17241=CARTESIAN_POINT('Ctrl Pts',(-36.614338362144,0.69713123132884,308.284130691537));
#17242=CARTESIAN_POINT('Ctrl Pts',(-36.6071718037381,0.72651384619626,308.282484954993));
#17243=CARTESIAN_POINT('Ctrl Pts',(-36.5995537056682,0.755779546793188,
308.280839218449));
#17244=CARTESIAN_POINT('Ctrl Pts',(-36.5914877430168,0.784916301390282,
308.279193481904));
#17245=CARTESIAN_POINT('Ctrl Pts',(-36.5667258956109,0.874363761341445,
308.274141204954));
#17246=CARTESIAN_POINT('Ctrl Pts',(-36.5376827365198,0.962798880669296,
308.269088928004));
#17247=CARTESIAN_POINT('Ctrl Pts',(-36.504457944753,1.04978148056907,308.264036651054));
#17248=CARTESIAN_POINT('Ctrl Pts',(-36.4712789761292,1.1366441153493,308.25899134213));
#17249=CARTESIAN_POINT('Ctrl Pts',(-36.4339299922255,1.22205780008999,308.253946033206));
#17250=CARTESIAN_POINT('Ctrl Pts',(-36.3925609108292,1.30559579005525,308.248900724282));
#17251=CARTESIAN_POINT('Ctrl Pts',(-36.3512361026708,1.38904437756851,308.243860814854));
#17252=CARTESIAN_POINT('Ctrl Pts',(-36.3058999446074,1.47062086428289,308.238820905425));
#17253=CARTESIAN_POINT('Ctrl Pts',(-36.256750666492,1.54991787037237,308.233780995996));
#17254=CARTESIAN_POINT('Ctrl Pts',(-36.2076368168306,1.62915771651067,308.228744719504));
#17255=CARTESIAN_POINT('Ctrl Pts',(-36.1547155437659,1.70612097144661,308.223708443012));
#17256=CARTESIAN_POINT('Ctrl Pts',(-36.0982307837188,1.78042522578225,308.21867216652));
#17257=CARTESIAN_POINT('Ctrl Pts',(-36.0417665629776,1.85470246118737,308.213637721347));
#17258=CARTESIAN_POINT('Ctrl Pts',(-35.9817416980309,1.92632226349075,308.208603276174));
#17259=CARTESIAN_POINT('Ctrl Pts',(-35.9184425808494,1.99493243946904,308.203568831));
#17260=CARTESIAN_POINT('Ctrl Pts',(-35.8551487731861,2.0635368604385,308.198534808116));
#17261=CARTESIAN_POINT('Ctrl Pts',(-35.788581560723,2.12913183060999,308.193500785231));
#17262=CARTESIAN_POINT('Ctrl Pts',(-35.719065859965,2.1914002672259,308.188466762346));
#17263=CARTESIAN_POINT('Ctrl Pts',(-35.6495365436839,2.25368089989717,308.183431753485));
#17264=CARTESIAN_POINT('Ctrl Pts',(-35.5770579233332,2.31263340892541,308.178396744624));
#17265=CARTESIAN_POINT('Ctrl Pts',(-35.5019889342145,2.36798019308723,308.173361735762));
#17266=CARTESIAN_POINT('Ctrl Pts',(-35.426837459255,2.42338779232167,308.168321194431));
#17267=CARTESIAN_POINT('Ctrl Pts',(-35.3490902921085,2.47518149408181,308.163280653099));
#17268=CARTESIAN_POINT('Ctrl Pts',(-35.2691361098323,2.52312653467766,308.158240111768));
#17269=CARTESIAN_POINT('Ctrl Pts',(-35.1891328049381,2.57110103196794,308.153196473606));
#17270=CARTESIAN_POINT('Ctrl Pts',(-35.1069201766292,2.61522195080013,308.148152835443));
#17271=CARTESIAN_POINT('Ctrl Pts',(-35.0229103528424,2.65530111304786,308.143109197281));
#17272=CARTESIAN_POINT('Ctrl Pts',(-34.9387644987399,2.69544517224276,308.138057392363));
#17273=CARTESIAN_POINT('Ctrl Pts',(-34.8528160486947,2.73153423780561,308.133005587445));
#17274=CARTESIAN_POINT('Ctrl Pts',(-34.7654957083083,2.76342882334186,308.127953782527));
#17275=CARTESIAN_POINT('Ctrl Pts',(-34.7212946023161,2.77957369805975,308.12539658493));
#17276=CARTESIAN_POINT('Ctrl Pts',(-34.6767421957652,2.79464460846863,308.122839387332));
#17277=CARTESIAN_POINT('Ctrl Pts',(-34.6318954307013,2.80862843751654,308.120282189735));
#17278=CARTESIAN_POINT('Ctrl Pts',(-34.5432912971566,2.83625640699576,308.115229912785));
#17279=CARTESIAN_POINT('Ctrl Pts',(-34.4532194654202,2.85973704898572,308.110177635835));
#17280=CARTESIAN_POINT('Ctrl Pts',(-34.3621039537994,2.87891576154549,308.105125358886));
#17281=CARTESIAN_POINT('Ctrl Pts',(-34.2711141073492,2.8980680231076,308.100080049962));
#17282=CARTESIAN_POINT('Ctrl Pts',(-34.1790838722977,2.91293005446492,308.095034741038));
#17283=CARTESIAN_POINT('Ctrl Pts',(-34.086453182512,2.92339676230127,308.089989432114));
#17284=CARTESIAN_POINT('Ctrl Pts',(-33.993921626196,2.93385226865497,308.084949522685));
#17285=CARTESIAN_POINT('Ctrl Pts',(-33.9007913315002,2.93992175154603,308.079909613256));
#17286=CARTESIAN_POINT('Ctrl Pts',(-33.8075121186447,2.94155121869017,308.074869703828));
#17287=CARTESIAN_POINT('Ctrl Pts',(-33.7143001445856,2.94317951125954,308.069833427335));
#17288=CARTESIAN_POINT('Ctrl Pts',(-33.6209399086419,2.94037414181107,308.064797150843));
#17289=CARTESIAN_POINT('Ctrl Pts',(-33.5278849940366,2.93313306469108,308.059760874351));
#17290=CARTESIAN_POINT('Ctrl Pts',(-33.4348639165824,2.92589462061226,308.054726429178));
#17291=CARTESIAN_POINT('Ctrl Pts',(-33.3421483823794,2.91422370756339,308.049691984005));
#17292=CARTESIAN_POINT('Ctrl Pts',(-33.2501895671361,2.89817033461967,308.044657538831));
#17293=CARTESIAN_POINT('Ctrl Pts',(-33.1582384653811,2.88211830822991,308.039623515947));
#17294=CARTESIAN_POINT('Ctrl Pts',(-33.0670443939925,2.86168462939915,308.034589493062));
#17295=CARTESIAN_POINT('Ctrl Pts',(-32.9770498778146,2.83697070804971,308.029555470177));
#17296=CARTESIAN_POINT('Ctrl Pts',(-32.8870377350805,2.81225194616841,308.024520461316));
#17297=CARTESIAN_POINT('Ctrl Pts',(-32.7982260424375,2.78325139481809,308.019485452454));
#17298=CARTESIAN_POINT('Ctrl Pts',(-32.7110425590968,2.75012044437866,308.014450443593));
#17299=CARTESIAN_POINT('Ctrl Pts',(-32.6237632785033,2.71695308963519,308.009409902261));
#17300=CARTESIAN_POINT('Ctrl Pts',(-32.5381161943465,2.67964643450673,308.00436936093));
#17301=CARTESIAN_POINT('Ctrl Pts',(-32.4545091626057,2.63840007194239,307.999328819598));
#17302=CARTESIAN_POINT('Ctrl Pts',(-32.3708507639925,2.59712836824825,307.994285181436));
#17303=CARTESIAN_POINT('Ctrl Pts',(-32.2892353013393,2.5519123535183,307.989241543273));
#17304=CARTESIAN_POINT('Ctrl Pts',(-32.2100441695635,2.50299656478565,307.984197905111));
#17305=CARTESIAN_POINT('Ctrl Pts',(-32.1307248099903,2.45400157067097,307.979146100193));
#17306=CARTESIAN_POINT('Ctrl Pts',(-32.0538379840869,2.40129509364048,307.974094295275));
#17307=CARTESIAN_POINT('Ctrl Pts',(-31.9797342158895,2.3451636588574,307.969042490357));
#17308=CARTESIAN_POINT('Ctrl Pts',(-31.9422232705864,2.316750216044,307.96648529276));
#17309=CARTESIAN_POINT('Ctrl Pts',(-31.9054248848701,2.28745980672361,307.963928095163));
#17310=CARTESIAN_POINT('Ctrl Pts',(-31.8693809247322,2.25733319475708,307.961370897566));
#17311=CARTESIAN_POINT('Ctrl Pts',(-31.7981685674183,2.19781179234146,307.956318620616));
#17312=CARTESIAN_POINT('Ctrl Pts',(-31.729647740805,2.13481042932596,307.951266343666));
#17313=CARTESIAN_POINT('Ctrl Pts',(-31.6641780539341,2.06860182282104,307.946214066715));
#17314=CARTESIAN_POINT('Ctrl Pts',(-31.5987986618902,2.00248453025022,307.941168757791));
#17315=CARTESIAN_POINT('Ctrl Pts',(-31.5364623572441,1.93316909716568,307.936123448867));
#17316=CARTESIAN_POINT('Ctrl Pts',(-31.4774957496721,1.86096843334964,307.931078139943));
#17317=CARTESIAN_POINT('Ctrl Pts',(-31.4185922482308,1.78884503876624,307.926038230514));
#17318=CARTESIAN_POINT('Ctrl Pts',(-31.3630515553963,1.71384289310981,307.920998321085));
#17319=CARTESIAN_POINT('Ctrl Pts',(-31.3111626774768,1.63631089285653,307.915958411656));
#17320=CARTESIAN_POINT('Ctrl Pts',(-31.2593112028072,1.55883478027881,307.910922135163));
#17321=CARTESIAN_POINT('Ctrl Pts',(-31.2111065572676,1.47883280591249,307.905885858671));
#17322=CARTESIAN_POINT('Ctrl Pts',(-31.1667961166072,1.39668516334488,307.900849582178));
#17323=CARTESIAN_POINT('Ctrl Pts',(-31.1225017883583,1.31456739176476,307.895815137005));
#17324=CARTESIAN_POINT('Ctrl Pts',(-31.082099062583,1.2303058925807,307.890780691831));
#17325=CARTESIAN_POINT('Ctrl Pts',(-31.0457902517092,1.1443070278345,307.885746246658));
#17326=CARTESIAN_POINT('Ctrl Pts',(-31.0094844864118,1.05831537665717,307.880712223773));
#17327=CARTESIAN_POINT('Ctrl Pts',(-30.9772721258904,0.970587059008257,
307.875678200888));
#17328=CARTESIAN_POINT('Ctrl Pts',(-30.9493075875979,0.881549002821452,
307.870644178003));
#17329=CARTESIAN_POINT('Ctrl Pts',(-30.9213375720993,0.792493507413119,
307.865609169141));
#17330=CARTESIAN_POINT('Ctrl Pts',(-30.8976171639206,0.702128187929003,
307.860574160279));
#17331=CARTESIAN_POINT('Ctrl Pts',(-30.8782507678829,0.610894628588975,
307.855539151418));
#17332=CARTESIAN_POINT('Ctrl Pts',(-30.85886309204,0.519560821770802,307.850498610086));
#17333=CARTESIAN_POINT('Ctrl Pts',(-30.8438390705406,0.427357306001022,
307.845458068754));
#17334=CARTESIAN_POINT('Ctrl Pts',(-30.8332318076716,0.334735040013718,
307.840417527422));
#17335=CARTESIAN_POINT('Ctrl Pts',(-30.8226180278637,0.242055868332932,
307.83537388926));
#17336=CARTESIAN_POINT('Ctrl Pts',(-30.8164264383679,0.148957877202129,
307.830330251097));
#17337=CARTESIAN_POINT('Ctrl Pts',(-30.814658030505,0.0558941223142514,
307.825286612934));
#17338=CARTESIAN_POINT('Ctrl Pts',(-30.8128867592023,-0.0373203231879657,
307.820234808016));
#17339=CARTESIAN_POINT('Ctrl Pts',(-30.8155529550959,-0.13049997825746,
307.815183003098));
#17340=CARTESIAN_POINT('Ctrl Pts',(-30.8226055931285,-0.223194998240111,
307.810131198179));
#17341=CARTESIAN_POINT('Ctrl Pts',(-30.8261756021257,-0.270116739267614,
307.807574000585));
#17342=CARTESIAN_POINT('Ctrl Pts',(-30.8308687418061,-0.316914428363191,
307.805016802991));
#17343=CARTESIAN_POINT('Ctrl Pts',(-30.8366734185194,-0.363530793885804,
307.802459605397));
#17344=CARTESIAN_POINT('Ctrl Pts',(-30.8481417674742,-0.455631142144299,
307.797407328447));
#17345=CARTESIAN_POINT('Ctrl Pts',(-30.8639932262164,-0.547353585824728,
307.792355051498));
#17346=CARTESIAN_POINT('Ctrl Pts',(-30.8841932976764,-0.638248121330135,
307.787302774549));
#17347=CARTESIAN_POINT('Ctrl Pts',(-30.9043655094956,-0.729017296432075,
307.782257465625));
#17348=CARTESIAN_POINT('Ctrl Pts',(-30.9288743206129,-0.818960402425294,
307.777212156702));
#17349=CARTESIAN_POINT('Ctrl Pts',(-30.9576335741544,-0.907633408448775,
307.772166847778));
#17350=CARTESIAN_POINT('Ctrl Pts',(-30.98636204951,-0.996211516520251,307.76712693835));
#17351=CARTESIAN_POINT('Ctrl Pts',(-31.019331789487,-1.08352180604538,307.762087028922));
#17352=CARTESIAN_POINT('Ctrl Pts',(-31.0564060196508,-1.16913236713625,
307.757047119494));
#17353=CARTESIAN_POINT('Ctrl Pts',(-31.0934535254617,-1.25468121725305,
307.752010843002));
#17354=CARTESIAN_POINT('Ctrl Pts',(-31.1345994646829,-1.33853236773558,
307.74697456651));
#17355=CARTESIAN_POINT('Ctrl Pts',(-31.1796582064977,-1.420271954929,307.741938290018));
#17356=CARTESIAN_POINT('Ctrl Pts',(-31.2247005637995,-1.50198181951436,
307.736903844846));
#17357=CARTESIAN_POINT('Ctrl Pts',(-31.2736526829091,-1.5815812574963,307.731869399673));
#17358=CARTESIAN_POINT('Ctrl Pts',(-31.3262825288465,-1.65868011480843,
307.7268349545));
#17359=CARTESIAN_POINT('Ctrl Pts',(-31.3789079602023,-1.73577250508275,
307.721800931616));
#17360=CARTESIAN_POINT('Ctrl Pts',(-31.4352102544216,-1.81036436490036,
307.716766908732));
#17361=CARTESIAN_POINT('Ctrl Pts',(-31.4949141485207,-1.88209466448401,
307.711732885847));
#17362=CARTESIAN_POINT('Ctrl Pts',(-31.5546297363773,-1.95383901334778,
307.706697876986));
#17363=CARTESIAN_POINT('Ctrl Pts',(-31.6177479628078,-2.02272034768013,
307.701662868126));
#17364=CARTESIAN_POINT('Ctrl Pts',(-31.6839541577908,-2.08841174276876,
307.696627859265));
#17365=CARTESIAN_POINT('Ctrl Pts',(-31.7502331001723,-2.15417531959355,
307.691587317934));
#17366=CARTESIAN_POINT('Ctrl Pts',(-31.8196064682104,-2.21674164717348,
307.686546776603));
#17367=CARTESIAN_POINT('Ctrl Pts',(-31.8917239274152,-2.2758218490813,307.681506235272));
#17368=CARTESIAN_POINT('Ctrl Pts',(-31.9638856944762,-2.33493834895518,
307.67646259711));
#17369=CARTESIAN_POINT('Ctrl Pts',(-32.0387945526474,-2.39056419454827,
307.671418958948));
#17370=CARTESIAN_POINT('Ctrl Pts',(-32.1160701807903,-2.44245318213392,
307.666375320786));
#17371=CARTESIAN_POINT('Ctrl Pts',(-32.1934709351106,-2.49442618936225,
307.661323515868));
#17372=CARTESIAN_POINT('Ctrl Pts',(-32.2732457304435,-2.54265002938284,
307.65627171095));
#17373=CARTESIAN_POINT('Ctrl Pts',(-32.354988773443,-2.58692396473145,307.651219906033));
#17374=CARTESIAN_POINT('Ctrl Pts',(-32.3963666803406,-2.60933520252767,
307.648662708431));
#17375=CARTESIAN_POINT('Ctrl Pts',(-32.4382485800879,-2.63073510326995,
307.646105510829));
#17376=CARTESIAN_POINT('Ctrl Pts',(-32.4805800486849,-2.65110239533602,
307.643548313227));
#17377=CARTESIAN_POINT('Ctrl Pts',(-32.5642146895439,-2.69134222668769,
307.638496036277));
#17378=CARTESIAN_POINT('Ctrl Pts',(-32.649905495541,-2.72769275884674,307.633443759327));
#17379=CARTESIAN_POINT('Ctrl Pts',(-32.7372554911071,-2.75993927413227,
307.628391482377));
#17380=CARTESIAN_POINT('Ctrl Pts',(-32.8244850148468,-2.79214131549923,
307.623346173453));
#17381=CARTESIAN_POINT('Ctrl Pts',(-32.9133687678067,-2.82025043500779,
307.618300864529));
#17382=CARTESIAN_POINT('Ctrl Pts',(-33.0034868169279,-2.84409857719549,
307.613255555605));
#17383=CARTESIAN_POINT('Ctrl Pts',(-33.0935084216101,-2.86792119707424,
307.608215646176));
#17384=CARTESIAN_POINT('Ctrl Pts',(-33.1847612697107,-2.88749179048228,
307.603175736747));
#17385=CARTESIAN_POINT('Ctrl Pts',(-33.2768082036211,-2.90269141784396,
307.598135827319));
#17386=CARTESIAN_POINT('Ctrl Pts',(-33.368788787003,-2.91788008880259,307.593099550826));
#17387=CARTESIAN_POINT('Ctrl Pts',(-33.4615618814021,-2.92870398407821,
307.588063274334));
#17388=CARTESIAN_POINT('Ctrl Pts',(-33.5546790395243,-2.93509500852085,
307.583026997842));
#17389=CARTESIAN_POINT('Ctrl Pts',(-33.647762337862,-2.94148370902325,307.577992552668));
#17390=CARTESIAN_POINT('Ctrl Pts',(-33.7411890086107,-2.94344271052498,
307.572958107495));
#17391=CARTESIAN_POINT('Ctrl Pts',(-33.834505403747,-2.940955768077,307.567923662322));
#17392=CARTESIAN_POINT('Ctrl Pts',(-33.9278139715212,-2.9384690342333,307.562889639437));
#17393=CARTESIAN_POINT('Ctrl Pts',(-34.02101183798,-2.93153710992028,307.557855616552));
#17394=CARTESIAN_POINT('Ctrl Pts',(-34.1136464263757,-2.92019586292155,
307.552821593667));
#17395=CARTESIAN_POINT('Ctrl Pts',(-34.2062991584189,-2.90885239459717,
307.547786584806));
#17396=CARTESIAN_POINT('Ctrl Pts',(-34.2983879524005,-2.89309794278361,
307.542751575945));
#17397=CARTESIAN_POINT('Ctrl Pts',(-34.3894675592989,-2.87301997346699,
307.537716567083));
#17398=CARTESIAN_POINT('Ctrl Pts',(-34.4806472445123,-2.85291994246822,
307.532676025752));
#17399=CARTESIAN_POINT('Ctrl Pts',(-34.5708150946446,-2.82848700682537,
307.52763548442));
#17400=CARTESIAN_POINT('Ctrl Pts',(-34.6595385301776,-2.79985922017128,
307.522594943089));
#17401=CARTESIAN_POINT('Ctrl Pts',(-34.7483164760227,-2.77121384504605,
307.517551304926));
#17402=CARTESIAN_POINT('Ctrl Pts',(-34.8356478250652,-2.73836864437978,
307.512507666764));
#17403=CARTESIAN_POINT('Ctrl Pts',(-34.9211196298216,-2.70150999097007,
307.507464028601));
#17404=CARTESIAN_POINT('Ctrl Pts',(-35.0067298321613,-2.66459165532285,
307.502412223683));
#17405=CARTESIAN_POINT('Ctrl Pts',(-35.0904740804961,-2.62364708804529,
307.497360418765));
#17406=CARTESIAN_POINT('Ctrl Pts',(-35.1719638527412,-2.57890869903166,
307.492308613847));
#17407=CARTESIAN_POINT('Ctrl Pts',(-35.2132135551927,-2.55626235723776,
307.489751416251));
#17408=CARTESIAN_POINT('Ctrl Pts',(-35.2538860418139,-2.5326446075465,307.487194218654));
#17409=CARTESIAN_POINT('Ctrl Pts',(-35.2939339552803,-2.50808968060835,
307.484637021058));
#17410=CARTESIAN_POINT('Ctrl Pts',(-35.3730569571472,-2.45957630346084,
307.479584744106));
#17411=CARTESIAN_POINT('Ctrl Pts',(-35.4500240456981,-2.40722802069595,
307.474532467154));
#17412=CARTESIAN_POINT('Ctrl Pts',(-35.5244397220976,-2.35126225806358,
307.469480190202));
#17413=CARTESIAN_POINT('Ctrl Pts',(-35.5987527654934,-2.29537368258595,
307.464434881275));
#17414=CARTESIAN_POINT('Ctrl Pts',(-35.6705210372082,-2.23587780607041,
307.459389572349));
#17415=CARTESIAN_POINT('Ctrl Pts',(-35.7393758311229,-2.17303662510182,
307.454344263423));
#17416=CARTESIAN_POINT('Ctrl Pts',(-35.8081569365588,-2.11026269683656,
307.449304353992));
#17417=CARTESIAN_POINT('Ctrl Pts',(-35.8740304353281,-2.04415087807459,
307.444264444561));
#17418=CARTESIAN_POINT('Ctrl Pts',(-35.9366595815888,-1.97500424576248,
307.43922453513));
#17419=CARTESIAN_POINT('Ctrl Pts',(-35.9992435826527,-1.90590745667042,
307.434188258635));
#17420=CARTESIAN_POINT('Ctrl Pts',(-36.0585875822009,-1.83378053050454,
307.429151982141));
#17421=CARTESIAN_POINT('Ctrl Pts',(-36.1143914620148,-1.75896357163144,
307.424115705646));
#17422=CARTESIAN_POINT('Ctrl Pts',(-36.1701750501082,-1.68417381812141,
307.419081260471));
#17423=CARTESIAN_POINT('Ctrl Pts',(-36.2224208104377,-1.60669633088304,
307.414046815295));
#17424=CARTESIAN_POINT('Ctrl Pts',(-36.2708693956229,-1.52690366778303,
307.40901237012));
#17425=CARTESIAN_POINT('Ctrl Pts',(-36.3193139169498,-1.44711769767692,
307.403978347233));
#17426=CARTESIAN_POINT('Ctrl Pts',(-36.3639616659837,-1.36501731765078,
307.398944324346));
#17427=CARTESIAN_POINT('Ctrl Pts',(-36.4045976837326,-1.28100240873976,
307.393910301459));
#17428=CARTESIAN_POINT('Ctrl Pts',(-36.4452416605558,-1.1969710444538,307.388875292595));
#17429=CARTESIAN_POINT('Ctrl Pts',(-36.4818721525028,-1.1110248066317,307.383840283732));
#17430=CARTESIAN_POINT('Ctrl Pts',(-36.5143215448634,-1.02358536137261,
307.378805274868));
#17431=CARTESIAN_POINT('Ctrl Pts',(-36.5468065926316,-0.936049837610105,
307.373764733534));
#17432=CARTESIAN_POINT('Ctrl Pts',(-36.5751012154517,-0.847018248450529,
307.3687241922));
#17433=CARTESIAN_POINT('Ctrl Pts',(-36.5990871864318,-0.756929007223363,
307.363683650867));
#17434=CARTESIAN_POINT('Ctrl Pts',(-36.623087894023,-0.666784416554289,
307.358640012702));
#17435=CARTESIAN_POINT('Ctrl Pts',(-36.6427745861121,-0.575581314116294,
307.353596374537));
#17436=CARTESIAN_POINT('Ctrl Pts',(-36.658080287479,-0.483767778879875,
307.348552736372));
#17437=CARTESIAN_POINT('Ctrl Pts',(-36.6734107721307,-0.391805577409473,
307.343500931452));
#17438=CARTESIAN_POINT('Ctrl Pts',(-36.6843460521414,-0.299231410509212,
307.338449126532));
#17439=CARTESIAN_POINT('Ctrl Pts',(-36.6908710815961,-0.206497757338855,
307.333397321612));
#17440=CARTESIAN_POINT('Ctrl Pts',(-36.6941740178253,-0.159556460774516,
307.330840124038));
#17441=CARTESIAN_POINT('Ctrl Pts',(-36.6963477327181,-0.112574291880736,
307.328282926463));
#17442=CARTESIAN_POINT('Ctrl Pts',(-36.6973953537782,-0.0656096002261236,
307.325725728889));
#17443=CARTESIAN_POINT('Ctrl Pts',(-36.6978800833787,-0.0438792464827141,
307.324542524956));
#17444=CARTESIAN_POINT('Ctrl Pts',(-36.6981239984268,-0.0221435009775741,
307.323359321023));
#17445=CARTESIAN_POINT('Ctrl Pts',(-36.6981269972618,-0.000405866257568911,
307.32217611709));
#17446=CARTESIAN_POINT('',(-36.698126022555,-0.00242897115736518,306.322176117119));
#17447=CARTESIAN_POINT('Ctrl Pts',(-36.6981269972619,-0.00040586526797348,
307.322176117036));
#17448=CARTESIAN_POINT('Ctrl Pts',(-36.698139753591,0.0920610758296735,
307.31714303732));
#17449=CARTESIAN_POINT('Ctrl Pts',(-36.6937888801165,0.18470001600166,307.312109957604));
#17450=CARTESIAN_POINT('Ctrl Pts',(-36.6850517529411,0.27706306062714,307.307076877888));
#17451=CARTESIAN_POINT('Ctrl Pts',(-36.6763266285064,0.369299220333856,
307.30205071243));
#17452=CARTESIAN_POINT('Ctrl Pts',(-36.6632272637743,0.461259795437067,
307.297024546972));
#17453=CARTESIAN_POINT('Ctrl Pts',(-36.6457830375716,0.55249627193066,307.291998381513));
#17454=CARTESIAN_POINT('Ctrl Pts',(-36.6276799638658,0.647178640723046,
307.286782383814));
#17455=CARTESIAN_POINT('Ctrl Pts',(-36.6048972960815,0.741080639958951,
307.281566386114));
#17456=CARTESIAN_POINT('Ctrl Pts',(-36.5775271082731,0.833705926307351,
307.276350388414));
#17457=CARTESIAN_POINT('Ctrl Pts',(-36.5511998042163,0.922801919879714,
307.271333135395));
#17458=CARTESIAN_POINT('Ctrl Pts',(-36.5206283477159,1.01071624850131,307.266315882377));
#17459=CARTESIAN_POINT('Ctrl Pts',(-36.4859465319387,1.09701844147827,307.261298629358));
#17460=CARTESIAN_POINT('Ctrl Pts',(-36.4512761743739,1.18329212185186,307.256283033945));
#17461=CARTESIAN_POINT('Ctrl Pts',(-36.412498321883,1.26795430918394,307.251267438531));
#17462=CARTESIAN_POINT('Ctrl Pts',(-36.3697956659223,1.35059255025555,307.246251843117));
#17463=CARTESIAN_POINT('Ctrl Pts',(-36.3270949344648,1.43322706702593,307.241236473744));
#17464=CARTESIAN_POINT('Ctrl Pts',(-36.2804699574415,1.51383742112168,307.236221104371));
#17465=CARTESIAN_POINT('Ctrl Pts',(-36.2301497892036,1.59203497558224,307.231205734998));
#17466=CARTESIAN_POINT('Ctrl Pts',(-36.1798175316409,1.67025131685651,307.226189160692));
#17467=CARTESIAN_POINT('Ctrl Pts',(-36.1257885629022,1.74605333106891,307.221172586386));
#17468=CARTESIAN_POINT('Ctrl Pts',(-36.0683350620437,1.8190816349526,307.216156012079));
#17469=CARTESIAN_POINT('Ctrl Pts',(-36.010817394194,1.89219150055938,307.211133835008));
#17470=CARTESIAN_POINT('Ctrl Pts',(-35.9498678401348,1.96252112227767,307.206111657937));
#17471=CARTESIAN_POINT('Ctrl Pts',(-35.8857983772258,2.02974479494494,307.201089480865));
#17472=CARTESIAN_POINT('Ctrl Pts',(-35.821686349775,2.09701312765286,307.196063967311));
#17473=CARTESIAN_POINT('Ctrl Pts',(-35.7544506125824,2.16117109661215,307.191038453757));
#17474=CARTESIAN_POINT('Ctrl Pts',(-35.6844378236209,2.22193192175536,307.186012940203));
#17475=CARTESIAN_POINT('Ctrl Pts',(-35.6143164860534,2.28278695115715,307.180979635036));
#17476=CARTESIAN_POINT('Ctrl Pts',(-35.5414098575938,2.34023405256001,307.17594632987));
#17477=CARTESIAN_POINT('Ctrl Pts',(-35.4660949213958,2.39402877889483,307.170913024704));
#17478=CARTESIAN_POINT('Ctrl Pts',(-35.4456520988773,2.40863034530928,307.169546828709));
#17479=CARTESIAN_POINT('Ctrl Pts',(-35.4250319892514,2.42296308250054,307.168180632714));
#17480=CARTESIAN_POINT('Ctrl Pts',(-35.4042424375054,2.43702268924837,307.166814436719));
#17481=CARTESIAN_POINT('Ctrl Pts',(-35.3273613944309,2.48901598112855,307.161762159766));
#17482=CARTESIAN_POINT('Ctrl Pts',(-35.2478795816544,2.5374609691507,307.156709882814));
#17483=CARTESIAN_POINT('Ctrl Pts',(-35.1661584636723,2.58208740027949,307.151657605861));
#17484=CARTESIAN_POINT('Ctrl Pts',(-35.0845500542523,2.62665228329191,307.146612296935));
#17485=CARTESIAN_POINT('Ctrl Pts',(-35.0007088632262,2.66740886353554,307.141566988008));
#17486=CARTESIAN_POINT('Ctrl Pts',(-34.9150258647783,2.70412970838266,307.136521679082));
#17487=CARTESIAN_POINT('Ctrl Pts',(-34.8294345643735,2.74081125453949,307.131481769651));
#17488=CARTESIAN_POINT('Ctrl Pts',(-34.7420057805569,2.77346547600108,307.12644186022));
#17489=CARTESIAN_POINT('Ctrl Pts',(-34.6531546828219,2.80191102313487,307.121401950789));
#17490=CARTESIAN_POINT('Ctrl Pts',(-34.5643676319506,2.83033606576025,307.116365674294));
#17491=CARTESIAN_POINT('Ctrl Pts',(-34.4741607268776,2.85455832900194,307.1113293978));
#17492=CARTESIAN_POINT('Ctrl Pts',(-34.3829677126316,2.8744451208281,307.106293121305));
#17493=CARTESIAN_POINT('Ctrl Pts',(-34.2918078585032,2.894324681307,307.10125867613));
#17494=CARTESIAN_POINT('Ctrl Pts',(-34.1996630411661,2.90987180767166,307.096224230954));
#17495=CARTESIAN_POINT('Ctrl Pts',(-34.10697970368,2.92100434748801,307.091189785779));
#17496=CARTESIAN_POINT('Ctrl Pts',(-34.014304140456,2.93213595350886,307.086155762892));
#17497=CARTESIAN_POINT('Ctrl Pts',(-33.9210905880013,2.93885365641507,307.081121740005));
#17498=CARTESIAN_POINT('Ctrl Pts',(-33.8277920205403,2.94112701671504,307.076087717118));
#17499=CARTESIAN_POINT('Ctrl Pts',(-33.734475179384,2.94340082228116,307.071052708254));
#17500=CARTESIAN_POINT('Ctrl Pts',(-33.641073734259,2.94122854601304,307.066017699391));
#17501=CARTESIAN_POINT('Ctrl Pts',(-33.548040925887,2.93463186366684,307.060982690527));
#17502=CARTESIAN_POINT('Ctrl Pts',(-33.4549058930231,2.92802793288311,307.055942149194));
#17503=CARTESIAN_POINT('Ctrl Pts',(-33.3621407492861,2.91698992328303,307.05090160786));
#17504=CARTESIAN_POINT('Ctrl Pts',(-33.2701935698905,2.90159140420477,307.045861066527));
#17505=CARTESIAN_POINT('Ctrl Pts',(-33.1781898995652,2.88618342451375,307.040817428362));
#17506=CARTESIAN_POINT('Ctrl Pts',(-33.087005627893,2.86640969600229,307.035773790198));
#17507=CARTESIAN_POINT('Ctrl Pts',(-32.9970764458735,2.84239445150329,307.030730152033));
#17508=CARTESIAN_POINT('Ctrl Pts',(-32.9070016488019,2.81834032106093,307.025678347113));
#17509=CARTESIAN_POINT('Ctrl Pts',(-32.8181864212957,2.7900310983714,307.020626542193));
#17510=CARTESIAN_POINT('Ctrl Pts',(-32.7310489954841,2.75764012026148,307.015574737274));
#17511=CARTESIAN_POINT('Ctrl Pts',(-32.6869404803156,2.74124397433476,307.013017539699));
#17512=CARTESIAN_POINT('Ctrl Pts',(-32.6432615239701,2.72380270133817,307.010460342125));
#17513=CARTESIAN_POINT('Ctrl Pts',(-32.600063964871,2.70534326849839,307.00790314455));
#17514=CARTESIAN_POINT('Ctrl Pts',(-32.5147181804377,2.66887281024197,307.002850867581));
#17515=CARTESIAN_POINT('Ctrl Pts',(-32.4309467017257,2.62829430803742,306.997798590612));
#17516=CARTESIAN_POINT('Ctrl Pts',(-32.3491724805325,2.58376525812186,306.992746313643));
#17517=CARTESIAN_POINT('Ctrl Pts',(-32.2675110411381,2.53929762201457,306.9877010047));
#17518=CARTESIAN_POINT('Ctrl Pts',(-32.1878417723216,2.4908904757435,306.982655695757));
#17519=CARTESIAN_POINT('Ctrl Pts',(-32.1105676113593,2.43874931375297,306.977610386814));
#17520=CARTESIAN_POINT('Ctrl Pts',(-32.0333761492907,2.38666395329252,306.972570477366));
#17521=CARTESIAN_POINT('Ctrl Pts',(-31.9585750665206,2.3308527672113,306.967530567918));
#17522=CARTESIAN_POINT('Ctrl Pts',(-31.8865416649192,2.27156654765131,306.962490658471));
#17523=CARTESIAN_POINT('Ctrl Pts',(-31.8145601874179,2.21232306359354,306.957454381959));
#17524=CARTESIAN_POINT('Ctrl Pts',(-31.7453427677007,2.14960980644218,306.952418105448));
#17525=CARTESIAN_POINT('Ctrl Pts',(-31.6792358642956,2.08371953619431,306.947381828936));
#17526=CARTESIAN_POINT('Ctrl Pts',(-31.6131529990541,2.01785322533666,306.942347383744));
#17527=CARTESIAN_POINT('Ctrl Pts',(-31.5501787174819,1.94881250970079,306.937312938552));
#17528=CARTESIAN_POINT('Ctrl Pts',(-31.4906238694807,1.87692819552715,306.932278493359));
#17529=CARTESIAN_POINT('Ctrl Pts',(-31.4310740169294,1.80504991099688,306.927244470455));
#17530=CARTESIAN_POINT('Ctrl Pts',(-31.3749433109655,1.73032884438235,306.922210447551));
#17531=CARTESIAN_POINT('Ctrl Pts',(-31.3225026665881,1.65312929950753,306.917176424647));
#17532=CARTESIAN_POINT('Ctrl Pts',(-31.2700517510524,1.57591463413311,306.912141415767));
#17533=CARTESIAN_POINT('Ctrl Pts',(-31.2212925817866,1.49622089408594,306.907106406886));
#17534=CARTESIAN_POINT('Ctrl Pts',(-31.1764524078117,1.41444083230993,306.902071398006));
#17535=CARTESIAN_POINT('Ctrl Pts',(-31.1315629634342,1.3325709105665,306.897030856655));
#17536=CARTESIAN_POINT('Ctrl Pts',(-31.0906013239388,1.24861048123626,306.891990315305));
#17537=CARTESIAN_POINT('Ctrl Pts',(-31.0537483167916,1.16297605995543,306.886949773954));
#17538=CARTESIAN_POINT('Ctrl Pts',(-31.016872667725,1.07728902620675,306.881906135773));
#17539=CARTESIAN_POINT('Ctrl Pts',(-30.9841108322309,0.989926368676627,
306.876862497592));
#17540=CARTESIAN_POINT('Ctrl Pts',(-30.9555943407051,0.901321631135792,
306.87181885941));
#17541=CARTESIAN_POINT('Ctrl Pts',(-30.927031674732,0.812573423112735,306.866767054474));
#17542=CARTESIAN_POINT('Ctrl Pts',(-30.9027281917879,0.722579548320724,
306.861715249537));
#17543=CARTESIAN_POINT('Ctrl Pts',(-30.8827646878,0.63178546808248,306.856663444601));
#17544=CARTESIAN_POINT('Ctrl Pts',(-30.8726592658241,0.585825976488276,
306.854106247194));
#17545=CARTESIAN_POINT('Ctrl Pts',(-30.8636650670121,0.539661560227087,
306.851549049788));
#17546=CARTESIAN_POINT('Ctrl Pts',(-30.8557874967225,0.493350402064106,
306.848991852381));
#17547=CARTESIAN_POINT('Ctrl Pts',(-30.8402237133945,0.401853048842495,
306.843939575486));
#17548=CARTESIAN_POINT('Ctrl Pts',(-30.8289659557546,0.309454249419359,
306.838887298591));
#17549=CARTESIAN_POINT('Ctrl Pts',(-30.8221108921367,0.216594853554895,
306.833835021696));
#17550=CARTESIAN_POINT('Ctrl Pts',(-30.8152652829216,0.123863528001442,
306.828789712827));
#17551=CARTESIAN_POINT('Ctrl Pts',(-30.8128103340577,0.0306733075301457,
306.823744403958));
#17552=CARTESIAN_POINT('Ctrl Pts',(-30.8147915248671,-0.0625257878188257,
306.818699095089));
#17553=CARTESIAN_POINT('Ctrl Pts',(-30.8167705954038,-0.155625141390326,
306.813659185715));
#17554=CARTESIAN_POINT('Ctrl Pts',(-30.8231763597282,-0.248732909191379,
306.808619276341));
#17555=CARTESIAN_POINT('Ctrl Pts',(-30.8340023341004,-0.341396088626811,
306.803579366967));
#17556=CARTESIAN_POINT('Ctrl Pts',(-30.8448205047467,-0.433992473329439,
306.79854309053));
#17557=CARTESIAN_POINT('Ctrl Pts',(-30.8600525009477,-0.526144466667463,
306.793506814092));
#17558=CARTESIAN_POINT('Ctrl Pts',(-30.8796398545442,-0.617402264914443,
306.788470537654));
#17559=CARTESIAN_POINT('Ctrl Pts',(-30.8992200856781,-0.708626879492081,
306.783436092535));
#17560=CARTESIAN_POINT('Ctrl Pts',(-30.9231524348441,-0.798957511002144,
306.778401647416));
#17561=CARTESIAN_POINT('Ctrl Pts',(-30.9513271653086,-0.887953684394656,
306.773367202297));
#17562=CARTESIAN_POINT('Ctrl Pts',(-30.9794995324835,-0.976942392809793,
306.768333179466));
#17563=CARTESIAN_POINT('Ctrl Pts',(-31.0119134391844,-1.0645964421749,306.763299156635));
#17564=CARTESIAN_POINT('Ctrl Pts',(-31.0484093608343,-1.15049078647766,
306.758265133804));
#17565=CARTESIAN_POINT('Ctrl Pts',(-31.0849124306717,-1.23640195427339,
306.753230124997));
#17566=CARTESIAN_POINT('Ctrl Pts',(-31.1254989292363,-1.32055232380034,
306.748195116189));
#17567=CARTESIAN_POINT('Ctrl Pts',(-31.16996176735,-1.40253814878296,306.743160107381));
#17568=CARTESIAN_POINT('Ctrl Pts',(-31.2144734612595,-1.48461405984412,
306.738119566102));
#17569=CARTESIAN_POINT('Ctrl Pts',(-31.2628697847167,-1.5645202876586,306.733079024823));
#17570=CARTESIAN_POINT('Ctrl Pts',(-31.3148985311617,-1.64187924026533,
306.728038483544));
#17571=CARTESIAN_POINT('Ctrl Pts',(-31.3669592432718,-1.71928572102787,
306.722994845434));
#17572=CARTESIAN_POINT('Ctrl Pts',(-31.4226565562559,-1.79414145480618,
306.717951207324));
#17573=CARTESIAN_POINT('Ctrl Pts',(-31.4816972501806,-1.86610106860357,
306.712907569213));
#17574=CARTESIAN_POINT('Ctrl Pts',(-31.5408335439427,-1.93817720080406,
306.707855764347));
#17575=CARTESIAN_POINT('Ctrl Pts',(-31.6033237289251,-2.00734752186671,
306.70280395948));
#17576=CARTESIAN_POINT('Ctrl Pts',(-31.6688370895148,-2.07330285393789,
306.697752154613));
#17577=CARTESIAN_POINT('Ctrl Pts',(-31.7019996220824,-2.10668911023929,
306.695194956479));
#17578=CARTESIAN_POINT('Ctrl Pts',(-31.7359362507718,-2.13925220939775,
306.692637758345));
#17579=CARTESIAN_POINT('Ctrl Pts',(-31.7706009921044,-2.17095609620994,
306.690080560212));
#17580=CARTESIAN_POINT('Ctrl Pts',(-31.8390884013205,-2.23359372125404,
306.685028283221));
#17581=CARTESIAN_POINT('Ctrl Pts',(-31.9106657048742,-2.29309973061691,
306.679976006231));
#17582=CARTESIAN_POINT('Ctrl Pts',(-31.9850146601458,-2.34915410097937,
306.67492372924));
#17583=CARTESIAN_POINT('Ctrl Pts',(-32.0592610744286,-2.40513116197615,
306.669878420275));
#17584=CARTESIAN_POINT('Ctrl Pts',(-32.1362711927408,-2.45766577846476,
306.664833111311));
#17585=CARTESIAN_POINT('Ctrl Pts',(-32.2156913400819,-2.5064759922723,306.659787802347));
#17586=CARTESIAN_POINT('Ctrl Pts',(-32.2950264918837,-2.55523396932897,
306.654747892878));
#17587=CARTESIAN_POINT('Ctrl Pts',(-32.3767661696773,-2.60027523483947,
306.64970798341));
#17588=CARTESIAN_POINT('Ctrl Pts',(-32.4605260485303,-2.64135989768591,
306.644668073941));
#17589=CARTESIAN_POINT('Ctrl Pts',(-32.544225550429,-2.68241494531745,306.63963179741));
#17590=CARTESIAN_POINT('Ctrl Pts',(-32.6299419612168,-2.7195188640592,306.634595520879));
#17591=CARTESIAN_POINT('Ctrl Pts',(-32.7172654908323,-2.7524771955988,306.629559244348));
#17592=CARTESIAN_POINT('Ctrl Pts',(-32.8045572673655,-2.78542354264103,
306.624524799136));
#17593=CARTESIAN_POINT('Ctrl Pts',(-32.8934545865554,-2.81422714045999,
306.619490353925));
#17594=CARTESIAN_POINT('Ctrl Pts',(-32.9835277338843,-2.83874168162049,
306.614455908713));
#17595=CARTESIAN_POINT('Ctrl Pts',(-33.0735933258834,-2.86325416650282,
306.609421885791));
#17596=CARTESIAN_POINT('Ctrl Pts',(-33.1648341212131,-2.8834781935354,306.604387862868));
#17597=CARTESIAN_POINT('Ctrl Pts',(-33.2568064110736,-2.89931766528798,
306.599353839946));
#17598=CARTESIAN_POINT('Ctrl Pts',(-33.3487967148501,-2.91516023939793,
306.594318831047));
#17599=CARTESIAN_POINT('Ctrl Pts',(-33.4415183598488,-2.92661647767775,
306.589283822149));
#17600=CARTESIAN_POINT('Ctrl Pts',(-33.534519782234,-2.93364180326083,306.58424881325));
#17601=CARTESIAN_POINT('Ctrl Pts',(-33.6276233946031,-2.94067484827325,
306.579208271883));
#17602=CARTESIAN_POINT('Ctrl Pts',(-33.7210069543244,-2.94326722859524,
306.574167730515));
#17603=CARTESIAN_POINT('Ctrl Pts',(-33.8142164488815,-2.94142645987675,
306.569127189148));
#17604=CARTESIAN_POINT('Ctrl Pts',(-33.9074832099043,-2.93958456021854,
306.56408355095));
#17605=CARTESIAN_POINT('Ctrl Pts',(-34.0005752499398,-2.93330411913235,
306.559039912753));
#17606=CARTESIAN_POINT('Ctrl Pts',(-34.0930434286844,-2.92264457933255,
306.553996274555));
#17607=CARTESIAN_POINT('Ctrl Pts',(-34.1856613336496,-2.91196777940469,
306.548944469603));
#17608=CARTESIAN_POINT('Ctrl Pts',(-34.2776529227837,-2.89689779674328,
306.543892664651));
#17609=CARTESIAN_POINT('Ctrl Pts',(-34.3685791756897,-2.87754519746104,
306.538840859699));
#17610=CARTESIAN_POINT('Ctrl Pts',(-34.4146055688879,-2.86774901302032,
306.53628366248));
#17611=CARTESIAN_POINT('Ctrl Pts',(-34.4603592237407,-2.85685627741157,
306.533726465261));
#17612=CARTESIAN_POINT('Ctrl Pts',(-34.5057849265722,-2.84488611916129,
306.531169268042));
#17613=CARTESIAN_POINT('Ctrl Pts',(-34.5955328883636,-2.82123657191558,
306.526116990939));
#17614=CARTESIAN_POINT('Ctrl Pts',(-34.684321735225,-2.79329347552173,306.521064713835));
#17615=CARTESIAN_POINT('Ctrl Pts',(-34.7717100848437,-2.76115103699193,
306.516012436732));
#17616=CARTESIAN_POINT('Ctrl Pts',(-34.8589779097587,-2.72905292883226,
306.510967127654));
#17617=CARTESIAN_POINT('Ctrl Pts',(-34.944848662327,-2.69276713934605,306.505921818576));
#17618=CARTESIAN_POINT('Ctrl Pts',(-35.0288937696123,-2.65243827722054,
306.500876509497));
#17619=CARTESIAN_POINT('Ctrl Pts',(-35.1128489317433,-2.61215257508189,
306.495836599914));
#17620=CARTESIAN_POINT('Ctrl Pts',(-35.1949819336989,-2.56783259183184,
306.49079669033));
#17621=CARTESIAN_POINT('Ctrl Pts',(-35.2748829662207,-2.51967148489425,
306.485756780746));
#17622=CARTESIAN_POINT('Ctrl Pts',(-35.3547264033976,-2.47154509409835,
306.480720504099));
#17623=CARTESIAN_POINT('Ctrl Pts',(-35.4323406896227,-2.41958331169321,
306.475684227451));
#17624=CARTESIAN_POINT('Ctrl Pts',(-35.5073404167459,-2.3640253081285,306.470647950803));
#17625=CARTESIAN_POINT('Ctrl Pts',(-35.5823128720508,-2.30848750687431,
306.465613505474));
#17626=CARTESIAN_POINT('Ctrl Pts',(-35.6546723003415,-2.24935634647697,
306.460579060145));
#17627=CARTESIAN_POINT('Ctrl Pts',(-35.7240629802756,-2.18691382476478,
306.455544614817));
#17628=CARTESIAN_POINT('Ctrl Pts',(-35.7934478397329,-2.1244765407193,306.450510591776));
#17629=CARTESIAN_POINT('Ctrl Pts',(-35.8598641158273,-2.05872874490757,
306.445476568736));
#17630=CARTESIAN_POINT('Ctrl Pts',(-35.9229907167373,-1.98999139258114,
306.440442545695));
#17631=CARTESIAN_POINT('Ctrl Pts',(-35.9861296817824,-1.92124057718371,
306.435407536678));
#17632=CARTESIAN_POINT('Ctrl Pts',(-36.0459773918053,-1.8494993698208,306.430372527661));
#17633=CARTESIAN_POINT('Ctrl Pts',(-36.1022518111705,-1.77512323203914,
306.425337518644));
#17634=CARTESIAN_POINT('Ctrl Pts',(-36.1585880648787,-1.70066536974278,
306.420296977159));
#17635=CARTESIAN_POINT('Ctrl Pts',(-36.2113429220369,-1.62356715256605,
306.415256435673));
#17636=CARTESIAN_POINT('Ctrl Pts',(-36.2602768120308,-1.54421431330102,
306.410215894187));
#17637=CARTESIAN_POINT('Ctrl Pts',(-36.3092407662475,-1.46481272088265,
306.405172255871));
#17638=CARTESIAN_POINT('Ctrl Pts',(-36.3543788650403,-1.38315413722627,
306.400128617554));
#17639=CARTESIAN_POINT('Ctrl Pts',(-36.3954978286515,-1.29964832250575,
306.395084979238));
#17640=CARTESIAN_POINT('Ctrl Pts',(-36.4366833728559,-1.21600729361156,
306.390033174168));
#17641=CARTESIAN_POINT('Ctrl Pts',(-36.4738366128949,-1.13051346928265,
306.384981369099));
#17642=CARTESIAN_POINT('Ctrl Pts',(-36.506812726369,-1.04359579038107,306.379929564029));
#17643=CARTESIAN_POINT('Ctrl Pts',(-36.5235050543643,-0.999598537461807,
306.377372367977));
#17644=CARTESIAN_POINT('Ctrl Pts',(-36.539127863107,-0.955236679408074,
306.374815171925));
#17645=CARTESIAN_POINT('Ctrl Pts',(-36.553667329706,-0.910566990938581,
306.372257975873));
#17646=CARTESIAN_POINT('Ctrl Pts',(-36.5880629328898,-0.804893177633095,
306.366208489802));
#17647=CARTESIAN_POINT('Ctrl Pts',(-36.6164932427341,-0.697188268922234,
306.36015900373));
#17648=CARTESIAN_POINT('Ctrl Pts',(-36.6387539381384,-0.588069792741501,
306.354109517659));
#17649=CARTESIAN_POINT('Ctrl Pts',(-36.6607618428289,-0.480190457431459,
306.348128729078));
#17650=CARTESIAN_POINT('Ctrl Pts',(-36.6767394151754,-0.370929531773017,
306.342147940497));
#17651=CARTESIAN_POINT('Ctrl Pts',(-36.6865353244095,-0.260904580760653,
306.336167151916));
#17652=CARTESIAN_POINT('Ctrl Pts',(-36.6941739440284,-0.175109711770168,
306.33150347365));
#17653=CARTESIAN_POINT('Ctrl Pts',(-36.6980546711137,-0.0888506926227376,
306.326839795385));
#17654=CARTESIAN_POINT('Ctrl Pts',(-36.698126022555,-0.00242897115734986,
306.322176117119));
#17655=CARTESIAN_POINT('',(-36.6981265705527,0.00163569045731701,305.322176117057));
#17656=CARTESIAN_POINT('Ctrl Pts',(-36.6981260225555,-0.00242897062730326,
306.32217611709));
#17657=CARTESIAN_POINT('Ctrl Pts',(-36.698202775672,0.0905353448933393,
306.31715937303));
#17658=CARTESIAN_POINT('Ctrl Pts',(-36.6938688627679,0.183566125357343,
306.31214262897));
#17659=CARTESIAN_POINT('Ctrl Pts',(-36.685132115652,0.276212201836619,306.30712588491));
#17660=CARTESIAN_POINT('Ctrl Pts',(-36.6763977473887,0.368833052525131,
306.302110506815));
#17661=CARTESIAN_POINT('Ctrl Pts',(-36.6632629682403,0.46106896195887,306.297095128721));
#17662=CARTESIAN_POINT('Ctrl Pts',(-36.6457875999744,0.552472409200222,
306.292079750626));
#17663=CARTESIAN_POINT('Ctrl Pts',(-36.6283120156875,0.643876986321143,
306.287064310534));
#17664=CARTESIAN_POINT('Ctrl Pts',(-36.6064958205825,0.734448641302927,
306.282048870442));
#17665=CARTESIAN_POINT('Ctrl Pts',(-36.5804500087084,0.82374977095704,306.27703343035));
#17666=CARTESIAN_POINT('Ctrl Pts',(-36.5543964610427,0.913077423682411,
306.272016500637));
#17667=CARTESIAN_POINT('Ctrl Pts',(-36.5241109274419,1.00113337224781,306.266999570923));
#17668=CARTESIAN_POINT('Ctrl Pts',(-36.4897539824691,1.08749605001895,306.26198264121));
#17669=CARTESIAN_POINT('Ctrl Pts',(-36.4553563024659,1.1739611229914,306.256959763215));
#17670=CARTESIAN_POINT('Ctrl Pts',(-36.4168777457047,1.2587285034919,306.25193688522));
#17671=CARTESIAN_POINT('Ctrl Pts',(-36.3745265169867,1.34139781635152,306.246914007225));
#17672=CARTESIAN_POINT('Ctrl Pts',(-36.3321451161448,1.4241260249936,306.2418875508));
#17673=CARTESIAN_POINT('Ctrl Pts',(-36.2858857760911,1.50475280471883,306.236861094376));
#17674=CARTESIAN_POINT('Ctrl Pts',(-36.2360008746042,1.5829054587457,306.231834637951));
#17675=CARTESIAN_POINT('Ctrl Pts',(-36.1860368178904,1.66118212205947,306.22680020576));
#17676=CARTESIAN_POINT('Ctrl Pts',(-36.1324359812999,1.73697646456414,306.22176577357));
#17677=CARTESIAN_POINT('Ctrl Pts',(-36.0754916759822,1.80994795974064,306.216731341379));
#17678=CARTESIAN_POINT('Ctrl Pts',(-36.062730423554,1.82630091487481,306.215603122154));
#17679=CARTESIAN_POINT('Ctrl Pts',(-36.0498014057685,1.84251224957421,306.214474902929));
#17680=CARTESIAN_POINT('Ctrl Pts',(-36.0367081721129,1.85857839022412,306.213346683704));
#17681=CARTESIAN_POINT('Ctrl Pts',(-35.978075374343,1.93052416011187,306.208294406214));
#17682=CARTESIAN_POINT('Ctrl Pts',(-35.9159294711306,1.99982180602581,306.203242128725));
#17683=CARTESIAN_POINT('Ctrl Pts',(-35.8505386944799,2.06610836110437,306.198189851235));
#17684=CARTESIAN_POINT('Ctrl Pts',(-35.7852381038654,2.13230349470184,306.193144541775));
#17685=CARTESIAN_POINT('Ctrl Pts',(-35.7167018420535,2.19549547619006,306.188099232316));
#17686=CARTESIAN_POINT('Ctrl Pts',(-35.6452387402726,2.25535383658378,306.183053922856));
#17687=CARTESIAN_POINT('Ctrl Pts',(-35.5738521184413,2.3151481364445,306.178014012896));
#17688=CARTESIAN_POINT('Ctrl Pts',(-35.4995452213187,2.37161562271623,306.172974102936));
#17689=CARTESIAN_POINT('Ctrl Pts',(-35.4226633308578,2.42446298014973,306.167934192977));
#17690=CARTESIAN_POINT('Ctrl Pts',(-35.3458368595817,2.47727224333955,306.162897915962));
#17691=CARTESIAN_POINT('Ctrl Pts',(-35.2664394493703,2.52646631353897,306.157861638948));
#17692=CARTESIAN_POINT('Ctrl Pts',(-35.1848481936732,2.57179311433115,306.152825361933));
#17693=CARTESIAN_POINT('Ctrl Pts',(-35.1032866067365,2.61710343308762,306.147790916243));
#17694=CARTESIAN_POINT('Ctrl Pts',(-35.019533147073,2.65854906056046,306.142756470554));
#17695=CARTESIAN_POINT('Ctrl Pts',(-34.9339916339833,2.69592265532811,306.137722024864));
#17696=CARTESIAN_POINT('Ctrl Pts',(-34.8484572962066,2.73329311515894,306.132688001469));
#17697=CARTESIAN_POINT('Ctrl Pts',(-34.7611356103776,2.76659204370274,306.127653978074));
#17698=CARTESIAN_POINT('Ctrl Pts',(-34.6724515546702,2.79565973551802,306.122619954679));
#17699=CARTESIAN_POINT('Ctrl Pts',(-34.5837501292006,2.82473312056524,306.117584945314));
#17700=CARTESIAN_POINT('Ctrl Pts',(-34.493686226165,2.84957348500391,306.112549935949));
#17701=CARTESIAN_POINT('Ctrl Pts',(-34.4027000997504,2.87007095022769,306.107514926585));
#17702=CARTESIAN_POINT('Ctrl Pts',(-34.3116139979904,2.89059093801889,306.102474384763));
#17703=CARTESIAN_POINT('Ctrl Pts',(-34.2196040841762,2.90675840339532,306.097433842942));
#17704=CARTESIAN_POINT('Ctrl Pts',(-34.1271206231304,2.91851464795662,306.092393301121));
#17705=CARTESIAN_POINT('Ctrl Pts',(-34.0345803418033,2.93027811535664,306.087349662475));
#17706=CARTESIAN_POINT('Ctrl Pts',(-33.9415663765902,2.93762493154942,306.08230602383));
#17707=CARTESIAN_POINT('Ctrl Pts',(-33.8485317360434,2.94054848105325,306.077262385184));
#17708=CARTESIAN_POINT('Ctrl Pts',(-33.7553464523236,2.94347676441505,306.072210579799));
#17709=CARTESIAN_POINT('Ctrl Pts',(-33.6621408700775,2.94196748977113,306.067158774413));
#17710=CARTESIAN_POINT('Ctrl Pts',(-33.569365432799,2.93606609387158,306.062106969028));
#17711=CARTESIAN_POINT('Ctrl Pts',(-33.5224030828902,2.93307884393437,306.05954977653));
#17712=CARTESIAN_POINT('Ctrl Pts',(-33.4755508324832,2.92896701434898,306.056992584032));
#17713=CARTESIAN_POINT('Ctrl Pts',(-33.4288660923819,2.92374148683042,306.054435391535));
#17714=CARTESIAN_POINT('Ctrl Pts',(-33.3366304507842,2.91341734488777,306.04938311342));
#17715=CARTESIAN_POINT('Ctrl Pts',(-33.2447182739149,2.89870573750591,306.044330835305));
#17716=CARTESIAN_POINT('Ctrl Pts',(-33.1535799591182,2.87963557296523,306.03927855719));
#17717=CARTESIAN_POINT('Ctrl Pts',(-33.0625673407369,2.86059170967151,306.034233247091));
#17718=CARTESIAN_POINT('Ctrl Pts',(-32.9723268946378,2.83720132452903,306.029187936992));
#17719=CARTESIAN_POINT('Ctrl Pts',(-32.8833036871683,2.80954505578512,306.024142626893));
#17720=CARTESIAN_POINT('Ctrl Pts',(-32.794375752273,2.78191838476061,306.019102716281));
#17721=CARTESIAN_POINT('Ctrl Pts',(-32.706662888694,2.75003503553994,306.01406280567));
#17722=CARTESIAN_POINT('Ctrl Pts',(-32.6205986710841,2.71402641049569,306.009022895058));
#17723=CARTESIAN_POINT('Ctrl Pts',(-32.5345964913271,2.67804374162513,306.003986617376));
#17724=CARTESIAN_POINT('Ctrl Pts',(-32.4502410040868,2.63794187841581,305.998950339694));
#17725=CARTESIAN_POINT('Ctrl Pts',(-32.3679483456585,2.59390129987756,305.993914062012));
#17726=CARTESIAN_POINT('Ctrl Pts',(-32.2856856108797,2.54987673558482,305.988879615645));
#17727=CARTESIAN_POINT('Ctrl Pts',(-32.205484606065,2.50191651061977,305.983845169278));
#17728=CARTESIAN_POINT('Ctrl Pts',(-32.1277383357946,2.45024779890302,305.978810722912));
#17729=CARTESIAN_POINT('Ctrl Pts',(-32.0499985868298,2.39858342112345,305.973776698831));
#17730=CARTESIAN_POINT('Ctrl Pts',(-31.9747135329271,2.34321142110991,305.96874267475));
#17731=CARTESIAN_POINT('Ctrl Pts',(-31.9022475932433,2.28440255899752,305.96370865067));
#17732=CARTESIAN_POINT('Ctrl Pts',(-31.8297674601869,2.22558217842415,305.958673640611));
#17733=CARTESIAN_POINT('Ctrl Pts',(-31.7601078826416,2.16332387908309,305.953638630553));
#17734=CARTESIAN_POINT('Ctrl Pts',(-31.6935996665186,2.09793824848428,305.948603620495));
#17735=CARTESIAN_POINT('Ctrl Pts',(-31.6270183712348,2.03248077222038,305.943563077973));
#17736=CARTESIAN_POINT('Ctrl Pts',(-31.5635956666475,1.96388941735336,305.938522535451));
#17737=CARTESIAN_POINT('Ctrl Pts',(-31.5036247560481,1.89251090543911,305.933481992929));
#17738=CARTESIAN_POINT('Ctrl Pts',(-31.4436170002741,1.82108853970131,305.928438353577));
#17739=CARTESIAN_POINT('Ctrl Pts',(-31.3870655295055,1.7468759609875,305.923394714226));
#17740=CARTESIAN_POINT('Ctrl Pts',(-31.3342212498735,1.67025040492765,305.918351074875));
#17741=CARTESIAN_POINT('Ctrl Pts',(-31.2812914039423,1.59350077554707,305.913299268782));
#17742=CARTESIAN_POINT('Ctrl Pts',(-31.2320809671197,1.5143307455475,305.90824746269));
#17743=CARTESIAN_POINT('Ctrl Pts',(-31.1867956989889,1.43314358521891,305.903195656597));
#17744=CARTESIAN_POINT('Ctrl Pts',(-31.1638726413815,1.39204726339045,305.900638470853));
#17745=CARTESIAN_POINT('Ctrl Pts',(-31.1419545771068,1.35043443778714,305.898081285109));
#17746=CARTESIAN_POINT('Ctrl Pts',(-31.1210634514639,1.30835926337743,305.895524099365));
#17747=CARTESIAN_POINT('Ctrl Pts',(-31.0797885279475,1.22523068354963,305.890471827515));
#17748=CARTESIAN_POINT('Ctrl Pts',(-31.0423770702963,1.13999781791052,305.885419555665));
#17749=CARTESIAN_POINT('Ctrl Pts',(-31.0090487077173,1.05305494505269,305.880367283814));
#17750=CARTESIAN_POINT('Ctrl Pts',(-30.9757663112028,0.966231982727323,
305.875321979995));
#17751=CARTESIAN_POINT('Ctrl Pts',(-30.9465559771828,0.877704110886948,
305.870276676176));
#17752=CARTESIAN_POINT('Ctrl Pts',(-30.9215909612622,0.787889143159898,
305.865231372356));
#17753=CARTESIAN_POINT('Ctrl Pts',(-30.8966526629464,0.698170295572656,
305.86019146803));
#17754=CARTESIAN_POINT('Ctrl Pts',(-30.8759507704791,0.60716751572271,305.855151563704));
#17755=CARTESIAN_POINT('Ctrl Pts',(-30.8596096412037,0.515316450226135,
305.850111659378));
#17756=CARTESIAN_POINT('Ctrl Pts',(-30.8432802910977,0.423531593694662,
305.845075387964));
#17757=CARTESIAN_POINT('Ctrl Pts',(-30.8313055338947,0.330900103028787,
305.840039116549));
#17758=CARTESIAN_POINT('Ctrl Pts',(-30.8237590265882,0.237869544876798,
305.835002845135));
#17759=CARTESIAN_POINT('Ctrl Pts',(-30.8162152633626,0.144872814741193,
305.829968405024));
#17760=CARTESIAN_POINT('Ctrl Pts',(-30.8130965870602,0.05147774775249,305.824933964912));
#17761=CARTESIAN_POINT('Ctrl Pts',(-30.8144248730321,-0.0418622454265086,
305.8198995248));
#17762=CARTESIAN_POINT('Ctrl Pts',(-30.8157530475937,-0.135194409683775,
305.814865506953));
#17763=CARTESIAN_POINT('Ctrl Pts',(-30.8215274363334,-0.228471065105655,
305.809831489107));
#17764=CARTESIAN_POINT('Ctrl Pts',(-30.8317177925861,-0.321239225290878,
305.80479747126));
#17765=CARTESIAN_POINT('Ctrl Pts',(-30.8419101448092,-0.414025555842328,
305.799762467408));
#17766=CARTESIAN_POINT('Ctrl Pts',(-30.8565201334637,-0.50630275182035,
305.794727463556));
#17767=CARTESIAN_POINT('Ctrl Pts',(-30.8754658266925,-0.597624513454089,
305.789692459703));
#17768=CARTESIAN_POINT('Ctrl Pts',(-30.8944323377595,-0.689046620936459,
305.784651923306));
#17769=CARTESIAN_POINT('Ctrl Pts',(-30.9177439728114,-0.77951076278748,
305.779611386909));
#17770=CARTESIAN_POINT('Ctrl Pts',(-30.9452680589654,-0.868582679780679,
305.774570850512));
#17771=CARTESIAN_POINT('Ctrl Pts',(-30.9728090557022,-0.957709321861172,
305.769527217249));
#17772=CARTESIAN_POINT('Ctrl Pts',(-31.0045675048311,-1.04544161878498,
305.764483583985));
#17773=CARTESIAN_POINT('Ctrl Pts',(-31.0403621743289,-1.1313643420492,305.759439950722));
#17774=CARTESIAN_POINT('Ctrl Pts',(-31.0762148040231,-1.21742619490936,
305.754388150601));
#17775=CARTESIAN_POINT('Ctrl Pts',(-31.11611651171,-1.3016722234562,305.74933635048));
#17776=CARTESIAN_POINT('Ctrl Pts',(-31.1598397286161,-1.38371105123071,
305.744284550359));
#17777=CARTESIAN_POINT('Ctrl Pts',(-31.1819726503707,-1.42523953619727,
305.741727302638));
#17778=CARTESIAN_POINT('Ctrl Pts',(-31.2050841090988,-1.46620288694025,
305.739170054917));
#17779=CARTESIAN_POINT('Ctrl Pts',(-31.229140462597,-1.50655332203433,305.736612807196));
#17780=CARTESIAN_POINT('Ctrl Pts',(-31.2766679332513,-1.58627255795134,
305.731560523772));
#17781=CARTESIAN_POINT('Ctrl Pts',(-31.328056785282,-1.66388364639719,305.726508240347));
#17782=CARTESIAN_POINT('Ctrl Pts',(-31.3830945186209,-1.73898841929601,
305.721455956923));
#17783=CARTESIAN_POINT('Ctrl Pts',(-31.4380563444698,-1.81398960844497,
305.716410641558));
#17784=CARTESIAN_POINT('Ctrl Pts',(-31.4966567910936,-1.88649099569085,
305.711365326192));
#17785=CARTESIAN_POINT('Ctrl Pts',(-31.5586384584447,-1.9561206503502,305.706320010826));
#17786=CARTESIAN_POINT('Ctrl Pts',(-31.6205537925266,-2.02567578680408,
305.701280094997));
#17787=CARTESIAN_POINT('Ctrl Pts',(-31.6858428610082,-2.0923649693723,305.696240179168));
#17788=CARTESIAN_POINT('Ctrl Pts',(-31.7542067899118,-2.1558477152417,305.691200263339));
#17789=CARTESIAN_POINT('Ctrl Pts',(-31.8225214386815,-2.21928469957774,
305.686163980532));
#17790=CARTESIAN_POINT('Ctrl Pts',(-31.8939062176371,-2.27951953993609,
305.681127697726));
#17791=CARTESIAN_POINT('Ctrl Pts',(-31.9680247735594,-2.33624791866612,
305.67609141492));
#17792=CARTESIAN_POINT('Ctrl Pts',(-32.0421163772862,-2.39295566889988,
305.671056963489));
#17793=CARTESIAN_POINT('Ctrl Pts',(-32.1189394306651,-2.44615922084135,
305.666022512058));
#17794=CARTESIAN_POINT('Ctrl Pts',(-32.1981246233513,-2.49559462165916,
305.660988060626));
#17795=CARTESIAN_POINT('Ctrl Pts',(-32.2773031730102,-2.54502587522794,
305.655954031547));
#17796=CARTESIAN_POINT('Ctrl Pts',(-32.3588430910346,-2.59068937108095,
305.650920002467));
#17797=CARTESIAN_POINT('Ctrl Pts',(-32.4423471949681,-2.63236520215651,
305.645885973388));
#17798=CARTESIAN_POINT('Ctrl Pts',(-32.5258676530354,-2.67404919537122,
305.640850958403));
#17799=CARTESIAN_POINT('Ctrl Pts',(-32.6113526633519,-2.71174377474132,
305.635815943417));
#17800=CARTESIAN_POINT('Ctrl Pts',(-32.6983826723174,-2.74527610338617,
305.630780928432));
#17801=CARTESIAN_POINT('Ctrl Pts',(-32.7855083072953,-2.7788452763668,305.62574038112));
#17802=CARTESIAN_POINT('Ctrl Pts',(-32.8741819143405,-2.80824290968469,
305.620699833809));
#17803=CARTESIAN_POINT('Ctrl Pts',(-32.9639665807851,-2.83334534256119,
305.615659286497));
#17804=CARTESIAN_POINT('Ctrl Pts',(-33.0538064081832,-2.85846319760482,
305.610615642427));
#17805=CARTESIAN_POINT('Ctrl Pts',(-33.1447582211694,-2.87928049974766,
305.605571998358));
#17806=CARTESIAN_POINT('Ctrl Pts',(-33.2363748058769,-2.89572471593017,
305.600528354288));
#17807=CARTESIAN_POINT('Ctrl Pts',(-33.3281397346472,-2.91219555831628,
305.595476543633));
#17808=CARTESIAN_POINT('Ctrl Pts',(-33.4205711440586,-2.92427912122125,
305.590424732978));
#17809=CARTESIAN_POINT('Ctrl Pts',(-33.5132167756848,-2.93195474225857,
305.585372922323));
#17810=CARTESIAN_POINT('Ctrl Pts',(-33.5601123294462,-2.93584000368633,
305.582815786557));
#17811=CARTESIAN_POINT('Ctrl Pts',(-33.6070627676053,-2.93859669249374,
305.580258650791));
#17812=CARTESIAN_POINT('Ctrl Pts',(-33.6540097105623,-2.94022721129498,
305.577701515026));
#17813=CARTESIAN_POINT('Ctrl Pts',(-33.746765573912,-2.94344872412606,305.572649230027));
#17814=CARTESIAN_POINT('Ctrl Pts',(-33.8398405204643,-2.9422824371313,305.567596945028));
#17815=CARTESIAN_POINT('Ctrl Pts',(-33.9327847446478,-2.93669134404347,
305.562544660029));
#17816=CARTESIAN_POINT('Ctrl Pts',(-34.025600783513,-2.93110796198938,305.557499342959));
#17817=CARTESIAN_POINT('Ctrl Pts',(-34.1182860186593,-2.92111192679462,
305.552454025889));
#17818=CARTESIAN_POINT('Ctrl Pts',(-34.2103883835416,-2.90671818695414,
305.54740870882));
#17819=CARTESIAN_POINT('Ctrl Pts',(-34.3023921820682,-2.89233985104474,
305.542368791161));
#17820=CARTESIAN_POINT('Ctrl Pts',(-34.3938139136144,-2.87357323329236,
305.537328873502));
#17821=CARTESIAN_POINT('Ctrl Pts',(-34.4842054863197,-2.8504851787963,305.532288955843));
#17822=CARTESIAN_POINT('Ctrl Pts',(-34.5745319034569,-2.82741376650773,
305.52725267103));
#17823=CARTESIAN_POINT('Ctrl Pts',(-34.6638292084842,-2.8000272185105,305.522216386218));
#17824=CARTESIAN_POINT('Ctrl Pts',(-34.7516594132438,-2.76844347323014,
305.517180101405));
#17825=CARTESIAN_POINT('Ctrl Pts',(-34.8394576816598,-2.73687121226023,
305.512145647859));
#17826=CARTESIAN_POINT('Ctrl Pts',(-34.9257894919556,-2.70110493606891,
305.507111194314));
#17827=CARTESIAN_POINT('Ctrl Pts',(-35.0102329392263,-2.66131214940086,
305.502076740768));
#17828=CARTESIAN_POINT('Ctrl Pts',(-35.0946693041096,-2.62152270020831,
305.497042709468));
#17829=CARTESIAN_POINT('Ctrl Pts',(-35.1772172190718,-2.57770760152444,
305.492008678169));
#17830=CARTESIAN_POINT('Ctrl Pts',(-35.2574767108073,-2.53008164328739,
305.48697464687));
#17831=CARTESIAN_POINT('Ctrl Pts',(-35.3377519228428,-2.48244635662909,
305.481939629562));
#17832=CARTESIAN_POINT('Ctrl Pts',(-35.4157374396239,-2.43099895502573,
305.476904612255));
#17833=CARTESIAN_POINT('Ctrl Pts',(-35.4910607411503,-2.37599852724254,
305.471869594948));
#17834=CARTESIAN_POINT('Ctrl Pts',(-35.5664668077397,-2.32093766512127,
305.466829045176));
#17835=CARTESIAN_POINT('Ctrl Pts',(-35.6392044606158,-2.2623162462482,305.461788495404));
#17836=CARTESIAN_POINT('Ctrl Pts',(-35.7089331178811,-2.20043458539732,
305.456747945632));
#17837=CARTESIAN_POINT('Ctrl Pts',(-35.7787046154201,-2.13851490535329,
305.451704299019));
#17838=CARTESIAN_POINT('Ctrl Pts',(-35.8454631193548,-2.07333130579444,
305.446660652407));
#17839=CARTESIAN_POINT('Ctrl Pts',(-35.9089054489725,-2.00522045131894,
305.441617005794));
#17840=CARTESIAN_POINT('Ctrl Pts',(-35.9724505045914,-1.93699931155341,
305.436565192495));
#17841=CARTESIAN_POINT('Ctrl Pts',(-36.032668379603,-1.86584179309872,305.431513379195));
#17842=CARTESIAN_POINT('Ctrl Pts',(-36.0892967659652,-1.79211689380081,
305.426461565895));
#17843=CARTESIAN_POINT('Ctrl Pts',(-36.1179607823449,-1.75479900683956,
305.423904451549));
#17844=CARTESIAN_POINT('Ctrl Pts',(-36.1457058122861,-1.71682376995429,
305.421347337203));
#17845=CARTESIAN_POINT('Ctrl Pts',(-36.1725022585399,-1.67824155948422,
305.418790222857));
#17846=CARTESIAN_POINT('Ctrl Pts',(-36.226108056709,-1.60105855664165,305.413674762611));
#17847=CARTESIAN_POINT('Ctrl Pts',(-36.2761046912628,-1.52117167573944,
305.408559302366));
#17848=CARTESIAN_POINT('Ctrl Pts',(-36.3222123092792,-1.43894764155196,
305.40344384212));
#17849=CARTESIAN_POINT('Ctrl Pts',(-36.3682523754555,-1.35684407302804,
305.398335876487));
#17850=CARTESIAN_POINT('Ctrl Pts',(-36.4104145423665,-1.27241052870167,
305.393227910855));
#17851=CARTESIAN_POINT('Ctrl Pts',(-36.4484613602111,-1.18604377188642,
305.388119945222));
#17852=CARTESIAN_POINT('Ctrl Pts',(-36.4864621471144,-1.09978150588898,
305.383018159461));
#17853=CARTESIAN_POINT('Ctrl Pts',(-36.5203573121079,-1.01159106855782,
305.377916373701));
#17854=CARTESIAN_POINT('Ctrl Pts',(-36.5499550823211,-0.921894130345155,
305.37281458794));
#17855=CARTESIAN_POINT('Ctrl Pts',(-36.5795207165609,-0.832294581172113,
305.367718341477));
#17856=CARTESIAN_POINT('Ctrl Pts',(-36.6047981081081,-0.741192193038616,
305.362622095014));
#17857=CARTESIAN_POINT('Ctrl Pts',(-36.6256438502739,-0.649027881487562,
305.357525848551));
#17858=CARTESIAN_POINT('Ctrl Pts',(-36.6464764407366,-0.556921716950648,
305.35243281734));
#17859=CARTESIAN_POINT('Ctrl Pts',(-36.6628828474354,-0.463755379522535,
305.347339786129));
#17860=CARTESIAN_POINT('Ctrl Pts',(-36.6747698928038,-0.369983528987202,
305.342246754918));
#17861=CARTESIAN_POINT('Ctrl Pts',(-36.686652822147,-0.276244148025949,
305.337155487227));
#17862=CARTESIAN_POINT('Ctrl Pts',(-36.6940194483778,-0.181900096871285,
305.332064219537));
#17863=CARTESIAN_POINT('Ctrl Pts',(-36.6968281006551,-0.0874138727897526,
305.326972951846));
#17864=CARTESIAN_POINT('Ctrl Pts',(-36.6977101757216,-0.0577398746709374,
305.325374006927));
#17865=CARTESIAN_POINT('Ctrl Pts',(-36.6981430762226,-0.0280518897877842,
305.323775062009));
#17866=CARTESIAN_POINT('Ctrl Pts',(-36.6981265705531,0.00163568983778872,
305.32217611709));
#17867=CARTESIAN_POINT('',(-36.6981264963869,0.00176405078021327,304.322176117128));
#17868=CARTESIAN_POINT('Ctrl Pts',(-36.6981265705527,0.00163569045731642,
305.322176117057));
#17869=CARTESIAN_POINT('Ctrl Pts',(-36.6980687822406,0.105575398122983,
305.316578022853));
#17870=CARTESIAN_POINT('Ctrl Pts',(-36.6924986516524,0.20931837606196,305.310979928649));
#17871=CARTESIAN_POINT('Ctrl Pts',(-36.6815031459867,0.312311626854009,
305.305381834446));
#17872=CARTESIAN_POINT('Ctrl Pts',(-36.6704676688315,0.415679284586532,
305.299763389731));
#17873=CARTESIAN_POINT('Ctrl Pts',(-36.6539674239736,0.518291508928275,
305.294144945016));
#17874=CARTESIAN_POINT('Ctrl Pts',(-36.6321402925598,0.619606073486603,
305.288526500301));
#17875=CARTESIAN_POINT('Ctrl Pts',(-36.6102032420979,0.721430847119007,
305.282879761712));
#17876=CARTESIAN_POINT('Ctrl Pts',(-36.5828856408373,0.821944618092324,
305.277233023124));
#17877=CARTESIAN_POINT('Ctrl Pts',(-36.5503759963964,0.920617557561025,
305.271586284535));
#17878=CARTESIAN_POINT('Ctrl Pts',(-36.52790863729,0.988810255551313,305.267683833253));
#17879=CARTESIAN_POINT('Ctrl Pts',(-36.5029624841091,1.0561241721974,305.26378138197));
#17880=CARTESIAN_POINT('Ctrl Pts',(-36.4756127117875,1.12239101954654,305.259878930687));
#17881=CARTESIAN_POINT('Ctrl Pts',(-36.4402040385224,1.20818409740135,305.254826580679));
#17882=CARTESIAN_POINT('Ctrl Pts',(-36.4006679936895,1.29245392580459,305.249774230672));
#17883=CARTESIAN_POINT('Ctrl Pts',(-36.3571568190445,1.37477562235905,305.244721880664));
#17884=CARTESIAN_POINT('Ctrl Pts',(-36.3137056557643,1.45698377940559,305.239676498945));
#17885=CARTESIAN_POINT('Ctrl Pts',(-36.2662904630271,1.53724875446474,305.234631117226));
#17886=CARTESIAN_POINT('Ctrl Pts',(-36.2151117253316,1.61516508283266,305.229585735506));
#17887=CARTESIAN_POINT('Ctrl Pts',(-36.1639877620064,1.69299802075333,305.224545753639));
#17888=CARTESIAN_POINT('Ctrl Pts',(-36.1091085024822,1.76848693894027,305.219505771772));
#17889=CARTESIAN_POINT('Ctrl Pts',(-36.0507200434947,1.84125144416985,305.214465789905));
#17890=CARTESIAN_POINT('Ctrl Pts',(-35.9923736818115,1.91396348715653,305.209429441798));
#17891=CARTESIAN_POINT('Ctrl Pts',(-35.9305234268017,1.98395467595569,305.204393093691));
#17892=CARTESIAN_POINT('Ctrl Pts',(-35.8654577225004,2.05087493759837,305.199356745583));
#17893=CARTESIAN_POINT('Ctrl Pts',(-35.80041568435,2.11777085853768,305.194322229332));
#17894=CARTESIAN_POINT('Ctrl Pts',(-35.7321608297071,2.18159775313175,305.18928771308));
#17895=CARTESIAN_POINT('Ctrl Pts',(-35.6610200879099,2.24204068202593,305.184253196829));
#17896=CARTESIAN_POINT('Ctrl Pts',(-35.5898853220741,2.30247853359578,305.179219103487));
#17897=CARTESIAN_POINT('Ctrl Pts',(-35.5158654897394,2.35953269714093,305.174185010144));
#17898=CARTESIAN_POINT('Ctrl Pts',(-35.439321511082,2.4129277492064,305.169150916802));
#17899=CARTESIAN_POINT('Ctrl Pts',(-35.3627625512686,2.46633325172957,305.164115838189));
#17900=CARTESIAN_POINT('Ctrl Pts',(-35.28367882854,2.51607796663302,305.159080759576));
#17901=CARTESIAN_POINT('Ctrl Pts',(-35.202460252322,2.5619297797343,305.154045680963));
#17902=CARTESIAN_POINT('Ctrl Pts',(-35.1211524583318,2.60783196058155,305.149005071368));
#17903=CARTESIAN_POINT('Ctrl Pts',(-35.0377055171747,2.64983248486244,305.143964461773));
#17904=CARTESIAN_POINT('Ctrl Pts',(-34.952533675687,2.68774536122904,305.138923852178));
#17905=CARTESIAN_POINT('Ctrl Pts',(-34.8673095192103,2.72568152477222,305.133880146495));
#17906=CARTESIAN_POINT('Ctrl Pts',(-34.7803587668598,2.7595248809654,305.128836440813));
#17907=CARTESIAN_POINT('Ctrl Pts',(-34.6921133049353,2.78913852009093,305.123792735131));
#17908=CARTESIAN_POINT('Ctrl Pts',(-34.6037249878439,2.81880009892089,305.118740864503));
#17909=CARTESIAN_POINT('Ctrl Pts',(-34.5140382037932,2.84421817004464,305.113688993875));
#17910=CARTESIAN_POINT('Ctrl Pts',(-34.4234973861619,2.86530640619576,305.108637123247));
#17911=CARTESIAN_POINT('Ctrl Pts',(-34.3776792810693,2.87597809047547,305.106080628337));
#17912=CARTESIAN_POINT('Ctrl Pts',(-34.3316425948253,2.88554178733248,305.103524133428));
#17913=CARTESIAN_POINT('Ctrl Pts',(-34.2854453897896,2.89399137334049,305.100967638519));
#17914=CARTESIAN_POINT('Ctrl Pts',(-34.1941472619466,2.91069003255554,305.095915315573));
#17915=CARTESIAN_POINT('Ctrl Pts',(-34.1018943172055,2.92309408399761,305.090862992627));
#17916=CARTESIAN_POINT('Ctrl Pts',(-34.0091261817993,2.9311014016559,305.08581066968));
#17917=CARTESIAN_POINT('Ctrl Pts',(-33.9164859724032,2.93909767733092,305.080765313819));
#17918=CARTESIAN_POINT('Ctrl Pts',(-33.8233324228397,2.94270922938106,305.075719957959));
#17919=CARTESIAN_POINT('Ctrl Pts',(-33.7301149631016,2.94188500329676,305.070674602098));
#17920=CARTESIAN_POINT('Ctrl Pts',(-33.6369972479132,2.94106165915089,305.065634644869));
#17921=CARTESIAN_POINT('Ctrl Pts',(-33.543816200319,2.93581197491237,305.06059468764));
#17922=CARTESIAN_POINT('Ctrl Pts',(-33.4510248765455,2.92613681820438,305.055554730411));
#17923=CARTESIAN_POINT('Ctrl Pts',(-33.3583004195325,2.91646863355327,305.050518405047));
#17924=CARTESIAN_POINT('Ctrl Pts',(-33.2659655687111,2.90238136107195,305.045482079684));
#17925=CARTESIAN_POINT('Ctrl Pts',(-33.1744708260699,2.88392788847893,305.04044575432));
#17926=CARTESIAN_POINT('Ctrl Pts',(-33.0830093412368,2.86548112361612,305.035411259632));
#17927=CARTESIAN_POINT('Ctrl Pts',(-32.9923877929635,2.84267139930572,305.030376764943));
#17928=CARTESIAN_POINT('Ctrl Pts',(-32.9030479908327,2.8156029835587,305.025342270255));
#17929=CARTESIAN_POINT('Ctrl Pts',(-32.8137156721683,2.78853683517266,305.020308197276));
#17930=CARTESIAN_POINT('Ctrl Pts',(-32.725665311288,2.75721283359567,305.015274124297));
#17931=CARTESIAN_POINT('Ctrl Pts',(-32.6393239072545,2.72178522216918,305.010240051319));
#17932=CARTESIAN_POINT('Ctrl Pts',(-32.5529655835358,2.68635066825618,305.00520499185));
#17933=CARTESIAN_POINT('Ctrl Pts',(-32.4683172925889,2.64681107641035,305.000169932382));
#17934=CARTESIAN_POINT('Ctrl Pts',(-32.385785325272,2.6033685150744,304.995134872913));
#17935=CARTESIAN_POINT('Ctrl Pts',(-32.3031626651733,2.55987821554846,304.990094280515));
#17936=CARTESIAN_POINT('Ctrl Pts',(-32.2226613645728,2.51247659262798,304.985053688117));
#17937=CARTESIAN_POINT('Ctrl Pts',(-32.1446621217005,2.46141115309973,304.980013095719));
#17938=CARTESIAN_POINT('Ctrl Pts',(-32.0666149525732,2.41031433666084,304.974969406153));
#17939=CARTESIAN_POINT('Ctrl Pts',(-31.9910732611988,2.35554948244164,304.969925716588));
#17940=CARTESIAN_POINT('Ctrl Pts',(-31.9183860381808,2.29740550717932,304.964882027022));
#17941=CARTESIAN_POINT('Ctrl Pts',(-31.8455811196529,2.23916738490559,304.95983017069));
#17942=CARTESIAN_POINT('Ctrl Pts',(-31.7756402295717,2.1775395117591,304.954778314357));
#17943=CARTESIAN_POINT('Ctrl Pts',(-31.7088766314584,2.11284874638222,304.949726458025));
#17944=CARTESIAN_POINT('Ctrl Pts',(-31.6750881109795,2.08010926989354,304.947169754133));
#17945=CARTESIAN_POINT('Ctrl Pts',(-31.6421127640942,2.04658584750536,304.944613050241));
#17946=CARTESIAN_POINT('Ctrl Pts',(-31.6099871925103,2.01232398442582,304.942056346349));
#17947=CARTESIAN_POINT('Ctrl Pts',(-31.546509622489,1.94462527260648,304.937004503149));
#17948=CARTESIAN_POINT('Ctrl Pts',(-31.4861244092015,1.8737984283578,304.93195265995));
#17949=CARTESIAN_POINT('Ctrl Pts',(-31.4291554856856,1.80015761921618,304.92690081675));
#17950=CARTESIAN_POINT('Ctrl Pts',(-31.3722651506293,1.72661839735042,304.921855942554));
#17951=CARTESIAN_POINT('Ctrl Pts',(-31.3187820100551,1.65027327269262,304.916811068357));
#17952=CARTESIAN_POINT('Ctrl Pts',(-31.2689923786189,1.57147231903376,304.91176619416));
#17953=CARTESIAN_POINT('Ctrl Pts',(-31.2192560404307,1.49275571142532,304.906726719837));
#17954=CARTESIAN_POINT('Ctrl Pts',(-31.1732055894753,1.41158887323433,304.901687245514));
#17955=CARTESIAN_POINT('Ctrl Pts',(-31.1310856598489,1.32835305167465,304.896647771191));
#17956=CARTESIAN_POINT('Ctrl Pts',(-31.0889960839191,1.2451772139491,304.891611928562));
#17957=CARTESIAN_POINT('Ctrl Pts',(-31.0508315993594,1.15993575175802,304.886576085933));
#17958=CARTESIAN_POINT('Ctrl Pts',(-31.0167917289375,1.07303594270398,304.881540243303));
#17959=CARTESIAN_POINT('Ctrl Pts',(-30.9827642310606,0.986167719310951,
304.876506231062));
#17960=CARTESIAN_POINT('Ctrl Pts',(-30.9528585309551,0.897642759815976,
304.871472218822));
#17961=CARTESIAN_POINT('Ctrl Pts',(-30.9272262524522,0.807888864647229,
304.866438206581));
#17962=CARTESIAN_POINT('Ctrl Pts',(-30.9015961167322,0.718142472639308,
304.861404615168));
#17963=CARTESIAN_POINT('Ctrl Pts',(-30.8802388141739,0.627167776529021,
304.856371023756));
#17964=CARTESIAN_POINT('Ctrl Pts',(-30.8632559364977,0.535407194401948,
304.851337432344));
#17965=CARTESIAN_POINT('Ctrl Pts',(-30.8462697255113,0.443628601988464,
304.846302852965));
#17966=CARTESIAN_POINT('Ctrl Pts',(-30.833659725059,0.351064254181437,304.841268273586));
#17967=CARTESIAN_POINT('Ctrl Pts',(-30.8254761077667,0.258165063107938,
304.836233694206));
#17968=CARTESIAN_POINT('Ctrl Pts',(-30.8172834884007,0.165163681850032,
304.831193576732));
#17969=CARTESIAN_POINT('Ctrl Pts',(-30.8135270104799,0.071827165406105,
304.826153459257));
#17970=CARTESIAN_POINT('Ctrl Pts',(-30.8142047884544,-0.0213904792602384,
304.821113341782));
#17971=CARTESIAN_POINT('Ctrl Pts',(-30.8148829832253,-0.114665447679882,
304.816070124911));
#17972=CARTESIAN_POINT('Ctrl Pts',(-30.820000838066,-0.207820955455111,
304.81102690804));
#17973=CARTESIAN_POINT('Ctrl Pts',(-30.8295044839954,-0.300407225238978,
304.805983691168));
#17974=CARTESIAN_POINT('Ctrl Pts',(-30.8390235349569,-0.393143573684762,
304.800932299443));
#17975=CARTESIAN_POINT('Ctrl Pts',(-30.8529425033414,-0.485308403255275,
304.795880907718));
#17976=CARTESIAN_POINT('Ctrl Pts',(-30.8711562754231,-0.576461423340376,
304.790829515992));
#17977=CARTESIAN_POINT('Ctrl Pts',(-30.880392214324,-0.622683793992275,
304.788268028722));
#17978=CARTESIAN_POINT('Ctrl Pts',(-30.8907316985239,-0.668646219021566,
304.785706541451));
#17979=CARTESIAN_POINT('Ctrl Pts',(-30.90215618544,-0.714292968935603,304.78314505418));
#17980=CARTESIAN_POINT('Ctrl Pts',(-30.9246933650259,-0.804340689054872,
304.77809198711));
#17981=CARTESIAN_POINT('Ctrl Pts',(-30.9515368623356,-0.893482143182679,
304.77303892004));
#17982=CARTESIAN_POINT('Ctrl Pts',(-30.982597877132,-0.981274714082561,
304.76798585297));
#17983=CARTESIAN_POINT('Ctrl Pts',(-31.0136160475477,-1.06894618725381,
304.762939755908));
#17984=CARTESIAN_POINT('Ctrl Pts',(-31.0488400284389,-1.15527205942261,
304.757893658847));
#17985=CARTESIAN_POINT('Ctrl Pts',(-31.0881304644289,-1.2398219030998,304.752847561785));
#17986=CARTESIAN_POINT('Ctrl Pts',(-31.1273788348419,-1.32428122505439,
304.747806867233));
#17987=CARTESIAN_POINT('Ctrl Pts',(-31.1706848205516,-1.40696789742434,
304.742766172682));
#17988=CARTESIAN_POINT('Ctrl Pts',(-31.2178602900946,-1.487469657225,304.73772547813));
#17989=CARTESIAN_POINT('Ctrl Pts',(-31.2650016873628,-1.56791327498474,
304.732688424198));
#17990=CARTESIAN_POINT('Ctrl Pts',(-31.3160067895996,-1.64617473474176,
304.727651370266));
#17991=CARTESIAN_POINT('Ctrl Pts',(-31.3706411549913,-1.72186560531297,
304.722614316334));
#17992=CARTESIAN_POINT('Ctrl Pts',(-31.4252556022491,-1.79752888114809,
304.717579098768));
#17993=CARTESIAN_POINT('Ctrl Pts',(-31.4834964244442,-1.87062306985752,
304.712543881203));
#17994=CARTESIAN_POINT('Ctrl Pts',(-31.5450859880084,-1.94078889413562,
304.707508663637));
#17995=CARTESIAN_POINT('Ctrl Pts',(-31.6066703131885,-2.01094875059188,
304.702473874332));
#17996=CARTESIAN_POINT('Ctrl Pts',(-31.671602520337,-2.07818040417835,304.697439085027));
#17997=CARTESIAN_POINT('Ctrl Pts',(-31.739565591196,-2.14215872022952,304.692404295722));
#17998=CARTESIAN_POINT('Ctrl Pts',(-31.8075418782633,-2.20614947760719,
304.687368527345));
#17999=CARTESIAN_POINT('Ctrl Pts',(-31.8785498759646,-2.26688533688328,
304.682332758967));
#18000=CARTESIAN_POINT('Ctrl Pts',(-31.9522375755747,-2.32407978635046,
304.677296990589));
#18001=CARTESIAN_POINT('Ctrl Pts',(-32.0260060111398,-2.38133690093709,
304.672255704769));
#18002=CARTESIAN_POINT('Ctrl Pts',(-32.1024596578963,-2.4350445877322,304.66721441895));
#18003=CARTESIAN_POINT('Ctrl Pts',(-32.1812157087587,-2.48495841920214,
304.66217313313));
#18004=CARTESIAN_POINT('Ctrl Pts',(-32.2600200228257,-2.53490283881662,
304.657128757915));
#18005=CARTESIAN_POINT('Ctrl Pts',(-32.341129164255,-2.58104855506556,304.6520843827));
#18006=CARTESIAN_POINT('Ctrl Pts',(-32.4241357195483,-2.62319712593525,
304.647040007484));
#18007=CARTESIAN_POINT('Ctrl Pts',(-32.5072763533554,-2.66541377838859,
304.64198748421));
#18008=CARTESIAN_POINT('Ctrl Pts',(-32.5923201150392,-2.70362021404384,
304.636934960935));
#18009=CARTESIAN_POINT('Ctrl Pts',(-32.6788398043432,-2.73766620384124,
304.631882437661));
#18010=CARTESIAN_POINT('Ctrl Pts',(-32.7224985866249,-2.75484618296607,
304.629332879111));
#18011=CARTESIAN_POINT('Ctrl Pts',(-32.7665329455022,-2.77096757030336,
304.626783320561));
#18012=CARTESIAN_POINT('Ctrl Pts',(-32.8108867998765,-2.78601595765738,
304.624233762011));
#18013=CARTESIAN_POINT('Ctrl Pts',(-32.8987820482044,-2.8158370805806,304.619181346949));
#18014=CARTESIAN_POINT('Ctrl Pts',(-32.9882474431162,-2.84154809940506,
304.614128931887));
#18015=CARTESIAN_POINT('Ctrl Pts',(-33.0788628772053,-2.86298398070318,
304.609076516826));
#18016=CARTESIAN_POINT('Ctrl Pts',(-33.1693534986685,-2.88439033647221,
304.604031060901));
#18017=CARTESIAN_POINT('Ctrl Pts',(-33.260990583047,-2.90153315461889,304.598985604975));
#18018=CARTESIAN_POINT('Ctrl Pts',(-33.3533368915402,-2.91429650313414,
304.59394014905));
#18019=CARTESIAN_POINT('Ctrl Pts',(-33.4455845304219,-2.92704621434587,
304.588900084063));
#18020=CARTESIAN_POINT('Ctrl Pts',(-33.5385394495211,-2.93542569637416,
304.583860019075));
#18021=CARTESIAN_POINT('Ctrl Pts',(-33.631753266253,-2.93936985901248,304.578819954088));
#18022=CARTESIAN_POINT('Ctrl Pts',(-33.72490011394,-2.943311187985,304.573783510112));
#18023=CARTESIAN_POINT('Ctrl Pts',(-33.8183050470046,-2.94282351250116,
304.568747066137));
#18024=CARTESIAN_POINT('Ctrl Pts',(-33.9115146381822,-2.93789358039899,
304.563710622161));
#18025=CARTESIAN_POINT('Ctrl Pts',(-34.0046904724401,-2.93296543372813,
304.558676002191));
#18026=CARTESIAN_POINT('Ctrl Pts',(-34.0976706622015,-2.92359824996414,
304.553641382221));
#18027=CARTESIAN_POINT('Ctrl Pts',(-34.1900029021185,-2.90983087540809,
304.548606762251));
#18028=CARTESIAN_POINT('Ctrl Pts',(-34.2823275267241,-2.89606463634755,
304.543572557523));
#18029=CARTESIAN_POINT('Ctrl Pts',(-34.3740038684061,-2.87789899375566,
304.538538352795));
#18030=CARTESIAN_POINT('Ctrl Pts',(-34.4645870007847,-2.85542439281381,
304.533504148067));
#18031=CARTESIAN_POINT('Ctrl Pts',(-34.5551879964678,-2.83294535980355,
304.528468950577));
#18032=CARTESIAN_POINT('Ctrl Pts',(-34.6446949236627,-2.80615578816217,
304.523433753086));
#18033=CARTESIAN_POINT('Ctrl Pts',(-34.7326763824026,-2.77519645305691,
304.518398555595));
#18034=CARTESIAN_POINT('Ctrl Pts',(-34.8207546691694,-2.74420304564398,
304.513357816616));
#18035=CARTESIAN_POINT('Ctrl Pts',(-34.9073037166122,-2.70903086219687,
304.508317077637));
#18036=CARTESIAN_POINT('Ctrl Pts',(-34.9919108299709,-2.66986935785409,
304.503276338658));
#18037=CARTESIAN_POINT('Ctrl Pts',(-35.0765700134753,-2.63068375216623,
304.498232497434));
#18038=CARTESIAN_POINT('Ctrl Pts',(-35.1592844901276,-2.5875041432499,304.49318865621));
#18039=CARTESIAN_POINT('Ctrl Pts',(-35.2396669071173,-2.54056557068138,
304.488144814986));
#18040=CARTESIAN_POINT('Ctrl Pts',(-35.3201795764497,-2.4935509384562,304.483092800679));
#18041=CARTESIAN_POINT('Ctrl Pts',(-35.3983522699958,-2.44276542423807,
304.478040786372));
#18042=CARTESIAN_POINT('Ctrl Pts',(-35.4738274576828,-2.38848680642084,
304.472988772065));
#18043=CARTESIAN_POINT('Ctrl Pts',(-35.512004678629,-2.36103133597326,304.47043333799));
#18044=CARTESIAN_POINT('Ctrl Pts',(-35.5494922554282,-2.33268275877039,
304.467877903916));
#18045=CARTESIAN_POINT('Ctrl Pts',(-35.586247416328,-2.30348070410589,304.465322469841));
#18046=CARTESIAN_POINT('Ctrl Pts',(-35.6579640035599,-2.24650172076255,
304.460336312625));
#18047=CARTESIAN_POINT('Ctrl Pts',(-35.7271624638713,-2.18605451410487,
304.455350155409));
#18048=CARTESIAN_POINT('Ctrl Pts',(-35.7934814879079,-2.1223927048308,304.450363998194));
#18049=CARTESIAN_POINT('Ctrl Pts',(-35.8597084827952,-2.05881923735966,
304.445384760136));
#18050=CARTESIAN_POINT('Ctrl Pts',(-35.9230636498218,-1.99204033925046,
304.440405522078));
#18051=CARTESIAN_POINT('Ctrl Pts',(-35.9832171786362,-1.92235102120401,
304.43542628402));
#18052=CARTESIAN_POINT('Ctrl Pts',(-36.0433021744706,-1.85274110027249,
304.430452718814));
#18053=CARTESIAN_POINT('Ctrl Pts',(-36.1001924846239,-1.7802276933431,304.425479153607));
#18054=CARTESIAN_POINT('Ctrl Pts',(-36.1535947455384,-1.70514296474278,
304.420505588401));
#18055=CARTESIAN_POINT('Ctrl Pts',(-36.2069639779374,-1.63010467494626,
304.415535099271));
#18056=CARTESIAN_POINT('Ctrl Pts',(-36.2568491791805,-1.55249859148548,
304.410564610142));
#18057=CARTESIAN_POINT('Ctrl Pts',(-36.3029975866806,-1.47268949319156,
304.405594121013));
#18058=CARTESIAN_POINT('Ctrl Pts',(-36.3491311627868,-1.39290604432389,
304.400625229323));
#18059=CARTESIAN_POINT('Ctrl Pts',(-36.3915301017078,-1.31092138203121,
304.395656337633));
#18060=CARTESIAN_POINT('Ctrl Pts',(-36.4299859857538,-1.22712764591723,
304.390687445943));
#18061=CARTESIAN_POINT('Ctrl Pts',(-36.4684409351638,-1.14333594633526,
304.385718675017));
#18062=CARTESIAN_POINT('Ctrl Pts',(-36.5029528313446,-1.05773567643545,
304.380749904092));
#18063=CARTESIAN_POINT('Ctrl Pts',(-36.5333606476721,-0.970740648438338,
304.375781133166));
#18064=CARTESIAN_POINT('Ctrl Pts',(-36.563793940195,-0.883672734499373,
304.370808199318));
#18065=CARTESIAN_POINT('Ctrl Pts',(-36.5901161366452,-0.795208161451882,
304.36583526547));
#18066=CARTESIAN_POINT('Ctrl Pts',(-36.6122157250354,-0.705777117085485,
304.360862331623));
#18067=CARTESIAN_POINT('Ctrl Pts',(-36.6343253241258,-0.616305562128438,
304.355887145129));
#18068=CARTESIAN_POINT('Ctrl Pts',(-36.6522084192237,-0.525867112738204,
304.350911958635));
#18069=CARTESIAN_POINT('Ctrl Pts',(-36.6658048340246,-0.43490119471985,
304.345936772141));
#18070=CARTESIAN_POINT('Ctrl Pts',(-36.6794212809244,-0.34380125326306,
304.340954255521));
#18071=CARTESIAN_POINT('Ctrl Pts',(-36.6887383934852,-0.252172746146416,
304.335971738902));
#18072=CARTESIAN_POINT('Ctrl Pts',(-36.693747993094,-0.16045887114041,304.330989222282));
#18073=CARTESIAN_POINT('Ctrl Pts',(-36.6967016629967,-0.106384187850478,
304.328051520564));
#18074=CARTESIAN_POINT('Ctrl Pts',(-36.6981589016092,-0.0522798282133653,
304.325113818846));
#18075=CARTESIAN_POINT('Ctrl Pts',(-36.6981264963869,0.00176405078021291,
304.322176117128));
#18076=CARTESIAN_POINT('',(-32.4661441993221,2.64410822562003,304.000000575692));
#18077=CARTESIAN_POINT('Ctrl Pts',(-36.6981264963864,0.00176405147736488,
304.32217611709));
#18078=CARTESIAN_POINT('Ctrl Pts',(-36.6980685296926,0.098438091249218,
304.316921137284));
#18079=CARTESIAN_POINT('Ctrl Pts',(-36.6932458848664,0.194972500880357,
304.311666157478));
#18080=CARTESIAN_POINT('Ctrl Pts',(-36.6836973150382,0.291026112907725,
304.306411177672));
#18081=CARTESIAN_POINT('Ctrl Pts',(-36.6745022247276,0.383523906099266,
304.30135073252));
#18082=CARTESIAN_POINT('Ctrl Pts',(-36.6609028368121,0.475748978558183,
304.296290287368));
#18083=CARTESIAN_POINT('Ctrl Pts',(-36.6429231820279,0.56724945945851,304.291229842216));
#18084=CARTESIAN_POINT('Ctrl Pts',(-36.6249683274534,0.658623729309089,
304.286176377181));
#18085=CARTESIAN_POINT('Ctrl Pts',(-36.6026452976773,0.749274963134519,
304.281122912146));
#18086=CARTESIAN_POINT('Ctrl Pts',(-36.5760299087034,0.838756059849511,
304.276069447112));
#18087=CARTESIAN_POINT('Ctrl Pts',(-36.5494430792957,0.928141139131874,
304.271021404683));
#18088=CARTESIAN_POINT('Ctrl Pts',(-36.5185731718854,1.01635815514199,304.265973362255));
#18089=CARTESIAN_POINT('Ctrl Pts',(-36.483546892717,1.10297092735386,304.260925319826));
#18090=CARTESIAN_POINT('Ctrl Pts',(-36.4485462929598,1.18952019967226,304.255880978355));
#18091=CARTESIAN_POINT('Ctrl Pts',(-36.4093955445818,1.27446715704452,304.250836636883));
#18092=CARTESIAN_POINT('Ctrl Pts',(-36.3662706263333,1.35739249363027,304.245792295412));
#18093=CARTESIAN_POINT('Ctrl Pts',(-36.3231617525194,1.44028697821212,304.240749830665));
#18094=CARTESIAN_POINT('Ctrl Pts',(-36.276081850531,1.52116094401507,304.235707365919));
#18095=CARTESIAN_POINT('Ctrl Pts',(-36.2252538677438,1.5996176529765,304.230664901173));
#18096=CARTESIAN_POINT('Ctrl Pts',(-36.1744306986924,1.67806693158478,304.22562291398));
#18097=CARTESIAN_POINT('Ctrl Pts',(-36.1198603954981,1.75409903712175,304.220580926787));
#18098=CARTESIAN_POINT('Ctrl Pts',(-36.0618098429471,1.82734527230395,304.215538939594));
#18099=CARTESIAN_POINT('Ctrl Pts',(-36.0037486888104,1.90060488421044,304.2104960316));
#18100=CARTESIAN_POINT('Ctrl Pts',(-35.9422062982593,1.97107726861895,304.205453123605));
#18101=CARTESIAN_POINT('Ctrl Pts',(-35.8774898113599,2.03842682717338,304.20041021561));
#18102=CARTESIAN_POINT('Ctrl Pts',(-35.8127042051563,2.10584831723789,304.195361921627));
#18103=CARTESIAN_POINT('Ctrl Pts',(-35.7447380426834,2.1701400039321,304.190313627643));
#18104=CARTESIAN_POINT('Ctrl Pts',(-35.6739350791312,2.23100342189282,304.185265333659));
#18105=CARTESIAN_POINT('Ctrl Pts',(-35.6030896928956,2.29190330710553,304.180214014913));
#18106=CARTESIAN_POINT('Ctrl Pts',(-35.5294044701116,2.34937056151589,304.175162696166));
#18107=CARTESIAN_POINT('Ctrl Pts',(-35.4532542564075,2.40314859326042,304.170111377419));
#18108=CARTESIAN_POINT('Ctrl Pts',(-35.3769837305676,2.45701159062149,304.165052077934));
#18109=CARTESIAN_POINT('Ctrl Pts',(-35.2982408115342,2.50717349092762,304.159992778449));
#18110=CARTESIAN_POINT('Ctrl Pts',(-35.2174269911309,2.55342248947147,304.154933478964));
#18111=CARTESIAN_POINT('Ctrl Pts',(-35.1778472635012,2.57607359984317,304.152455614477));
#18112=CARTESIAN_POINT('Ctrl Pts',(-35.1377711312594,2.59778684433811,304.14997774999));
#18113=CARTESIAN_POINT('Ctrl Pts',(-35.0972474845098,2.61854156235396,304.147499885503));
#18114=CARTESIAN_POINT('Ctrl Pts',(-35.0155248361917,2.66039689022785,304.142502861191));
#18115=CARTESIAN_POINT('Ctrl Pts',(-34.9316801408628,2.6985049312846,304.137505836878));
#18116=CARTESIAN_POINT('Ctrl Pts',(-34.8460959220293,2.73264190922819,304.132508812566));
#18117=CARTESIAN_POINT('Ctrl Pts',(-34.7606286011108,2.76673226009962,304.127518613597));
#18118=CARTESIAN_POINT('Ctrl Pts',(-34.6734268941707,2.7968621534048,304.122528414629));
#18119=CARTESIAN_POINT('Ctrl Pts',(-34.5848978326186,2.82285368888757,304.11753821566));
#18120=CARTESIAN_POINT('Ctrl Pts',(-34.4964665348272,2.8488165215895,304.112553527431));
#18121=CARTESIAN_POINT('Ctrl Pts',(-34.4067112296767,2.87064995180145,304.107568839202));
#18122=CARTESIAN_POINT('Ctrl Pts',(-34.3160575921275,2.8882246727505,304.102584150973));
#18123=CARTESIAN_POINT('Ctrl Pts',(-34.2254585176852,2.90578881573044,304.097602462956));
#18124=CARTESIAN_POINT('Ctrl Pts',(-34.1339626294416,2.91909925134569,304.092620774938));
#18125=CARTESIAN_POINT('Ctrl Pts',(-34.0420084006083,2.92807715732144,304.087639086921));
#18126=CARTESIAN_POINT('Ctrl Pts',(-33.9500824386787,2.93705230347192,304.082658930284));
#18127=CARTESIAN_POINT('Ctrl Pts',(-33.8576988683455,2.94169752078434,304.077678773646));
#18128=CARTESIAN_POINT('Ctrl Pts',(-33.7653026560057,2.94198569129769,304.072698617009));
#18129=CARTESIAN_POINT('Ctrl Pts',(-33.6729076380417,2.94227385808597,304.067718524749));
#18130=CARTESIAN_POINT('Ctrl Pts',(-33.5805004332759,2.93820509012,304.062738432489));
#18131=CARTESIAN_POINT('Ctrl Pts',(-33.488526091266,2.92980438598327,304.057758340228));
#18132=CARTESIAN_POINT('Ctrl Pts',(-33.3964673617753,2.92139597410716,304.052773678678));
#18133=CARTESIAN_POINT('Ctrl Pts',(-33.304842742193,2.9086477291594,304.047789017128));
#18134=CARTESIAN_POINT('Ctrl Pts',(-33.2140917891522,2.89163652674748,304.042804355577));
#18135=CARTESIAN_POINT('Ctrl Pts',(-33.1232994960559,2.87461757517117,304.037817423349));
#18136=CARTESIAN_POINT('Ctrl Pts',(-33.0333821047478,2.85333190480005,304.032830491121));
#18137=CARTESIAN_POINT('Ctrl Pts',(-32.9447663500711,2.82790697420564,304.027843558893));
#18138=CARTESIAN_POINT('Ctrl Pts',(-32.8560038399768,2.80243993770894,304.02284836787));
#18139=CARTESIAN_POINT('Ctrl Pts',(-32.7685477034634,2.77282009480686,304.017853176847));
#18140=CARTESIAN_POINT('Ctrl Pts',(-32.6828068523918,2.7392239423821,304.012857985824));
#18141=CARTESIAN_POINT('Ctrl Pts',(-32.6092424126289,2.71039891789928,304.008572182447));
#18142=CARTESIAN_POINT('Ctrl Pts',(-32.536940474007,2.67864765089728,304.004286379069));
#18143=CARTESIAN_POINT('Ctrl Pts',(-32.4661441993221,2.64410822562003,304.000000575692));
#18144=CARTESIAN_POINT('Ctrl Pts',(-32.4661441993221,2.64410822562003,304.));
#18145=CARTESIAN_POINT('Ctrl Pts',(-32.4496278394245,2.63585700138036,304.));
#18146=CARTESIAN_POINT('Ctrl Pts',(-32.4331114795268,2.6276057771407,304.));
#18147=CARTESIAN_POINT('Ctrl Pts',(-32.4165951196292,2.61935455290104,304.));
#18148=CARTESIAN_POINT('Origin',(-33.7561270252576,0.,302.151410108095));
#18149=CARTESIAN_POINT('',(-32.4049121771464,-1.94920919778867,314.));
#18150=CARTESIAN_POINT('Ctrl Pts',(-32.4049121771464,-1.94920919778867,
314.));
#18151=CARTESIAN_POINT('Ctrl Pts',(-32.546952397172,-2.04767315668297,313.987706520162));
#18152=CARTESIAN_POINT('Ctrl Pts',(-32.6993597984201,-2.1303378470281,313.974877189416));
#18153=CARTESIAN_POINT('Ctrl Pts',(-32.9571916953468,-2.23563193038453,
313.954758328853));
#18154=CARTESIAN_POINT('Ctrl Pts',(-33.0575139549198,-2.26898502116613,
313.947268440236));
#18155=CARTESIAN_POINT('Ctrl Pts',(-33.1919371907971,-2.30390855521111,
313.937699059563));
#18156=CARTESIAN_POINT('Ctrl Pts',(-33.2243097112393,-2.3115958427466,313.935428300996));
#18157=CARTESIAN_POINT('Ctrl Pts',(-33.2793153484165,-2.32344087527509,
313.931624624882));
#18158=CARTESIAN_POINT('Ctrl Pts',(-33.3018658348899,-2.32795483446128,
313.930080595254));
#18159=CARTESIAN_POINT('Ctrl Pts',(-33.347557267435,-2.33641170649212,313.926981619148));
#18160=CARTESIAN_POINT('Ctrl Pts',(-33.3706982218082,-2.34034049083399,
313.925427277736));
#18161=CARTESIAN_POINT('Ctrl Pts',(-33.42928515672,-2.34939457623398,313.921527820823));
#18162=CARTESIAN_POINT('Ctrl Pts',(-33.464796649993,-2.35406187527999,313.919197146517));
#18163=CARTESIAN_POINT('Ctrl Pts',(-33.6879281557284,-2.37826128555859,
313.904729739823));
#18164=CARTESIAN_POINT('Ctrl Pts',(-33.8772083579459,-2.37615718787244,
313.893306804096));
#18165=CARTESIAN_POINT('Ctrl Pts',(-34.167251331297,-2.3381544080642,313.875257458118));
#18166=CARTESIAN_POINT('Ctrl Pts',(-34.2692421070532,-2.31790791933874,
313.868785711074));
#18167=CARTESIAN_POINT('Ctrl Pts',(-34.3908902770311,-2.28533609520776,
313.860568378906));
#18168=CARTESIAN_POINT('Ctrl Pts',(-34.4121343053052,-2.27932880839701,
313.85911434623));
#18169=CARTESIAN_POINT('Ctrl Pts',(-34.4462839737763,-2.26915518751873,
313.856741554283));
#18170=CARTESIAN_POINT('Ctrl Pts',(-34.459243676734,-2.26517302436779,313.855832769321));
#18171=CARTESIAN_POINT('Ctrl Pts',(-34.4850303036276,-2.25700688965477,
313.854006537219));
#18172=CARTESIAN_POINT('Ctrl Pts',(-34.4978569923614,-2.25282416468677,
313.853089152264));
#18173=CARTESIAN_POINT('Ctrl Pts',(-34.5315680215517,-2.24151205800829,
313.850655593389));
#18174=CARTESIAN_POINT('Ctrl Pts',(-34.5523893071388,-2.23420037944764,
313.849129638672));
#18175=CARTESIAN_POINT('Ctrl Pts',(-34.6674173892997,-2.19199460440589,
313.840583150255));
#18176=CARTESIAN_POINT('Ctrl Pts',(-34.7594270324946,-2.15143567467892,
313.833314737358));
#18177=CARTESIAN_POINT('Ctrl Pts',(-34.9675437451218,-2.04343623286027,
313.816227684194));
#18178=CARTESIAN_POINT('Ctrl Pts',(-35.0810725147094,-1.97172185827824,
313.806408802031));
#18179=CARTESIAN_POINT('Ctrl Pts',(-35.2488180842235,-1.84469587552593,
313.791410683873));
#18180=CARTESIAN_POINT('Ctrl Pts',(-35.3074395161469,-1.79567848113724,
313.786057415392));
#18181=CARTESIAN_POINT('Ctrl Pts',(-35.3858820445179,-1.72337315872949,
313.778735173008));
#18182=CARTESIAN_POINT('Ctrl Pts',(-35.4077701362672,-1.70240760355948,
313.776673022591));
#18183=CARTESIAN_POINT('Ctrl Pts',(-35.4451893470748,-1.66516431478187,
313.773112134324));
#18184=CARTESIAN_POINT('Ctrl Pts',(-35.4609014395612,-1.64907488566002,
313.771605494546));
#18185=CARTESIAN_POINT('Ctrl Pts',(-35.493140037088,-1.6151087792166,313.768488564435));
#18186=CARTESIAN_POINT('Ctrl Pts',(-35.5096249735042,-1.59719616553267,
313.766880158734));
#18187=CARTESIAN_POINT('Ctrl Pts',(-35.5526638902841,-1.5489601850766,313.76263860479));
#18188=CARTESIAN_POINT('Ctrl Pts',(-35.5787263229804,-1.51820765015145,
313.760025781307));
#18189=CARTESIAN_POINT('Ctrl Pts',(-35.6993112958567,-1.36833927619302,
313.747687238571));
#18190=CARTESIAN_POINT('Ctrl Pts',(-35.7830192973965,-1.24097993977316,
313.738382399714));
#18191=CARTESIAN_POINT('Ctrl Pts',(-35.897886604779,-1.02319512526853,313.723283990641));
#18192=CARTESIAN_POINT('Ctrl Pts',(-35.9368094258337,-0.937381690122294,
313.717508739824));
#18193=CARTESIAN_POINT('Ctrl Pts',(-35.9889492360539,-0.80146648230257,
313.708313282547));
#18194=CARTESIAN_POINT('Ctrl Pts',(-36.0058029628861,-0.752861784914797,
313.705015106783));
#18195=CARTESIAN_POINT('Ctrl Pts',(-36.0265141381641,-0.686205521457368,
313.700430320496));
#18196=CARTESIAN_POINT('Ctrl Pts',(-36.0317617784603,-0.668597096852082,
313.699213415459));
#18197=CARTESIAN_POINT('Ctrl Pts',(-36.0403013893281,-0.638676691086577,
313.697133124901));
#18198=CARTESIAN_POINT('Ctrl Pts',(-36.0436997804577,-0.626395501086884,
313.696275672194));
#18199=CARTESIAN_POINT('Ctrl Pts',(-36.0507301357466,-0.600168548460251,
313.694435980716));
#18200=CARTESIAN_POINT('Ctrl Pts',(-36.0543341787238,-0.586216319855497,
313.693452326629));
#18201=CARTESIAN_POINT('Ctrl Pts',(-36.0643104034602,-0.546089080092318,
313.690610757855));
#18202=CARTESIAN_POINT('Ctrl Pts',(-36.0703638315002,-0.519838092049073,
313.688736599195));
#18203=CARTESIAN_POINT('Ctrl Pts',(-36.0974819260065,-0.392359244398201,
313.679580186892));
#18204=CARTESIAN_POINT('Ctrl Pts',(-36.1123572848319,-0.289937465168354,
313.672060948067));
#18205=CARTESIAN_POINT('Ctrl Pts',(-36.128133741848,-0.0903387662782653,
313.657439242264));
#18206=CARTESIAN_POINT('Ctrl Pts',(-36.1298446285413,0.00658624064446136,
313.650353717353));
#18207=CARTESIAN_POINT('Ctrl Pts',(-36.1214038017457,0.200112860721583,
313.636406114048));
#18208=CARTESIAN_POINT('Ctrl Pts',(-36.111259420544,0.296538515661029,313.629557095198));
#18209=CARTESIAN_POINT('Ctrl Pts',(-36.0899023192132,0.423951591307785,
313.62066387304));
#18210=CARTESIAN_POINT('Ctrl Pts',(-36.0839099567062,0.455707010347677,
313.618460013956));
#18211=CARTESIAN_POINT('Ctrl Pts',(-36.0726202738657,0.509479384929339,
313.614747757973));
#18212=CARTESIAN_POINT('Ctrl Pts',(-36.067653359524,0.531560234068789,313.613229033218));
#18213=CARTESIAN_POINT('Ctrl Pts',(-36.0575692570726,0.573572110180929,
313.610349055141));
#18214=CARTESIAN_POINT('Ctrl Pts',(-36.0525072964069,0.593514117459212,
313.608986169565));
#18215=CARTESIAN_POINT('Ctrl Pts',(-36.0385100200212,0.645795179190906,
313.605422488699));
#18216=CARTESIAN_POINT('Ctrl Pts',(-36.0291467352573,0.678015583222187,
313.603235738591));
#18217=CARTESIAN_POINT('Ctrl Pts',(-35.9881147377419,0.808791307870451,
313.594384793789));
#18218=CARTESIAN_POINT('Ctrl Pts',(-35.9506928190437,0.905426474581189,
313.587908386437));
#18219=CARTESIAN_POINT('Ctrl Pts',(-35.8560951271363,1.10904012995237,313.574055173609));
#18220=CARTESIAN_POINT('Ctrl Pts',(-35.7967986431042,1.21469920176365,313.566732922974));
#18221=CARTESIAN_POINT('Ctrl Pts',(-35.6842453467343,1.38357353035682,313.554153580709));
#18222=CARTESIAN_POINT('Ctrl Pts',(-35.6352886229486,1.44936702732116,313.548997777689));
#18223=CARTESIAN_POINT('Ctrl Pts',(-35.5696865950633,1.52860644025295,313.542277456499));
#18224=CARTESIAN_POINT('Ctrl Pts',(-35.5561296798544,1.54454728979497,313.540897791833));
#18225=CARTESIAN_POINT('Ctrl Pts',(-35.5337187495388,1.57020330700864,313.538627664557));
#18226=CARTESIAN_POINT('Ctrl Pts',(-35.5249913545983,1.58002839680919,313.537746141578));
#18227=CARTESIAN_POINT('Ctrl Pts',(-35.5071369081008,1.59979516842411,313.535946585833));
#18228=CARTESIAN_POINT('Ctrl Pts',(-35.4980058704805,1.60973235553793,313.535028322804));
#18229=CARTESIAN_POINT('Ctrl Pts',(-35.4734912843044,1.63595844722554,313.532569729515));
#18230=CARTESIAN_POINT('Ctrl Pts',(-35.4579612824317,1.65210777743187,313.5310191106));
#18231=CARTESIAN_POINT('Ctrl Pts',(-35.3579117961932,1.75323958875642,313.521086431675));
#18232=CARTESIAN_POINT('Ctrl Pts',(-35.2672886449006,1.83192478525135,313.51235148184));
#18233=CARTESIAN_POINT('Ctrl Pts',(-35.080206232925,1.97100101161773,313.495324689864));
#18234=CARTESIAN_POINT('Ctrl Pts',(-34.984561623233,2.0319898926767,313.487056435203));
#18235=CARTESIAN_POINT('Ctrl Pts',(-34.8170163848832,2.12265698300166,313.473467876795));
#18236=CARTESIAN_POINT('Ctrl Pts',(-34.747355239735,2.1560676693847,313.468052939947));
#18237=CARTESIAN_POINT('Ctrl Pts',(-34.6482245646911,2.19778981212911,313.460670121061));
#18238=CARTESIAN_POINT('Ctrl Pts',(-34.6200438056141,2.2090192447726,313.458606034392));
#18239=CARTESIAN_POINT('Ctrl Pts',(-34.5706848275723,2.22759863218599,313.455048800781));
#18240=CARTESIAN_POINT('Ctrl Pts',(-34.5496040529138,2.23519447602278,313.453547603489));
#18241=CARTESIAN_POINT('Ctrl Pts',(-34.505581055095,2.25035555175753,313.450448632843));
#18242=CARTESIAN_POINT('Ctrl Pts',(-34.4826244620117,2.25787134242534,313.448852641262));
#18243=CARTESIAN_POINT('Ctrl Pts',(-34.4216084089499,2.27682048568616,313.444660505233));
#18244=CARTESIAN_POINT('Ctrl Pts',(-34.3833686727503,2.28765058682674,313.442084061991));
#18245=CARTESIAN_POINT('Ctrl Pts',(-34.1889463169214,2.33747196546371,313.429207272684));
#18246=CARTESIAN_POINT('Ctrl Pts',(-34.0293544471349,2.3614530994093,313.419391192156));
#18247=CARTESIAN_POINT('Ctrl Pts',(-33.7806442261837,2.37325557290962,313.404119197688));
#18248=CARTESIAN_POINT('Ctrl Pts',(-33.6925785497909,2.37253087335058,313.398707720936));
#18249=CARTESIAN_POINT('Ctrl Pts',(-33.5554374422751,2.3637607162759,313.39001598739));
#18250=CARTESIAN_POINT('Ctrl Pts',(-33.5062262736265,2.35906546636591,313.386842940111));
#18251=CARTESIAN_POINT('Ctrl Pts',(-33.4392539520886,2.35055670877303,313.382406970114));
#18252=CARTESIAN_POINT('Ctrl Pts',(-33.4213335149318,2.34807125976028,313.38120839125));
#18253=CARTESIAN_POINT('Ctrl Pts',(-33.3908933985363,2.34349387427042,313.379149980199));
#18254=CARTESIAN_POINT('Ctrl Pts',(-33.3783590314818,2.34150602736475,313.378295826024));
#18255=CARTESIAN_POINT('Ctrl Pts',(-33.3514543302274,2.33701750095182,313.376447456013));
#18256=CARTESIAN_POINT('Ctrl Pts',(-33.3370909008514,2.3344848442745,313.375451661093));
#18257=CARTESIAN_POINT('Ctrl Pts',(-33.2963533547509,2.32691366546731,313.372603467335));
#18258=CARTESIAN_POINT('Ctrl Pts',(-33.2700410606749,2.32155967373467,313.370735247782));
#18259=CARTESIAN_POINT('Ctrl Pts',(-33.1398084133472,2.29274917163599,313.361364416972));
#18260=CARTESIAN_POINT('Ctrl Pts',(-33.0374675207498,2.26275760058699,313.353611370755));
#18261=CARTESIAN_POINT('Ctrl Pts',(-32.846386320345,2.19248583290265,313.338745192836));
#18262=CARTESIAN_POINT('Ctrl Pts',(-32.7574124410887,2.15341433065302,313.331649495554));
#18263=CARTESIAN_POINT('Ctrl Pts',(-32.6707032669284,2.10880380957248,313.324639106241));
#18264=CARTESIAN_POINT('Ctrl Pts',(-32.6703261471224,2.1086096593382,313.324608614338));
#18265=CARTESIAN_POINT('Ctrl Pts',(-32.6699490794749,2.10841540797709,313.324578124683));
#18266=CARTESIAN_POINT('',(-35.1331518153888,-1.93106208855754,314.));
#18267=CARTESIAN_POINT('Origin',(-33.7561270252576,0.,314.));
#18268=CARTESIAN_POINT('',(-36.1278767566871,0.00112870026910663,313.848589891954));
#18269=CARTESIAN_POINT('Ctrl Pts',(-36.1278767566871,0.00112870026910672,
313.848589891954));
#18270=CARTESIAN_POINT('Ctrl Pts',(-36.1279148957173,-0.0790132446041546,
313.854008225009));
#18271=CARTESIAN_POINT('Ctrl Pts',(-36.123886772926,-0.159300080416319,
313.859426558064));
#18272=CARTESIAN_POINT('Ctrl Pts',(-36.1157746507306,-0.239293013060521,
313.864844891119));
#18273=CARTESIAN_POINT('Ctrl Pts',(-36.1073434386814,-0.322432463048055,
313.870476353989));
#18274=CARTESIAN_POINT('Ctrl Pts',(-36.094500195761,-0.405253930370168,
313.876107816859));
#18275=CARTESIAN_POINT('Ctrl Pts',(-36.0772847864738,-0.487262465254211,
313.881739279729));
#18276=CARTESIAN_POINT('Ctrl Pts',(-36.0607750699741,-0.565909312326557,
313.887139898089));
#18277=CARTESIAN_POINT('Ctrl Pts',(-36.0402446877037,-0.643808064903195,
313.892540516448));
#18278=CARTESIAN_POINT('Ctrl Pts',(-36.0157815835671,-0.720527126214705,
313.897941134808));
#18279=CARTESIAN_POINT('Ctrl Pts',(-35.9913404357878,-0.79717732990626,
313.903336905953));
#18280=CARTESIAN_POINT('Ctrl Pts',(-35.9629737164686,-0.872649518442759,
313.908732677098));
#18281=CARTESIAN_POINT('Ctrl Pts',(-35.9308198228037,-0.946524853768198,
313.914128448244));
#18282=CARTESIAN_POINT('Ctrl Pts',(-35.8986858374103,-1.02035444874764,
313.919520878566));
#18283=CARTESIAN_POINT('Ctrl Pts',(-35.8627695184512,-1.0925887433214,313.924913308888));
#18284=CARTESIAN_POINT('Ctrl Pts',(-35.8232578094233,-1.16282775321819,
313.93030573921));
#18285=CARTESIAN_POINT('Ctrl Pts',(-35.7837595696115,-1.23304281921512,
313.935696331297));
#18286=CARTESIAN_POINT('Ctrl Pts',(-35.7406685988365,-1.30126356100973,
313.941086923384));
#18287=CARTESIAN_POINT('Ctrl Pts',(-35.6942177298364,-1.36711465624701,
313.946477515471));
#18288=CARTESIAN_POINT('Ctrl Pts',(-35.647754830922,-1.43298280569759,313.951869503621));
#18289=CARTESIAN_POINT('Ctrl Pts',(-35.5979305514185,-1.49647971103082,
313.957261491771));
#18290=CARTESIAN_POINT('Ctrl Pts',(-35.5450205211567,-1.55725981224386,
313.962653479922));
#18291=CARTESIAN_POINT('Ctrl Pts',(-35.4921025627892,-1.61804902082397,
313.968046276014));
#18292=CARTESIAN_POINT('Ctrl Pts',(-35.436098236994,-1.6761202813854,313.973439072107));
#18293=CARTESIAN_POINT('Ctrl Pts',(-35.3773216657082,-1.73116319284876,
313.9788318682));
#18294=CARTESIAN_POINT('Ctrl Pts',(-35.3184964663978,-1.78625164334224,
313.984229125952));
#18295=CARTESIAN_POINT('Ctrl Pts',(-35.2568947803512,-1.83830644365573,
313.989626383703));
#18296=CARTESIAN_POINT('Ctrl Pts',(-35.1928650153576,-1.88705644067775,
313.995023641455));
#18297=CARTESIAN_POINT('Ctrl Pts',(-35.1731861906162,-1.90203920139284,
313.996682427637));
#18298=CARTESIAN_POINT('Ctrl Pts',(-35.1532782346255,-1.91671010143613,
313.998341213818));
#18299=CARTESIAN_POINT('Ctrl Pts',(-35.1331518153888,-1.93106208855753,
314.));
#18300=CARTESIAN_POINT('Ctrl Pts',(-32.6699490794746,2.10841540797695,313.522886073942));
#18301=CARTESIAN_POINT('Ctrl Pts',(-32.6716174179545,2.10927487450148,313.523012757125));
#18302=CARTESIAN_POINT('Ctrl Pts',(-32.6732867045892,2.11013232378011,313.523139440309));
#18303=CARTESIAN_POINT('Ctrl Pts',(-32.6749569340628,2.11098775373186,313.523266123492));
#18304=CARTESIAN_POINT('Ctrl Pts',(-32.7452259553958,2.14697695550172,313.52859587216));
#18305=CARTESIAN_POINT('Ctrl Pts',(-32.8174259095208,2.17952132864185,313.533925620827));
#18306=CARTESIAN_POINT('Ctrl Pts',(-32.8911850198945,2.20840969701243,313.539255369495));
#18307=CARTESIAN_POINT('Ctrl Pts',(-32.9648389334936,2.23725686419224,313.544577516764));
#18308=CARTESIAN_POINT('Ctrl Pts',(-33.0400471541795,2.26245821167335,313.549899664034));
#18309=CARTESIAN_POINT('Ctrl Pts',(-33.1164141623099,2.28384883814127,313.555221811303));
#18310=CARTESIAN_POINT('Ctrl Pts',(-33.1926946841532,2.30521523954253,313.560537931195));
#18311=CARTESIAN_POINT('Ctrl Pts',(-33.270130936211,2.32277936968305,313.565854051088));
#18312=CARTESIAN_POINT('Ctrl Pts',(-33.3483097391138,2.33642528740432,313.57117017098));
#18313=CARTESIAN_POINT('Ctrl Pts',(-33.4264402244559,2.35006277141422,313.576483005302));
#18314=CARTESIAN_POINT('Ctrl Pts',(-33.5053118887913,2.35978676889661,313.581795839624));
#18315=CARTESIAN_POINT('Ctrl Pts',(-33.5844999923704,2.36553212281769,313.587108673946));
#18316=CARTESIAN_POINT('Ctrl Pts',(-33.663663866723,2.37127571882973,313.592419882697));
#18317=CARTESIAN_POINT('Ctrl Pts',(-33.7431435204535,2.37304305460202,313.597731091449));
#18318=CARTESIAN_POINT('Ctrl Pts',(-33.8225091910446,2.37082084320293,313.6030423002));
#18319=CARTESIAN_POINT('Ctrl Pts',(-33.9018753451706,2.36859861826502,313.60835354131));
#18320=CARTESIAN_POINT('Ctrl Pts',(-33.981127045836,2.36238681243055,313.61366478242));
#18321=CARTESIAN_POINT('Ctrl Pts',(-34.059836132218,2.35222423268899,313.61897602353));
#18322=CARTESIAN_POINT('Ctrl Pts',(-34.1386265621813,2.34205115021299,313.624292753655));
#18323=CARTESIAN_POINT('Ctrl Pts',(-34.2168727912834,2.32791919817414,313.62960948378));
#18324=CARTESIAN_POINT('Ctrl Pts',(-34.2941539597541,2.30991884711482,313.634926213905));
#18325=CARTESIAN_POINT('Ctrl Pts',(-34.3714735949446,2.29190953637654,313.640245590433));
#18326=CARTESIAN_POINT('Ctrl Pts',(-34.4478267611363,2.27002812078966,313.645564966962));
#18327=CARTESIAN_POINT('Ctrl Pts',(-34.5228074577539,2.24441510797964,313.650884343491));
#18328=CARTESIAN_POINT('Ctrl Pts',(-34.5979275613812,2.21875447446609,313.65621361001));
#18329=CARTESIAN_POINT('Ctrl Pts',(-34.6716696596955,2.18934855474684,313.661542876529));
#18330=CARTESIAN_POINT('Ctrl Pts',(-34.7436476134916,2.15638613200745,313.666872143048));
#18331=CARTESIAN_POINT('Ctrl Pts',(-34.8125527934063,2.12483089113858,313.671973900586));
#18332=CARTESIAN_POINT('Ctrl Pts',(-34.8798410874767,2.09001683724949,313.677075658123));
#18333=CARTESIAN_POINT('Ctrl Pts',(-34.9451978764374,2.05214730791302,313.682177415661));
#18334=CARTESIAN_POINT('Ctrl Pts',(-35.013046995834,2.01283365345862,313.687473724764));
#18335=CARTESIAN_POINT('Ctrl Pts',(-35.0790828745383,1.97007105799335,313.692770033867));
#18336=CARTESIAN_POINT('Ctrl Pts',(-35.1429293220549,1.92405235170398,313.698066342969));
#18337=CARTESIAN_POINT('Ctrl Pts',(-35.2066825731113,1.87810081877663,313.703354921066));
#18338=CARTESIAN_POINT('Ctrl Pts',(-35.2682523544018,1.82890288543903,313.708643499163));
#18339=CARTESIAN_POINT('Ctrl Pts',(-35.3272881060166,1.77669663161954,313.71393207726));
#18340=CARTESIAN_POINT('Ctrl Pts',(-35.386431186956,1.72439546477183,313.719230270201));
#18341=CARTESIAN_POINT('Ctrl Pts',(-35.4430306056107,1.66907528072418,313.724528463141));
#18342=CARTESIAN_POINT('Ctrl Pts',(-35.4967642823664,1.6110183120203,313.729826656081));
#18343=CARTESIAN_POINT('Ctrl Pts',(-35.5503054039893,1.55316939100624,313.735105862898));
#18344=CARTESIAN_POINT('Ctrl Pts',(-35.6010009517321,1.49260360694134,313.740385069715));
#18345=CARTESIAN_POINT('Ctrl Pts',(-35.6485679839444,1.42963816414665,313.745664276531));
#18346=CARTESIAN_POINT('Ctrl Pts',(-35.6961206913763,1.36669168335346,313.750941893518));
#18347=CARTESIAN_POINT('Ctrl Pts',(-35.7405464664373,1.30134735762143,313.756219510505));
#18348=CARTESIAN_POINT('Ctrl Pts',(-35.7816031421524,1.23395484617098,313.761497127492));
#18349=CARTESIAN_POINT('Ctrl Pts',(-35.8226606883943,1.1665609057935,313.76677485638));
#18350=CARTESIAN_POINT('Ctrl Pts',(-35.8603487469998,1.09711910072152,313.772052585269));
#18351=CARTESIAN_POINT('Ctrl Pts',(-35.8944697687086,1.02600603021152,313.777330314157));
#18352=CARTESIAN_POINT('Ctrl Pts',(-35.9288201111352,0.954415022653908,
313.78264351363));
#18353=CARTESIAN_POINT('Ctrl Pts',(-35.9595550682039,0.881130636100437,
313.787956713103));
#18354=CARTESIAN_POINT('Ctrl Pts',(-35.9865220636178,0.806558141337787,
313.793269912575));
#18355=CARTESIAN_POINT('Ctrl Pts',(-36.013352938898,0.732362062924119,313.798556292842));
#18356=CARTESIAN_POINT('Ctrl Pts',(-36.0364537219332,0.656891326621502,
313.803842673108));
#18357=CARTESIAN_POINT('Ctrl Pts',(-36.0557246703262,0.580558983476379,
313.809129053374));
#18358=CARTESIAN_POINT('Ctrl Pts',(-36.0751422686538,0.503645759052962,
313.81445566245));
#18359=CARTESIAN_POINT('Ctrl Pts',(-36.0906714086751,0.425858242206631,
313.819782271526));
#18360=CARTESIAN_POINT('Ctrl Pts',(-36.1022630534639,0.347625947898785,
313.825108880602));
#18361=CARTESIAN_POINT('Ctrl Pts',(-36.1138546982526,0.269393653590927,
313.830435489678));
#18362=CARTESIAN_POINT('Ctrl Pts',(-36.1215088749716,0.19071707224102,313.835762098754));
#18363=CARTESIAN_POINT('Ctrl Pts',(-36.1252298902417,0.112025343668419,
313.84108870783));
#18364=CARTESIAN_POINT('Ctrl Pts',(-36.1269765937627,0.0750861995389757,
313.843589102522));
#18365=CARTESIAN_POINT('Ctrl Pts',(-36.1278591566815,0.038111753064283,
313.846089497213));
#18366=CARTESIAN_POINT('Ctrl Pts',(-36.1278767566867,0.00112870099215847,
313.848589891905));
#18367=CARTESIAN_POINT('Ctrl Pts',(-34.7933121966354,2.12810918362782,303.66825685423));
#18368=CARTESIAN_POINT('Ctrl Pts',(-35.5015959476307,1.78291007010875,303.721227284953));
#18369=CARTESIAN_POINT('Ctrl Pts',(-36.5334100271131,0.333763633321939,
303.827168146399));
#18370=CARTESIAN_POINT('Ctrl Pts',(-35.5413299366473,-2.15794291786034,
303.986079438568));
#18371=CARTESIAN_POINT('Ctrl Pts',(-32.9089357156284,-2.66755271063891,
304.144990730738));
#18372=CARTESIAN_POINT('Ctrl Pts',(-31.0548666733256,-0.733421038154457,
304.303902022907));
#18373=CARTESIAN_POINT('Ctrl Pts',(-31.6765983504046,1.8740003336691,304.462813315076));
#18374=CARTESIAN_POINT('Ctrl Pts',(-34.2052449936392,2.76288312959717,304.621724607246));
#18375=CARTESIAN_POINT('Ctrl Pts',(-36.3219606220703,1.11889486817046,304.780635899415));
#18376=CARTESIAN_POINT('Ctrl Pts',(-36.0863485172746,-1.55101144960505,
304.939547191584));
#18377=CARTESIAN_POINT('Ctrl Pts',(-33.7143042574469,-2.79887542003478,
305.098458483753));
#18378=CARTESIAN_POINT('Ctrl Pts',(-31.3806218553374,-1.48069437689556,
305.257369775923));
#18379=CARTESIAN_POINT('Ctrl Pts',(-31.224842213905,1.19502694802466,305.416281068092));
#18380=CARTESIAN_POINT('Ctrl Pts',(-33.3897996861207,2.775118803617,305.575192360261));
#18381=CARTESIAN_POINT('Ctrl Pts',(-35.8906115960418,1.81092775317516,305.734103652431));
#18382=CARTESIAN_POINT('Ctrl Pts',(-36.4344857504044,-0.813559522228039,
305.8930149446));
#18383=CARTESIAN_POINT('Ctrl Pts',(-34.5227860158784,-2.69215848558538,
306.051926236769));
#18384=CARTESIAN_POINT('Ctrl Pts',(-31.908198004047,-2.102532305537,306.210837528939));
#18385=CARTESIAN_POINT('Ctrl Pts',(-30.9878286152358,0.41473814013526,306.369748821108));
#18386=CARTESIAN_POINT('Ctrl Pts',(-32.6054912639837,2.55176821696523,306.528660113277));
#18387=CARTESIAN_POINT('Ctrl Pts',(-35.2780800389393,2.34928558602826,306.687571405446));
#18388=CARTESIAN_POINT('Ctrl Pts',(-36.5553115068302,-0.00706961484117916,
306.846482697616));
#18389=CARTESIAN_POINT('Ctrl Pts',(-35.2661940011202,-2.35694324448151,
307.005393989785));
#18390=CARTESIAN_POINT('Ctrl Pts',(-32.5926165407175,-2.54592362172222,
307.164305281954));
#18391=CARTESIAN_POINT('Ctrl Pts',(-30.9857690329855,-0.400749709361767,
307.323216574124));
#18392=CARTESIAN_POINT('Ctrl Pts',(-31.9188417860902,2.11183964440955,307.482127866293));
#18393=CARTESIAN_POINT('Ctrl Pts',(-34.5363748202831,2.68825168330378,307.641039158462));
#18394=CARTESIAN_POINT('Ctrl Pts',(-36.4385608892421,0.800020187051445,
307.799950450632));
#18395=CARTESIAN_POINT('Ctrl Pts',(-35.8814373175924,-1.82168600355083,
307.958861742801));
#18396=CARTESIAN_POINT('Ctrl Pts',(-33.3757862682556,-2.77323360769926,
308.11777303497));
#18397=CARTESIAN_POINT('Ctrl Pts',(-31.2188393204144,-1.18222452907508,
308.27668432714));
#18398=CARTESIAN_POINT('Ctrl Pts',(-31.3881290776734,1.49267191791212,308.435595619309));
#18399=CARTESIAN_POINT('Ctrl Pts',(-33.7284472653066,2.79905654912215,308.594506911478));
#18400=CARTESIAN_POINT('Ctrl Pts',(-36.0941428169125,1.53920950239539,308.753418203648));
#18401=CARTESIAN_POINT('Ctrl Pts',(-36.3162981853304,-1.13181595916618,
308.912329495817));
#18402=CARTESIAN_POINT('Ctrl Pts',(-34.1912368338946,-2.76516964917568,
309.071240787986));
#18403=CARTESIAN_POINT('Ctrl Pts',(-31.6672580062641,-1.86335985675752,
309.230152080156));
#18404=CARTESIAN_POINT('Ctrl Pts',(-31.0583965596219,0.746815953951488,
309.389063372325));
#18405=CARTESIAN_POINT('Ctrl Pts',(-32.9228689874342,2.67229578765376,309.547974664494));
#18406=CARTESIAN_POINT('Ctrl Pts',(-35.5512892437397,2.14776077428841,309.706885956663));
#18407=CARTESIAN_POINT('Ctrl Pts',(-36.5338684563932,-0.345884772855582,
309.865797248833));
#18408=CARTESIAN_POINT('Ctrl Pts',(-34.969758122513,-2.52241616197692,310.024708541002));
#18409=CARTESIAN_POINT('Ctrl Pts',(-32.2929662431881,-2.38634537726121,
310.183619833172));
#18410=CARTESIAN_POINT('Ctrl Pts',(-30.9576297730183,-0.0624248677114656,
310.342531125341));
#18411=CARTESIAN_POINT('Ctrl Pts',(-32.1880122064702,2.31872802423598,310.50144241751));
#18412=CARTESIAN_POINT('Ctrl Pts',(-34.8560740328554,2.5740241470846,310.66035370968));
#18413=CARTESIAN_POINT('Ctrl Pts',(-36.5156821890243,0.469402854123652,
310.819265001849));
#18414=CARTESIAN_POINT('Ctrl Pts',(-35.6452743329216,-2.06557647898139,
310.978176294018));
#18415=CARTESIAN_POINT('Ctrl Pts',(-33.0428580095468,-2.70679349036151,
311.137087586187));
#18416=CARTESIAN_POINT('Ctrl Pts',(-31.0943811349663,-0.86636748976959,
311.295998878356));
#18417=CARTESIAN_POINT('Ctrl Pts',(-31.5862467830163,1.76836181184454,311.454910170526));
#18418=CARTESIAN_POINT('Ctrl Pts',(-34.0675024665792,2.78182110387257,311.613821462695));
#18419=CARTESIAN_POINT('Ctrl Pts',(-36.2632830024395,1.24485077935404,311.772732754865));
#18420=CARTESIAN_POINT('Ctrl Pts',(-36.1604518779547,-1.43342447057343,
311.931644047034));
#18421=CARTESIAN_POINT('Ctrl Pts',(-33.8532877870383,-2.79750601070989,
312.090555339203));
#18422=CARTESIAN_POINT('Ctrl Pts',(-31.4570432481482,-1.5967798810487,312.249466631373));
#18423=CARTESIAN_POINT('Ctrl Pts',(-31.1686484045087,1.06791153063105,312.408377923542));
#18424=CARTESIAN_POINT('Ctrl Pts',(-33.2524995915862,2.75350906460025,312.567289215711));
#18425=CARTESIAN_POINT('Ctrl Pts',(-35.7981008484644,1.91465705127629,312.72620050788));
#18426=CARTESIAN_POINT('Ctrl Pts',(-36.4715489807011,-0.679640623010668,
312.88511180005));
#18427=CARTESIAN_POINT('Ctrl Pts',(-34.6555073427497,-2.65072540672241,
313.044023092219));
#18428=CARTESIAN_POINT('Ctrl Pts',(-32.0147597975284,-2.19179308747854,
313.202934384388));
#18429=CARTESIAN_POINT('Ctrl Pts',(-30.970820086982,0.277090540655818,313.361845676558));
#18430=CARTESIAN_POINT('Ctrl Pts',(-32.4798917398762,2.49094240710133,313.520756968727));
#18431=CARTESIAN_POINT('Ctrl Pts',(-35.1603047572903,2.42321108623274,313.679668260896));
#18432=CARTESIAN_POINT('Ctrl Pts',(-36.5506207995528,0.129250313862038,
313.838606176025));
#18433=CARTESIAN_POINT('Ctrl Pts',(-35.7717615680654,-1.47086186108563,
313.94457366043));
#18434=CARTESIAN_POINT('Ctrl Pts',(-35.1296610793728,-1.92821312738253,
313.997570714112));
#18435=CARTESIAN_POINT('Ctrl Pts',(-34.8778062619321,2.30147513725125,303.779604659097));
#18436=CARTESIAN_POINT('Ctrl Pts',(-35.6437901952638,1.92815445273122,303.83257508982));
#18437=CARTESIAN_POINT('Ctrl Pts',(-36.7596607852054,0.360953615405971,
303.938515951266));
#18438=CARTESIAN_POINT('Ctrl Pts',(-35.686761105088,-2.33373927018,304.097427243436));
#18439=CARTESIAN_POINT('Ctrl Pts',(-32.8399194591199,-2.8848643143285,304.256338535605));
#18440=CARTESIAN_POINT('Ctrl Pts',(-30.8348090839403,-0.793169024143786,
304.415249827774));
#18441=CARTESIAN_POINT('Ctrl Pts',(-31.5071899974042,2.02666536487924,304.574161119944));
#18442=CARTESIAN_POINT('Ctrl Pts',(-34.2418322916392,2.98796080521536,304.733072412113));
#18443=CARTESIAN_POINT('Ctrl Pts',(-36.5309857001877,1.2100453962153,304.891983704282));
#18444=CARTESIAN_POINT('Ctrl Pts',(-36.2761795063165,-1.67736426134529,
305.050894996451));
#18445=CARTESIAN_POINT('Ctrl Pts',(-33.7108971747275,-3.02688519979633,
305.209806288621));
#18446=CARTESIAN_POINT('Ctrl Pts',(-31.1871018412851,-1.60131882354062,
305.36871758079));
#18447=CARTESIAN_POINT('Ctrl Pts',(-31.0186316451104,1.292379559462,305.52762887296));
#18448=CARTESIAN_POINT('Ctrl Pts',(-33.3599569087968,3.00119325576856,305.686540165129));
#18449=CARTESIAN_POINT('Ctrl Pts',(-36.0644969191988,1.95845459027906,305.845451457298));
#18450=CARTESIAN_POINT('Ctrl Pts',(-36.6526776637248,-0.879835972461675,
306.004362749467));
#18451=CARTESIAN_POINT('Ctrl Pts',(-34.5852417244649,-2.91147459340051,
306.163274041637));
#18452=CARTESIAN_POINT('Ctrl Pts',(-31.7576568666583,-2.27381464432759,
306.322185333806));
#18453=CARTESIAN_POINT('Ctrl Pts',(-30.7623097849709,0.448524692874981,
306.481096625975));
#18454=CARTESIAN_POINT('Ctrl Pts',(-32.5117549709583,2.75964746196053,306.640007918145));
#18455=CARTESIAN_POINT('Ctrl Pts',(-35.4020656114921,2.54066962735892,306.798919210314));
#18456=CARTESIAN_POINT('Ctrl Pts',(-36.7833464642229,-0.00764553948268389,
306.957830502483));
#18457=CARTESIAN_POINT('Ctrl Pts',(-35.389211280177,-2.54895111529913,307.116741794653));
#18458=CARTESIAN_POINT('Ctrl Pts',(-32.4978314111505,-2.7533267380322,307.275653086822));
#18459=CARTESIAN_POINT('Ctrl Pts',(-30.7600824192988,-0.433396697618922,
307.434564378991));
#18460=CARTESIAN_POINT('Ctrl Pts',(-31.7691677420999,2.28388020354508,307.593475671161));
#18461=CARTESIAN_POINT('Ctrl Pts',(-34.5999375378766,2.90724952431741,307.75238696333));
#18462=CARTESIAN_POINT('Ctrl Pts',(-36.6570847828653,0.865193658278026,
307.911298255499));
#18463=CARTESIAN_POINT('Ctrl Pts',(-36.054575260143,-1.97008925919095,308.070209547668));
#18464=CARTESIAN_POINT('Ctrl Pts',(-33.3448018908812,-2.99915448277377,
308.229120839838));
#18465=CARTESIAN_POINT('Ctrl Pts',(-31.0121397272021,-1.27853419422617,
308.388032132007));
#18466=CARTESIAN_POINT('Ctrl Pts',(-31.1952206378624,1.61427211234131,308.546943424176));
#18467=CARTESIAN_POINT('Ctrl Pts',(-33.7261923396586,3.02708108452555,308.705854716346));
#18468=CARTESIAN_POINT('Ctrl Pts',(-36.284608766886,1.66460087106293,308.864766008515));
#18469=CARTESIAN_POINT('Ctrl Pts',(-36.5248619742656,-1.22401910108982,
309.023677300684));
#18470=CARTESIAN_POINT('Ctrl Pts',(-34.2266829601957,-2.990433595616,309.182588592854));
#18471=CARTESIAN_POINT('Ctrl Pts',(-31.4970887441518,-2.01515806382118,
309.341499885023));
#18472=CARTESIAN_POINT('Ctrl Pts',(-30.8386265316591,0.807655153854402,
309.500411177192));
#18473=CARTESIAN_POINT('Ctrl Pts',(-32.8549878018948,2.88999378508484,309.659322469362));
#18474=CARTESIAN_POINT('Ctrl Pts',(-35.6975317449751,2.3227276404878,309.818233761531));
#18475=CARTESIAN_POINT('Ctrl Pts',(-36.7601565603275,-0.374062200945844,
309.9771450537));
#18476=CARTESIAN_POINT('Ctrl Pts',(-35.0686263169372,-2.72790424817124,
310.13605634587));
#18477=CARTESIAN_POINT('Ctrl Pts',(-32.1737701670472,-2.58074848645625,
310.294967638039));
#18478=CARTESIAN_POINT('Ctrl Pts',(-30.7296508006143,-0.067510296036245,
310.453878930208));
#18479=CARTESIAN_POINT('Ctrl Pts',(-32.0602660724647,2.50762270041502,310.612790222377));
#18480=CARTESIAN_POINT('Ctrl Pts',(-34.9456809775434,2.78371646660568,310.771701514547));
#18481=CARTESIAN_POINT('Ctrl Pts',(-36.740488752627,0.507642655946229,310.930612806716));
#18482=CARTESIAN_POINT('Ctrl Pts',(-35.7991733090868,-2.2338482193675,311.089524098886));
#18483=CARTESIAN_POINT('Ctrl Pts',(-32.9847517037003,-2.9273018356703,311.248435391055));
#18484=CARTESIAN_POINT('Ctrl Pts',(-30.8775425826384,-0.936945929639025,
311.407346683224));
#18485=CARTESIAN_POINT('Ctrl Pts',(-31.409477959152,1.91242102375915,311.566257975393));
#18486=CARTESIAN_POINT('Ctrl Pts',(-34.0928685994519,3.0084415574625,311.725169267563));
#18487=CARTESIAN_POINT('Ctrl Pts',(-36.4675279209855,1.34626227841713,311.884080559732));
#18488=CARTESIAN_POINT('Ctrl Pts',(-36.3563196812212,-1.5501980845402,312.042991851901));
#18489=CARTESIAN_POINT('Ctrl Pts',(-33.8612029674485,-3.02540423183745,
312.201903144071));
#18490=CARTESIAN_POINT('Ctrl Pts',(-31.2697488863056,-1.72686120814153,
312.36081443624));
#18491=CARTESIAN_POINT('Ctrl Pts',(-30.9578600192052,1.15490871212794,312.519725728409));
#18492=CARTESIAN_POINT('Ctrl Pts',(-33.2114716918049,2.97782308404421,312.678637020578));
#18493=CARTESIAN_POINT('Ctrl Pts',(-35.964449803611,2.07063417317869,312.837548312748));
#18494=CARTESIAN_POINT('Ctrl Pts',(-36.6927602420485,-0.735007399130949,
312.996459604917));
#18495=CARTESIAN_POINT('Ctrl Pts',(-34.7287751654779,-2.86666617774379,
313.155370897087));
#18496=CARTESIAN_POINT('Ctrl Pts',(-31.8728996935609,-2.37034703653308,
313.314282189256));
#18497=CARTESIAN_POINT('Ctrl Pts',(-30.7439156606475,0.299663661523098,
313.473193481425));
#18498=CARTESIAN_POINT('Ctrl Pts',(-32.3759235088286,2.69386649067301,313.632104773595));
#18499=CARTESIAN_POINT('Ctrl Pts',(-35.2746957920377,2.62061745242278,313.791016065764));
#18500=CARTESIAN_POINT('Ctrl Pts',(-36.7782736294934,0.13977966268081,313.949953980892));
#18501=CARTESIAN_POINT('Ctrl Pts',(-35.9359647994402,-1.59068530396026,
314.055921465297));
#18502=CARTESIAN_POINT('Ctrl Pts',(-35.2415557335371,-2.08529459208821,
314.108918518978));
#18503=CARTESIAN_POINT('Ctrl Pts',(-34.9623003272288,2.47484109087468,303.890952463964));
#18504=CARTESIAN_POINT('Ctrl Pts',(-35.785984442897,2.0733988353537,303.943922894687));
#18505=CARTESIAN_POINT('Ctrl Pts',(-36.9859115432976,0.388143597490006,
304.049863756133));
#18506=CARTESIAN_POINT('Ctrl Pts',(-35.8321922735287,-2.50953562249967,
304.208775048302));
#18507=CARTESIAN_POINT('Ctrl Pts',(-32.7709032026114,-3.10217591801808,
304.367686340471));
#18508=CARTESIAN_POINT('Ctrl Pts',(-30.614751494555,-0.852917010133116,
304.526597632641));
#18509=CARTESIAN_POINT('Ctrl Pts',(-31.337781644404,2.17933039608939,304.68550892481));
#18510=CARTESIAN_POINT('Ctrl Pts',(-34.2784195896392,3.21303848083357,304.844420216979));
#18511=CARTESIAN_POINT('Ctrl Pts',(-36.7400107783054,1.30119592426015,305.003331509149));
#18512=CARTESIAN_POINT('Ctrl Pts',(-36.4660104953585,-1.80371707308553,
305.162242801318));
#18513=CARTESIAN_POINT('Ctrl Pts',(-33.7074900920081,-3.25489497955788,
305.321154093487));
#18514=CARTESIAN_POINT('Ctrl Pts',(-30.9935818272327,-1.72194327018567,
305.480065385657));
#18515=CARTESIAN_POINT('Ctrl Pts',(-30.8124210763159,1.38973217089934,305.638976677826));
#18516=CARTESIAN_POINT('Ctrl Pts',(-33.330114131473,3.22726770792011,305.797887969995));
#18517=CARTESIAN_POINT('Ctrl Pts',(-36.2383822423557,2.10598142738296,305.956799262165));
#18518=CARTESIAN_POINT('Ctrl Pts',(-36.8708695770453,-0.94611242269531,
306.115710554334));
#18519=CARTESIAN_POINT('Ctrl Pts',(-34.6476974330514,-3.13079070121565,
306.274621846503));
#18520=CARTESIAN_POINT('Ctrl Pts',(-31.6071157292697,-2.44509698311818,
306.433533138673));
#18521=CARTESIAN_POINT('Ctrl Pts',(-30.5367909547061,0.482311245614701,
306.592444430842));
#18522=CARTESIAN_POINT('Ctrl Pts',(-32.418018677933,2.96752670695583,306.751355723011));
#18523=CARTESIAN_POINT('Ctrl Pts',(-35.5260511840449,2.73205366868956,306.91026701518));
#18524=CARTESIAN_POINT('Ctrl Pts',(-37.0113814216157,-0.00822146412418619,
307.06917830735));
#18525=CARTESIAN_POINT('Ctrl Pts',(-35.5122285592338,-2.74095898611676,
307.228089599519));
#18526=CARTESIAN_POINT('Ctrl Pts',(-32.4030462815833,-2.96072985434218,
307.387000891688));
#18527=CARTESIAN_POINT('Ctrl Pts',(-30.534395805612,-0.466043685876077,
307.545912183858));
#18528=CARTESIAN_POINT('Ctrl Pts',(-31.6194936981096,2.45592076268062,307.704823476027));
#18529=CARTESIAN_POINT('Ctrl Pts',(-34.6635002554701,3.12624736533102,307.863734768196));
#18530=CARTESIAN_POINT('Ctrl Pts',(-36.8756086764883,0.930367129504609,
308.022646060366));
#18531=CARTESIAN_POINT('Ctrl Pts',(-36.2277132026935,-2.11849251483108,
308.181557352535));
#18532=CARTESIAN_POINT('Ctrl Pts',(-33.3138175135068,-3.22507535784829,
308.340468644704));
#18533=CARTESIAN_POINT('Ctrl Pts',(-30.8054401339898,-1.37484385937724,
308.499379936874));
#18534=CARTESIAN_POINT('Ctrl Pts',(-31.0023121980512,1.73587230677052,308.658291229043));
#18535=CARTESIAN_POINT('Ctrl Pts',(-33.7239374140105,3.25510561992896,308.817202521212));
#18536=CARTESIAN_POINT('Ctrl Pts',(-36.4750747168593,1.78999223973046,308.976113813381));
#18537=CARTESIAN_POINT('Ctrl Pts',(-36.7334257632008,-1.31622224301346,
309.135025105551));
#18538=CARTESIAN_POINT('Ctrl Pts',(-34.2621290864967,-3.21569754205633,
309.29393639772));
#18539=CARTESIAN_POINT('Ctrl Pts',(-31.3269194820396,-2.16695627088482,
309.452847689889));
#18540=CARTESIAN_POINT('Ctrl Pts',(-30.6188565036962,0.868494353757314,
309.611758982059));
#18541=CARTESIAN_POINT('Ctrl Pts',(-32.7871066163556,3.10769178251591,309.770670274228));
#18542=CARTESIAN_POINT('Ctrl Pts',(-35.8437742462105,2.49769450668719,309.929581566397));
#18543=CARTESIAN_POINT('Ctrl Pts',(-36.9864446642617,-0.402239629036108,
310.088492858567));
#18544=CARTESIAN_POINT('Ctrl Pts',(-35.1674945113613,-2.93339233436557,
310.247404150736));
#18545=CARTESIAN_POINT('Ctrl Pts',(-32.0545740909063,-2.77515159565129,
310.406315442906));
#18546=CARTESIAN_POINT('Ctrl Pts',(-30.5016718282103,-0.0725957243610234,
310.565226735075));
#18547=CARTESIAN_POINT('Ctrl Pts',(-31.9325199384592,2.69651737659405,310.724138027244));
#18548=CARTESIAN_POINT('Ctrl Pts',(-35.0352879222314,2.99340878612678,310.883049319413));
#18549=CARTESIAN_POINT('Ctrl Pts',(-36.9652953162298,0.545882457768805,
311.041960611583));
#18550=CARTESIAN_POINT('Ctrl Pts',(-35.9530722852521,-2.4021199597536,311.200871903752));
#18551=CARTESIAN_POINT('Ctrl Pts',(-32.9266453978538,-3.14781018097909,
311.359783195921));
#18552=CARTESIAN_POINT('Ctrl Pts',(-30.6607040303105,-1.00752436950846,
311.51869448809));
#18553=CARTESIAN_POINT('Ctrl Pts',(-31.2327091352876,2.05648023567375,311.67760578026));
#18554=CARTESIAN_POINT('Ctrl Pts',(-34.1182347323246,3.23506201105244,311.836517072429));
#18555=CARTESIAN_POINT('Ctrl Pts',(-36.6717728395313,1.44767377748021,311.995428364599));
#18556=CARTESIAN_POINT('Ctrl Pts',(-36.5521874844876,-1.66697169850697,
312.154339656768));
#18557=CARTESIAN_POINT('Ctrl Pts',(-33.8691181478586,-3.253302452965,312.313250948937));
#18558=CARTESIAN_POINT('Ctrl Pts',(-31.0824545244631,-1.85694253523434,
312.472162241106));
#18559=CARTESIAN_POINT('Ctrl Pts',(-30.7470716339017,1.24190589362483,312.631073533276));
#18560=CARTESIAN_POINT('Ctrl Pts',(-33.1704437920237,3.20213710348816,312.789984825445));
#18561=CARTESIAN_POINT('Ctrl Pts',(-36.1307987587576,2.2266112950811,312.948896117615));
#18562=CARTESIAN_POINT('Ctrl Pts',(-36.9139715033961,-0.79037417525123,
313.107807409784));
#18563=CARTESIAN_POINT('Ctrl Pts',(-34.802042988206,-3.08260694876516,313.266718701953));
#18564=CARTESIAN_POINT('Ctrl Pts',(-31.7310395895932,-2.54890098558761,
313.425629994122));
#18565=CARTESIAN_POINT('Ctrl Pts',(-30.517011234313,0.322236782390377,313.584541286292));
#18566=CARTESIAN_POINT('Ctrl Pts',(-32.2719552777809,2.89679057424468,313.743452578461));
#18567=CARTESIAN_POINT('Ctrl Pts',(-35.3890868267849,2.81802381861281,313.90236387063));
#18568=CARTESIAN_POINT('Ctrl Pts',(-37.005926459434,0.15030901149958,314.061301785759));
#18569=CARTESIAN_POINT('Ctrl Pts',(-36.100168030815,-1.7105087468349,314.167269270164));
#18570=CARTESIAN_POINT('Ctrl Pts',(-35.3534503877015,-2.24237605679389,
314.220266323846));
#18571=CARTESIAN_POINT('Ctrl Pts',(-35.0467943925255,2.64820704449811,304.002300268831));
#18572=CARTESIAN_POINT('Ctrl Pts',(-35.9281786905302,2.21864321797617,304.055270699554));
#18573=CARTESIAN_POINT('Ctrl Pts',(-37.2121623013899,0.415333579574038,
304.161211561));
#18574=CARTESIAN_POINT('Ctrl Pts',(-35.9776234419694,-2.68533197481934,
304.32012285317));
#18575=CARTESIAN_POINT('Ctrl Pts',(-32.7018869461029,-3.31948752170765,
304.479034145339));
#18576=CARTESIAN_POINT('Ctrl Pts',(-30.3946939051697,-0.912664996122445,
304.637945437508));
#18577=CARTESIAN_POINT('Ctrl Pts',(-31.1683732914037,2.33199542729953,304.796856729678));
#18578=CARTESIAN_POINT('Ctrl Pts',(-34.3150068876391,3.43811615645176,304.955768021847));
#18579=CARTESIAN_POINT('Ctrl Pts',(-36.9490358564228,1.39234645230499,305.114679314016));
#18580=CARTESIAN_POINT('Ctrl Pts',(-36.6558414844005,-1.93006988482577,
305.273590606185));
#18581=CARTESIAN_POINT('Ctrl Pts',(-33.7040830092887,-3.48290475931941,
305.432501898355));
#18582=CARTESIAN_POINT('Ctrl Pts',(-30.8000618131804,-1.84256771683072,
305.591413190524));
#18583=CARTESIAN_POINT('Ctrl Pts',(-30.6062105075215,1.48708478233668,305.750324482693));
#18584=CARTESIAN_POINT('Ctrl Pts',(-33.3002713541492,3.45334216007167,305.909235774863));
#18585=CARTESIAN_POINT('Ctrl Pts',(-36.4122675655127,2.25350826448685,306.068147067032));
#18586=CARTESIAN_POINT('Ctrl Pts',(-37.0890614903658,-1.01238887292895,
306.227058359201));
#18587=CARTESIAN_POINT('Ctrl Pts',(-34.710153141638,-3.35010680903079,306.385969651371));
#18588=CARTESIAN_POINT('Ctrl Pts',(-31.4565745918809,-2.61637932190877,
306.54488094354));
#18589=CARTESIAN_POINT('Ctrl Pts',(-30.3112721244413,0.516097798354423,
306.703792235709));
#18590=CARTESIAN_POINT('Ctrl Pts',(-32.3242823849075,3.17540595195113,306.862703527879));
#18591=CARTESIAN_POINT('Ctrl Pts',(-35.6500367565977,2.92343771002022,307.021614820048));
#18592=CARTESIAN_POINT('Ctrl Pts',(-37.2394163790084,-0.00879738876569104,
307.180526112217));
#18593=CARTESIAN_POINT('Ctrl Pts',(-35.6352458382906,-2.93296685693438,
307.339437404387));
#18594=CARTESIAN_POINT('Ctrl Pts',(-32.3082611520162,-3.16813297065216,
307.498348696556));
#18595=CARTESIAN_POINT('Ctrl Pts',(-30.3087091919254,-0.498690674133233,
307.657259988725));
#18596=CARTESIAN_POINT('Ctrl Pts',(-31.4698196541192,2.62796132181615,307.816171280895));
#18597=CARTESIAN_POINT('Ctrl Pts',(-34.7270629730636,3.34524520634464,307.975082573064));
#18598=CARTESIAN_POINT('Ctrl Pts',(-37.0941325701115,0.995540600731191,
308.133993865233));
#18599=CARTESIAN_POINT('Ctrl Pts',(-36.4008511452441,-2.2668957704712,308.292905157402));
#18600=CARTESIAN_POINT('Ctrl Pts',(-33.2828331361324,-3.45099623292281,
308.451816449572));
#18601=CARTESIAN_POINT('Ctrl Pts',(-30.5987405407777,-1.47115352452833,
308.610727741741));
#18602=CARTESIAN_POINT('Ctrl Pts',(-30.8094037582401,1.85747250119972,308.76963903391));
#18603=CARTESIAN_POINT('Ctrl Pts',(-33.7216824883626,3.48313015533236,308.92855032608));
#18604=CARTESIAN_POINT('Ctrl Pts',(-36.6655406668328,1.91538360839799,309.087461618249));
#18605=CARTESIAN_POINT('Ctrl Pts',(-36.9419895521361,-1.4084253849371,309.246372910419));
#18606=CARTESIAN_POINT('Ctrl Pts',(-34.2975752127978,-3.44096148849664,
309.405284202588));
#18607=CARTESIAN_POINT('Ctrl Pts',(-31.1567502199273,-2.31875447794848,
309.564195494757));
#18608=CARTESIAN_POINT('Ctrl Pts',(-30.3990864757334,0.92933355366023,309.723106786926));
#18609=CARTESIAN_POINT('Ctrl Pts',(-32.7192254308164,3.32538977994698,309.882018079096));
#18610=CARTESIAN_POINT('Ctrl Pts',(-35.9900167474459,2.6726613728866,310.040929371265));
#18611=CARTESIAN_POINT('Ctrl Pts',(-37.212732768196,-0.430417057126371,
310.199840663434));
#18612=CARTESIAN_POINT('Ctrl Pts',(-35.2663627057854,-3.1388804205599,310.358751955604));
#18613=CARTESIAN_POINT('Ctrl Pts',(-31.9353780147653,-2.96955470484632,
310.517663247773));
#18614=CARTESIAN_POINT('Ctrl Pts',(-30.2736928558063,-0.0776811526858028,
310.676574539942));
#18615=CARTESIAN_POINT('Ctrl Pts',(-31.8047738044536,2.8854120527731,310.835485832111));
#18616=CARTESIAN_POINT('Ctrl Pts',(-35.1248948669194,3.20310110564787,310.994397124281));
#18617=CARTESIAN_POINT('Ctrl Pts',(-37.1901018798325,0.584122259591381,
311.15330841645));
#18618=CARTESIAN_POINT('Ctrl Pts',(-36.1069712614174,-2.57039170013971,
311.31221970862));
#18619=CARTESIAN_POINT('Ctrl Pts',(-32.8685390920073,-3.36831852628788,
311.471131000788));
#18620=CARTESIAN_POINT('Ctrl Pts',(-30.4438654779826,-1.07810280937789,
311.630042292958));
#18621=CARTESIAN_POINT('Ctrl Pts',(-31.0559403114233,2.20053944758835,311.788953585127));
#18622=CARTESIAN_POINT('Ctrl Pts',(-34.1436008651973,3.46168246464236,311.947864877297));
#18623=CARTESIAN_POINT('Ctrl Pts',(-36.8760177580772,1.54908527654329,312.106776169466));
#18624=CARTESIAN_POINT('Ctrl Pts',(-36.7480552877541,-1.78374531247374,
312.265687461635));
#18625=CARTESIAN_POINT('Ctrl Pts',(-33.8770333282688,-3.48120067409255,
312.424598753805));
#18626=CARTESIAN_POINT('Ctrl Pts',(-30.8951601626206,-1.98702386232717,
312.583510045974));
#18627=CARTESIAN_POINT('Ctrl Pts',(-30.5362832485983,1.32890307512172,312.742421338143));
#18628=CARTESIAN_POINT('Ctrl Pts',(-33.1294158922425,3.42645112293213,312.901332630312));
#18629=CARTESIAN_POINT('Ctrl Pts',(-36.2971477139041,2.38258841698351,313.060243922482));
#18630=CARTESIAN_POINT('Ctrl Pts',(-37.1351827647435,-0.845740951371512,
313.219155214651));
#18631=CARTESIAN_POINT('Ctrl Pts',(-34.8753108109342,-3.29854771978654,
313.378066506821));
#18632=CARTESIAN_POINT('Ctrl Pts',(-31.5891794856257,-2.72745493464214,
313.53697779899));
#18633=CARTESIAN_POINT('Ctrl Pts',(-30.2901068079786,0.344809903257656,
313.695889091159));
#18634=CARTESIAN_POINT('Ctrl Pts',(-32.1679870467333,3.09971465781636,313.854800383328));
#18635=CARTESIAN_POINT('Ctrl Pts',(-35.5034778615323,3.01543018480285,314.013711675498));
#18636=CARTESIAN_POINT('Ctrl Pts',(-37.2335792893745,0.160838360318353,
314.172649590626));
#18637=CARTESIAN_POINT('Ctrl Pts',(-36.2643712621899,-1.83033218970954,
314.278617075031));
#18638=CARTESIAN_POINT('Ctrl Pts',(-35.4653450418657,-2.39945752149957,
314.331614128713));
#18639=CARTESIAN_POINT('Ctrl Pts',(-35.048294363387,2.64856243216296,314.));
#18640=CARTESIAN_POINT('Ctrl Pts',(-35.1084097821696,2.6123298863998,314.));
#18641=CARTESIAN_POINT('Ctrl Pts',(-35.167002205871,2.5738771597971,314.));
#18642=CARTESIAN_POINT('Ctrl Pts',(-35.2239356243364,2.53320436048268,314.));
#18643=CARTESIAN_POINT('Ctrl Pts',(-35.302523371486,2.4770618741443,314.));
#18644=CARTESIAN_POINT('Ctrl Pts',(-35.3779519219753,2.41669059985685,314.));
#18645=CARTESIAN_POINT('Ctrl Pts',(-35.4500731232314,2.35247138102498,314.));
#18646=CARTESIAN_POINT('Ctrl Pts',(-35.5231270342098,2.28742164510913,314.));
#18647=CARTESIAN_POINT('Ctrl Pts',(-35.5927879602898,2.21842287923684,314.));
#18648=CARTESIAN_POINT('Ctrl Pts',(-35.6588581969503,2.14584033513384,314.));
#18649=CARTESIAN_POINT('Ctrl Pts',(-35.7205977405011,2.07801534510539,314.));
#18650=CARTESIAN_POINT('Ctrl Pts',(-35.7792017240155,2.00706006960028,314.));
#18651=CARTESIAN_POINT('Ctrl Pts',(-35.8344697486721,1.93325966121245,314.));
#18652=CARTESIAN_POINT('Ctrl Pts',(-35.843967544963,1.92057707938679,314.));
#18653=CARTESIAN_POINT('Ctrl Pts',(-35.8533667266025,1.90781045945915,314.));
#18654=CARTESIAN_POINT('Ctrl Pts',(-35.8626661550442,1.89496123542743,314.));
#18655=CARTESIAN_POINT('Ctrl Pts',(-35.8709857286912,1.88346589823451,314.));
#18656=CARTESIAN_POINT('Ctrl Pts',(-35.8792200303602,1.87191193902222,314.));
#18657=CARTESIAN_POINT('Ctrl Pts',(-35.887367573277,1.86030205283278,314.));
#18658=CARTESIAN_POINT('Ctrl Pts',(-35.9425286671464,1.78169994806992,314.));
#18659=CARTESIAN_POINT('Ctrl Pts',(-35.9937329226186,1.70051417088793,314.));
#18660=CARTESIAN_POINT('Ctrl Pts',(-36.0408251356185,1.61710612342277,314.));
#18661=CARTESIAN_POINT('Ctrl Pts',(-36.0877584401856,1.53397952890413,314.));
#18662=CARTESIAN_POINT('Ctrl Pts',(-36.1306077020639,1.4486446755458,314.));
#18663=CARTESIAN_POINT('Ctrl Pts',(-36.1691706243013,1.36144258670802,314.));
#18664=CARTESIAN_POINT('Ctrl Pts',(-36.2068531598979,1.27623131053712,314.));
#18665=CARTESIAN_POINT('Ctrl Pts',(-36.2404429370695,1.18923622578619,314.));
#18666=CARTESIAN_POINT('Ctrl Pts',(-36.2697019974602,1.10077293509858,314.));
#18667=CARTESIAN_POINT('Ctrl Pts',(-36.2828100229337,1.06114148240263,314.));
#18668=CARTESIAN_POINT('Ctrl Pts',(-36.2950481842672,1.02121539777195,314.));
#18669=CARTESIAN_POINT('Ctrl Pts',(-36.3063916868407,0.981023559239999,
314.));
#18670=CARTESIAN_POINT('Ctrl Pts',(-36.3110603578331,0.964481713415173,
314.));
#18671=CARTESIAN_POINT('Ctrl Pts',(-36.3155774556104,0.947894856897153,
314.));
#18672=CARTESIAN_POINT('Ctrl Pts',(-36.3199411435984,0.931265031017353,
314.));
#18673=CARTESIAN_POINT('Ctrl Pts',(-36.3234243468608,0.917990694283236,
314.));
#18674=CARTESIAN_POINT('Ctrl Pts',(-36.3268093077046,0.904690635360945,
314.));
#18675=CARTESIAN_POINT('Ctrl Pts',(-36.3300925197077,0.891377257943442,
314.));
#18676=CARTESIAN_POINT('Ctrl Pts',(-36.3520513927238,0.802334343916824,
314.));
#18677=CARTESIAN_POINT('Ctrl Pts',(-36.3695001180218,0.712556143612094,
314.));
#18678=CARTESIAN_POINT('Ctrl Pts',(-36.3822614546468,0.62235272186204,314.));
#18679=CARTESIAN_POINT('Ctrl Pts',(-36.3946616503746,0.53470202210478,314.));
#18680=CARTESIAN_POINT('Ctrl Pts',(-36.4026359984996,0.446649080643674,
314.));
#18681=CARTESIAN_POINT('Ctrl Pts',(-36.4059737703562,0.358481187047295,
314.));
#18682=CARTESIAN_POINT('Ctrl Pts',(-36.4089167669493,0.280741358916277,
314.));
#18683=CARTESIAN_POINT('Ctrl Pts',(-36.408254518313,0.202911894824171,314.));
#18684=CARTESIAN_POINT('Ctrl Pts',(-36.4038099638934,0.125198274633709,
314.));
#18685=CARTESIAN_POINT('Ctrl Pts',(-36.4008302127494,0.0730969328991553,
314.));
#18686=CARTESIAN_POINT('Ctrl Pts',(-36.3961496017144,0.0210478334846509,
314.));
#18687=CARTESIAN_POINT('Ctrl Pts',(-36.3897974146925,-0.0308821710389396,
314.));
#18688=CARTESIAN_POINT('Ctrl Pts',(-36.387060420309,-0.0532574774058058,
314.));
#18689=CARTESIAN_POINT('Ctrl Pts',(-36.3840130379563,-0.0756106332558332,
314.));
#18690=CARTESIAN_POINT('Ctrl Pts',(-36.3806573700362,-0.0979360923355628,
314.));
#18691=CARTESIAN_POINT('Ctrl Pts',(-36.3784396264198,-0.112690873063438,
314.));
#18692=CARTESIAN_POINT('Ctrl Pts',(-36.3760882417879,-0.12742648365222,
314.));
#18693=CARTESIAN_POINT('Ctrl Pts',(-36.3736056166943,-0.1421336397238,314.));
#18694=CARTESIAN_POINT('Ctrl Pts',(-36.358848312808,-0.229556413308451,
314.));
#18695=CARTESIAN_POINT('Ctrl Pts',(-36.3394450237544,-0.316061693843362,
314.));
#18696=CARTESIAN_POINT('Ctrl Pts',(-36.3156218303925,-0.401349704677867,
314.));
#18697=CARTESIAN_POINT('Ctrl Pts',(-36.2915442390384,-0.487548470774106,
314.));
#18698=CARTESIAN_POINT('Ctrl Pts',(-36.2629512749207,-0.572504691772821,
314.));
#18699=CARTESIAN_POINT('Ctrl Pts',(-36.2300287870974,-0.655885577779074,
314.));
#18700=CARTESIAN_POINT('Ctrl Pts',(-36.2020579810211,-0.726725625027795,
314.));
#18701=CARTESIAN_POINT('Ctrl Pts',(-36.1709610593741,-0.796428449700502,
314.));
#18702=CARTESIAN_POINT('Ctrl Pts',(-36.1368301419288,-0.864770030271797,
314.));
#18703=CARTESIAN_POINT('Ctrl Pts',(-36.1189794373775,-0.900513146913665,
314.));
#18704=CARTESIAN_POINT('Ctrl Pts',(-36.1002985225055,-0.935883572879644,
314.));
#18705=CARTESIAN_POINT('Ctrl Pts',(-36.080798805821,-0.970846733823177,
314.));
#18706=CARTESIAN_POINT('Ctrl Pts',(-36.0694443279123,-0.991205411078644,
314.));
#18707=CARTESIAN_POINT('Ctrl Pts',(-36.0578122052746,-1.01142596615713,
314.));
#18708=CARTESIAN_POINT('Ctrl Pts',(-36.0459045295853,-1.03150126491425,
314.));
#18709=CARTESIAN_POINT('Ctrl Pts',(-36.0381073298707,-1.0446466610288,314.));
#18710=CARTESIAN_POINT('Ctrl Pts',(-36.0301966102719,-1.05772193059368,
314.));
#18711=CARTESIAN_POINT('Ctrl Pts',(-36.0221748813531,-1.07072286206983,
314.));
#18712=CARTESIAN_POINT('Ctrl Pts',(-35.9764975905212,-1.14475270453075,
314.));
#18713=CARTESIAN_POINT('Ctrl Pts',(-35.9272075963404,-1.21640239869884,
314.));
#18714=CARTESIAN_POINT('Ctrl Pts',(-35.8744657309249,-1.28534907412501,
314.));
#18715=CARTESIAN_POINT('Ctrl Pts',(-35.8240263851529,-1.35128578634124,
314.));
#18716=CARTESIAN_POINT('Ctrl Pts',(-35.7704292800472,-1.41475065875741,
314.));
#18717=CARTESIAN_POINT('Ctrl Pts',(-35.7137905242578,-1.47542402497924,
314.));
#18718=CARTESIAN_POINT('Ctrl Pts',(-35.6981895359756,-1.49213633552136,
314.));
#18719=CARTESIAN_POINT('Ctrl Pts',(-35.682357657742,-1.50863661010363,314.));
#18720=CARTESIAN_POINT('Ctrl Pts',(-35.6662970719128,-1.52491759329652,
314.));
#18721=CARTESIAN_POINT('Ctrl Pts',(-35.6500715173412,-1.54136580907671,
314.));
#18722=CARTESIAN_POINT('Ctrl Pts',(-35.6336083386895,-1.55759402253731,
314.));
#18723=CARTESIAN_POINT('Ctrl Pts',(-35.6169334591263,-1.5735723090143,314.));
#18724=CARTESIAN_POINT('Ctrl Pts',(-35.5569485462704,-1.63105135216241,
314.));
#18725=CARTESIAN_POINT('Ctrl Pts',(-35.4941798129402,-1.68534916505214,
314.));
#18726=CARTESIAN_POINT('Ctrl Pts',(-35.428756278306,-1.73615449293592,314.));
#18727=CARTESIAN_POINT('Ctrl Pts',(-35.3640039973732,-1.78643855175975,
314.));
#18728=CARTESIAN_POINT('Ctrl Pts',(-35.2966505706336,-1.83330190156947,
314.));
#18729=CARTESIAN_POINT('Ctrl Pts',(-35.2268031625002,-1.87639577447683,
314.));
#18730=CARTESIAN_POINT('Ctrl Pts',(-35.1960663839232,-1.89535949646701,
314.));
#18731=CARTESIAN_POINT('Ctrl Pts',(-35.1648464609444,-1.91359260343915,
314.));
#18732=CARTESIAN_POINT('Ctrl Pts',(-35.1331518153888,-1.93106208855754,
314.));
#18733=CARTESIAN_POINT('Ctrl Pts',(-35.136256587458,-1.93376001453662,304.));
#18734=CARTESIAN_POINT('Ctrl Pts',(-35.1864755730177,-1.90645007575824,
304.));
#18735=CARTESIAN_POINT('Ctrl Pts',(-35.2355436729036,-1.87725776018492,
304.));
#18736=CARTESIAN_POINT('Ctrl Pts',(-35.2833415381341,-1.8462068102493,304.));
#18737=CARTESIAN_POINT('Ctrl Pts',(-35.3519691462361,-1.80162422453964,
304.));
#18738=CARTESIAN_POINT('Ctrl Pts',(-35.417979523451,-1.75321259707355,304.));
#18739=CARTESIAN_POINT('Ctrl Pts',(-35.4812868793252,-1.70133469307906,
304.));
#18740=CARTESIAN_POINT('Ctrl Pts',(-35.5178418155665,-1.6713793514499,304.));
#18741=CARTESIAN_POINT('Ctrl Pts',(-35.5534952315518,-1.64026732609317,
304.));
#18742=CARTESIAN_POINT('Ctrl Pts',(-35.5882275656708,-1.60806122732678,
304.));
#18743=CARTESIAN_POINT('Ctrl Pts',(-35.6031722450925,-1.59420354014004,
304.));
#18744=CARTESIAN_POINT('Ctrl Pts',(-35.6179463615319,-1.58014323230078,
304.));
#18745=CARTESIAN_POINT('Ctrl Pts',(-35.6325482026628,-1.56588502452514,
304.));
#18746=CARTESIAN_POINT('Ctrl Pts',(-35.6440421171294,-1.55466160282436,
304.));
#18747=CARTESIAN_POINT('Ctrl Pts',(-35.6554289453095,-1.54331576002995,
304.));
#18748=CARTESIAN_POINT('Ctrl Pts',(-35.6666983284761,-1.53185979753453,
304.));
#18749=CARTESIAN_POINT('Ctrl Pts',(-35.7265208404879,-1.47104684585338,
304.));
#18750=CARTESIAN_POINT('Ctrl Pts',(-35.7831066394599,-1.40706632820761,
304.));
#18751=CARTESIAN_POINT('Ctrl Pts',(-35.8363619838647,-1.34030711823897,
304.));
#18752=CARTESIAN_POINT('Ctrl Pts',(-35.8828522774344,-1.28202836134408,
304.));
#18753=CARTESIAN_POINT('Ctrl Pts',(-35.926804443913,-1.22163090931687,304.));
#18754=CARTESIAN_POINT('Ctrl Pts',(-35.9681403014762,-1.15934519918605,
304.));
#18755=CARTESIAN_POINT('Ctrl Pts',(-35.9878823140538,-1.12959753347161,
304.));
#18756=CARTESIAN_POINT('Ctrl Pts',(-36.0070272988542,-1.09941880216891,
304.));
#18757=CARTESIAN_POINT('Ctrl Pts',(-36.0255652755386,-1.06883236996832,
304.));
#18758=CARTESIAN_POINT('Ctrl Pts',(-36.0325711927724,-1.05727307112341,
304.));
#18759=CARTESIAN_POINT('Ctrl Pts',(-36.0394911006069,-1.04565433821461,
304.));
#18760=CARTESIAN_POINT('Ctrl Pts',(-36.0463222172369,-1.03398116891762,
304.));
#18761=CARTESIAN_POINT('Ctrl Pts',(-36.0912572282266,-0.957195188080242,
304.));
#18762=CARTESIAN_POINT('Ctrl Pts',(-36.1322282517761,-0.878271730335654,
304.));
#18763=CARTESIAN_POINT('Ctrl Pts',(-36.169138795271,-0.797614937086259,
304.));
#18764=CARTESIAN_POINT('Ctrl Pts',(-36.2065492466915,-0.715865746749425,
304.));
#18765=CARTESIAN_POINT('Ctrl Pts',(-36.2397891124247,-0.632335215633068,
304.));
#18766=CARTESIAN_POINT('Ctrl Pts',(-36.2687251047273,-0.547401107491553,
304.));
#18767=CARTESIAN_POINT('Ctrl Pts',(-36.2976016694788,-0.462641433528532,
304.));
#18768=CARTESIAN_POINT('Ctrl Pts',(-36.3221925833473,-0.37648307086863,
304.));
#18769=CARTESIAN_POINT('Ctrl Pts',(-36.3423240859166,-0.289271161890286,
304.));
#18770=CARTESIAN_POINT('Ctrl Pts',(-36.3536805126693,-0.240073857671492,
304.));
#18771=CARTESIAN_POINT('Ctrl Pts',(-36.3636170610722,-0.190540814642171,
304.));
#18772=CARTESIAN_POINT('Ctrl Pts',(-36.3720956766504,-0.140731332976591,
304.));
#18773=CARTESIAN_POINT('Ctrl Pts',(-36.3745105282781,-0.126544758910929,
304.));
#18774=CARTESIAN_POINT('Ctrl Pts',(-36.3768074143961,-0.112333537716529,
304.));
#18775=CARTESIAN_POINT('Ctrl Pts',(-36.3789842951394,-0.0981061290234124,
304.));
#18776=CARTESIAN_POINT('Ctrl Pts',(-36.392994413349,-0.00654039754206603,
304.));
#18777=CARTESIAN_POINT('Ctrl Pts',(-36.4019963253058,0.0854153674215651,
304.));
#18778=CARTESIAN_POINT('Ctrl Pts',(-36.405860521369,0.177365179482698,304.));
#18779=CARTESIAN_POINT('Ctrl Pts',(-36.4078070365684,0.223683146747381,
304.));
#18780=CARTESIAN_POINT('Ctrl Pts',(-36.4084492403383,0.270000128814116,
304.));
#18781=CARTESIAN_POINT('Ctrl Pts',(-36.4077662908771,0.316268099145672,
304.));
#18782=CARTESIAN_POINT('Ctrl Pts',(-36.4064446460242,0.405805946854447,
304.));
#18783=CARTESIAN_POINT('Ctrl Pts',(-36.4001638837636,0.495159815679732,
304.));
#18784=CARTESIAN_POINT('Ctrl Pts',(-36.3891755640259,0.584057949482216,
304.));
#18785=CARTESIAN_POINT('Ctrl Pts',(-36.3781872442881,0.6729560832847,304.));
#18786=CARTESIAN_POINT('Ctrl Pts',(-36.3624910987386,0.761399212765894,
304.));
#18787=CARTESIAN_POINT('Ctrl Pts',(-36.3422863391992,0.84911917863751,304.));
#18788=CARTESIAN_POINT('Ctrl Pts',(-36.3370360262829,0.87191367262448,304.));
#18789=CARTESIAN_POINT('Ctrl Pts',(-36.3314810075873,0.894659321429367,
304.));
#18790=CARTESIAN_POINT('Ctrl Pts',(-36.325624234848,0.917351364077548,304.));
#18791=CARTESIAN_POINT('Ctrl Pts',(-36.3220111917182,0.931350085291673,
304.));
#18792=CARTESIAN_POINT('Ctrl Pts',(-36.3182854034492,0.945320190717022,
304.));
#18793=CARTESIAN_POINT('Ctrl Pts',(-36.3144491483228,0.959256442722998,
304.));
#18794=CARTESIAN_POINT('Ctrl Pts',(-36.2899927853656,1.04810090850946,304.));
#18795=CARTESIAN_POINT('Ctrl Pts',(-36.2610373548936,1.13562270896613,304.));
#18796=CARTESIAN_POINT('Ctrl Pts',(-36.2278662880232,1.22154108776326,304.));
#18797=CARTESIAN_POINT('Ctrl Pts',(-36.1936404394721,1.31019152014043,304.));
#18798=CARTESIAN_POINT('Ctrl Pts',(-36.1549265381509,1.39713573522954,304.));
#18799=CARTESIAN_POINT('Ctrl Pts',(-36.1119793205632,1.48206836683025,304.));
#18800=CARTESIAN_POINT('Ctrl Pts',(-36.0690321029756,1.56700099843096,304.));
#18801=CARTESIAN_POINT('Ctrl Pts',(-36.0218512050178,1.64992291753996,304.));
#18802=CARTESIAN_POINT('Ctrl Pts',(-35.9706392647091,1.73051904816679,304.));
#18803=CARTESIAN_POINT('Ctrl Pts',(-35.9398454510111,1.778981617957,304.));
#18804=CARTESIAN_POINT('Ctrl Pts',(-35.90759318223,1.82660302327394,304.));
#18805=CARTESIAN_POINT('Ctrl Pts',(-35.8739182865488,1.87331104247519,304.));
#18806=CARTESIAN_POINT('Ctrl Pts',(-35.8647784686436,1.88598822473753,304.));
#18807=CARTESIAN_POINT('Ctrl Pts',(-35.8555329429828,1.89859915141812,304.));
#18808=CARTESIAN_POINT('Ctrl Pts',(-35.8461934502801,1.91112782045539,304.));
#18809=CARTESIAN_POINT('Ctrl Pts',(-35.7873991537107,1.98999872987687,304.));
#18810=CARTESIAN_POINT('Ctrl Pts',(-35.7247912432541,2.06574291947499,304.));
#18811=CARTESIAN_POINT('Ctrl Pts',(-35.6586401626076,2.13804857623474,304.));
#18812=CARTESIAN_POINT('Ctrl Pts',(-35.5923426775549,2.21051425860013,304.));
#18813=CARTESIAN_POINT('Ctrl Pts',(-35.5224859214325,2.27952707644113,304.));
#18814=CARTESIAN_POINT('Ctrl Pts',(-35.4492921764977,2.34475739531049,304.));
#18815=CARTESIAN_POINT('Ctrl Pts',(-35.3775470541738,2.40869670065248,304.));
#18816=CARTESIAN_POINT('Ctrl Pts',(-35.3025951940527,2.46900251941962,304.));
#18817=CARTESIAN_POINT('Ctrl Pts',(-35.2246051459773,2.52533702182221,304.));
#18818=CARTESIAN_POINT('Ctrl Pts',(-35.1664255709284,2.56736183769632,304.));
#18819=CARTESIAN_POINT('Ctrl Pts',(-35.1065543901557,2.60717614810924,304.));
#18820=CARTESIAN_POINT('Ctrl Pts',(-35.045048879311,2.6446255791971,304.));
#18821=CARTESIAN_POINT('Origin',(-33.7561270252576,0.,304.));
#18822=CARTESIAN_POINT('Ctrl Pts',(-32.4165951196292,2.61935455290103,304.));
#18823=CARTESIAN_POINT('Ctrl Pts',(-32.3729951199972,2.59185154803127,304.));
#18824=CARTESIAN_POINT('Ctrl Pts',(-32.33021699184,2.56313577813171,304.));
#18825=CARTESIAN_POINT('Ctrl Pts',(-32.2883183340065,2.5332036871298,304.));
#18826=CARTESIAN_POINT('Ctrl Pts',(-32.2088386511067,2.47642399001364,304.));
#18827=CARTESIAN_POINT('Ctrl Pts',(-32.1325211106366,2.41526919274723,304.));
#18828=CARTESIAN_POINT('Ctrl Pts',(-32.0595408108092,2.35011684676039,304.));
#18829=CARTESIAN_POINT('Ctrl Pts',(-32.0207536959428,2.31549008400965,304.));
#18830=CARTESIAN_POINT('Ctrl Pts',(-31.982909930747,2.27973359274166,304.));
#18831=CARTESIAN_POINT('Ctrl Pts',(-31.9460408721372,2.24290104434646,304.));
#18832=CARTESIAN_POINT('Ctrl Pts',(-31.9281541386185,2.22503202347093,304.));
#18833=CARTESIAN_POINT('Ctrl Pts',(-31.910496870039,2.20690971360344,304.));
#18834=CARTESIAN_POINT('Ctrl Pts',(-31.8930729674242,2.18854012322945,304.));
#18835=CARTESIAN_POINT('Ctrl Pts',(-31.8768341094174,2.17141989613,304.));
#18836=CARTESIAN_POINT('Ctrl Pts',(-31.8607950118222,2.15408142589293,304.));
#18837=CARTESIAN_POINT('Ctrl Pts',(-31.8449782280288,2.13655141487154,304.));
#18838=CARTESIAN_POINT('Ctrl Pts',(-31.7798728810234,2.06439404928693,304.));
#18839=CARTESIAN_POINT('Ctrl Pts',(-31.7184686521933,1.98893090454704,304.));
#18840=CARTESIAN_POINT('Ctrl Pts',(-31.6609384686365,1.91053545053345,304.));
#18841=CARTESIAN_POINT('Ctrl Pts',(-31.6137878951005,1.84628412382424,304.));
#18842=CARTESIAN_POINT('Ctrl Pts',(-31.5692402724945,1.78006228612976,304.));
#18843=CARTESIAN_POINT('Ctrl Pts',(-31.5274150673336,1.71206593956167,304.));
#18844=CARTESIAN_POINT('Ctrl Pts',(-31.508422782787,1.68118967829326,304.));
#18845=CARTESIAN_POINT('Ctrl Pts',(-31.489992159153,1.64994744210258,304.));
#18846=CARTESIAN_POINT('Ctrl Pts',(-31.4721359899822,1.61835732397993,304.));
#18847=CARTESIAN_POINT('Ctrl Pts',(-31.4616116348991,1.59973823401394,304.));
#18848=CARTESIAN_POINT('Ctrl Pts',(-31.4512868576275,1.58099829230828,304.));
#18849=CARTESIAN_POINT('Ctrl Pts',(-31.4411644485915,1.56214119768984,304.));
#18850=CARTESIAN_POINT('Ctrl Pts',(-31.433918782782,1.54864320474607,304.));
#18851=CARTESIAN_POINT('Ctrl Pts',(-31.4267770469623,1.53508547807366,304.));
#18852=CARTESIAN_POINT('Ctrl Pts',(-31.4197464253918,1.5214817248892,304.));
#18853=CARTESIAN_POINT('Ctrl Pts',(-31.3761638327664,1.43715250488072,304.));
#18854=CARTESIAN_POINT('Ctrl Pts',(-31.3367818849303,1.35093594766862,304.));
#18855=CARTESIAN_POINT('Ctrl Pts',(-31.3017640134589,1.26317540073157,304.));
#18856=CARTESIAN_POINT('Ctrl Pts',(-31.2671097254814,1.17632605384564,304.));
#18857=CARTESIAN_POINT('Ctrl Pts',(-31.2367291567388,1.08796369843067,304.));
#18858=CARTESIAN_POINT('Ctrl Pts',(-31.2108303189363,0.998412005752113,
304.));
#18859=CARTESIAN_POINT('Ctrl Pts',(-31.1856879329934,0.911475934090166,
304.));
#18860=CARTESIAN_POINT('Ctrl Pts',(-31.164769283098,0.823418230371202,304.));
#18861=CARTESIAN_POINT('Ctrl Pts',(-31.1483130220834,0.734538577814548,
304.));
#18862=CARTESIAN_POINT('Ctrl Pts',(-31.1382501561084,0.680189413640112,
304.));
#18863=CARTESIAN_POINT('Ctrl Pts',(-31.1298568208722,0.625533022136213,
304.));
#18864=CARTESIAN_POINT('Ctrl Pts',(-31.1231969611698,0.570640383078611,
304.));
#18865=CARTESIAN_POINT('Ctrl Pts',(-31.120787234397,0.550778664082103,304.));
#18866=CARTESIAN_POINT('Ctrl Pts',(-31.1186040726064,0.530880218793511,
304.));
#18867=CARTESIAN_POINT('Ctrl Pts',(-31.1166536015942,0.510981310296628,
304.));
#18868=CARTESIAN_POINT('Ctrl Pts',(-31.1079529873378,0.422216737087059,
304.));
#18869=CARTESIAN_POINT('Ctrl Pts',(-31.1038634706706,0.333340801037856,
304.));
#18870=CARTESIAN_POINT('Ctrl Pts',(-31.1045676259692,0.244642963201259,
304.));
#18871=CARTESIAN_POINT('Ctrl Pts',(-31.1048840697322,0.204782611901844,
304.));
#18872=CARTESIAN_POINT('Ctrl Pts',(-31.1061693062391,0.164958271719723,
304.));
#18873=CARTESIAN_POINT('Ctrl Pts',(-31.1084433320085,0.12519671516225,304.));
#18874=CARTESIAN_POINT('Ctrl Pts',(-31.1136824223524,0.0335907229086449,
304.));
#18875=CARTESIAN_POINT('Ctrl Pts',(-31.1241665977145,-0.0576836627488685,
304.));
#18876=CARTESIAN_POINT('Ctrl Pts',(-31.1396923668751,-0.148276725180234,
304.));
#18877=CARTESIAN_POINT('Ctrl Pts',(-31.1552181360356,-0.238869787611599,
304.));
#18878=CARTESIAN_POINT('Ctrl Pts',(-31.1757861692824,-0.328782421429016,
304.));
#18879=CARTESIAN_POINT('Ctrl Pts',(-31.2012379505196,-0.41763439700009,
304.));
#18880=CARTESIAN_POINT('Ctrl Pts',(-31.2056830871938,-0.433152335469932,
304.));
#18881=CARTESIAN_POINT('Ctrl Pts',(-31.2102772862545,-0.448637826840731,
304.));
#18882=CARTESIAN_POINT('Ctrl Pts',(-31.2150198204515,-0.464088718625177,
304.));
#18883=CARTESIAN_POINT('Ctrl Pts',(-31.2189504100873,-0.476894343759212,
304.));
#18884=CARTESIAN_POINT('Ctrl Pts',(-31.2229800422566,-0.489666905174659,
304.));
#18885=CARTESIAN_POINT('Ctrl Pts',(-31.2271076474096,-0.502404590095855,
304.));
#18886=CARTESIAN_POINT('Ctrl Pts',(-31.2544438085227,-0.586763290676307,
304.));
#18887=CARTESIAN_POINT('Ctrl Pts',(-31.2860768566243,-0.669605849478574,
304.));
#18888=CARTESIAN_POINT('Ctrl Pts',(-31.3217964375752,-0.750627783818284,
304.));
#18889=CARTESIAN_POINT('Ctrl Pts',(-31.3573807625506,-0.831342920024453,
304.));
#18890=CARTESIAN_POINT('Ctrl Pts',(-31.3970213965721,-0.910251957319242,
304.));
#18891=CARTESIAN_POINT('Ctrl Pts',(-31.4405519276009,-0.987024228084651,
304.));
#18892=CARTESIAN_POINT('Ctrl Pts',(-31.4836967496893,-1.06311624638121,
304.));
#18893=CARTESIAN_POINT('Ctrl Pts',(-31.5306634817197,-1.13710987045192,
304.));
#18894=CARTESIAN_POINT('Ctrl Pts',(-31.581321246188,-1.20864334882212,304.));
#18895=CARTESIAN_POINT('Ctrl Pts',(-31.5986762592469,-1.23315024256868,
304.));
#18896=CARTESIAN_POINT('Ctrl Pts',(-31.6164647169899,-1.25736799689345,
304.));
#18897=CARTESIAN_POINT('Ctrl Pts',(-31.6346820037716,-1.28128076205596,
304.));
#18898=CARTESIAN_POINT('Ctrl Pts',(-31.6453254812064,-1.29525183137379,
304.));
#18899=CARTESIAN_POINT('Ctrl Pts',(-31.6561153448988,-1.30911877942604,
304.));
#18900=CARTESIAN_POINT('Ctrl Pts',(-31.6670507171168,-1.3228783286073,304.));
#18901=CARTESIAN_POINT('Ctrl Pts',(-31.6759908550193,-1.33412735284745,
304.));
#18902=CARTESIAN_POINT('Ctrl Pts',(-31.6850238164214,-1.34529894988918,
304.));
#18903=CARTESIAN_POINT('Ctrl Pts',(-31.6941441122879,-1.3563859440613,304.));
#18904=CARTESIAN_POINT('Ctrl Pts',(-31.7483070899398,-1.4222286125845,304.));
#18905=CARTESIAN_POINT('Ctrl Pts',(-31.8055986639454,-1.48515504772159,
304.));
#18906=CARTESIAN_POINT('Ctrl Pts',(-31.8658620465816,-1.54486745321929,
304.));
#18907=CARTESIAN_POINT('Ctrl Pts',(-31.9251669866202,-1.60363017898558,
304.));
#18908=CARTESIAN_POINT('Ctrl Pts',(-31.9873505939602,-1.65928081190419,
304.));
#18909=CARTESIAN_POINT('Ctrl Pts',(-32.0522893270757,-1.71149313834578,
304.));
#18910=CARTESIAN_POINT('Ctrl Pts',(-32.1151930964543,-1.76206930427372,
304.));
#18911=CARTESIAN_POINT('Ctrl Pts',(-32.1806825889982,-1.80941956418428,
304.));
#18912=CARTESIAN_POINT('Ctrl Pts',(-32.2486612235432,-1.85320170266444,
304.));
#18913=CARTESIAN_POINT('Ctrl Pts',(-32.2911749746431,-1.88058299607264,
304.));
#18914=CARTESIAN_POINT('Ctrl Pts',(-32.3346625680721,-1.90656779027268,
304.));
#18915=CARTESIAN_POINT('Ctrl Pts',(-32.3791022351265,-1.93106208855756,
304.));
#18916=CARTESIAN_POINT('Ctrl Pts',(-32.0470519128079,-2.39933801925114,
303.668487391161));
#18917=CARTESIAN_POINT('Ctrl Pts',(-31.2480517507686,-1.83025205252113,
303.721485292345));
#18918=CARTESIAN_POINT('Ctrl Pts',(-30.2788767558638,0.160810338759522,
303.82745362425));
#18919=CARTESIAN_POINT('Ctrl Pts',(-32.0088834388462,3.01524564186955,303.986392386879));
#18920=CARTESIAN_POINT('Ctrl Pts',(-35.3441694449124,3.09952410938487,304.145303679049));
#18921=CARTESIAN_POINT('Ctrl Pts',(-37.2219347537451,0.34478896869055,304.304214971218));
#18922=CARTESIAN_POINT('Ctrl Pts',(-35.9229416834483,-2.72728782013422,
304.463126263387));
#18923=CARTESIAN_POINT('Ctrl Pts',(-32.6370118643326,-3.2983454038319,304.622037555556));
#18924=CARTESIAN_POINT('Ctrl Pts',(-30.3772784769107,-0.845689126967715,
304.780948847726));
#18925=CARTESIAN_POINT('Ctrl Pts',(-31.2152621400224,2.38244234343232,304.939860139895));
#18926=CARTESIAN_POINT('Ctrl Pts',(-34.3827997320786,3.42624101826296,305.098771432064));
#18927=CARTESIAN_POINT('Ctrl Pts',(-36.9757733735449,1.3288215966872,305.257682724234));
#18928=CARTESIAN_POINT('Ctrl Pts',(-36.6169184655888,-1.98690202842926,
305.416594016403));
#18929=CARTESIAN_POINT('Ctrl Pts',(-33.6352281354669,-3.48098722000116,
305.575505308572));
#18930=CARTESIAN_POINT('Ctrl Pts',(-30.7643822156783,-1.78363594109757,
305.734416600742));
#18931=CARTESIAN_POINT('Ctrl Pts',(-30.6364275912679,1.54899029327215,305.893327892911));
#18932=CARTESIAN_POINT('Ctrl Pts',(-33.3686769436664,3.46147020832407,306.05223918508));
#18933=CARTESIAN_POINT('Ctrl Pts',(-36.456148174692,2.20040451960325,306.21115047725));
#18934=CARTESIAN_POINT('Ctrl Pts',(-37.0681854782468,-1.07803670456918,
306.370061769419));
#18935=CARTESIAN_POINT('Ctrl Pts',(-34.6436605352495,-3.368111994789,306.528973061588));
#18936=CARTESIAN_POINT('Ctrl Pts',(-31.4054269332307,-2.57023409426841,
306.687884353758));
#18937=CARTESIAN_POINT('Ctrl Pts',(-30.3223627279394,0.584086443613537,
306.846795645927));
#18938=CARTESIAN_POINT('Ctrl Pts',(-32.3874431108284,3.20290470461917,307.005706938096));
#18939=CARTESIAN_POINT('Ctrl Pts',(-35.7073605970825,2.88523513113779,307.164618230265));
#18940=CARTESIAN_POINT('Ctrl Pts',(-37.2383476661245,-0.0776763895964064,
307.323529522435));
#18941=CARTESIAN_POINT('Ctrl Pts',(-35.576764394886,-2.96937262392716,307.482440814604));
#18942=CARTESIAN_POINT('Ctrl Pts',(-32.2459839461897,-3.13868795728262,
307.641352106774));
#18943=CARTESIAN_POINT('Ctrl Pts',(-30.2997332272108,-0.430390665717282,
307.800263398942));
#18944=CARTESIAN_POINT('Ctrl Pts',(-31.5223742760276,2.67249749624944,307.959174691112));
#18945=CARTESIAN_POINT('Ctrl Pts',(-34.7929650411445,3.32518588068037,308.118085983281));
#18946=CARTESIAN_POINT('Ctrl Pts',(-37.1129617348198,0.929276570737269,
308.276997275451));
#18947=CARTESIAN_POINT('Ctrl Pts',(-36.3553444474602,-2.31861230143106,
308.43590856762));
#18948=CARTESIAN_POINT('Ctrl Pts',(-33.2147120371004,-3.4407505028467,308.594819859789));
#18949=CARTESIAN_POINT('Ctrl Pts',(-30.5704598424069,-1.40833902606738,
308.753731151959));
#18950=CARTESIAN_POINT('Ctrl Pts',(-30.8468917769978,1.9152661649284,308.912642444128));
#18951=CARTESIAN_POINT('Ctrl Pts',(-33.7905694501548,3.48291658407265,309.071553736297));
#18952=CARTESIAN_POINT('Ctrl Pts',(-36.7026696112863,1.857358608602,309.230465028467));
#18953=CARTESIAN_POINT('Ctrl Pts',(-36.9133199117442,-1.47106331942605,
309.389376320636));
#18954=CARTESIAN_POINT('Ctrl Pts',(-34.2293918939422,-3.45078463198345,
309.548287612805));
#18955=CARTESIAN_POINT('Ctrl Pts',(-31.1115650689105,-2.26675677371728,
309.707198904975));
#18956=CARTESIAN_POINT('Ctrl Pts',(-30.4183261532173,0.99547955826326,309.866110197144));
#18957=CARTESIAN_POINT('Ctrl Pts',(-32.7852506112629,3.34504008962472,310.025021489313));
#18958=CARTESIAN_POINT('Ctrl Pts',(-36.042294209402,2.62780018600281,310.183932781483));
#18959=CARTESIAN_POINT('Ctrl Pts',(-37.2033334770637,-0.498660096465226,
310.342844073652));
#18960=CARTESIAN_POINT('Ctrl Pts',(-35.2039041212998,-3.16793871372917,
310.501755365821));
#18961=CARTESIAN_POINT('Ctrl Pts',(-31.8771234320867,-2.9327870194305,310.660666657991));
#18962=CARTESIAN_POINT('Ctrl Pts',(-30.2730512525257,-0.00879684934994839,
310.81957795016));
#18963=CARTESIAN_POINT('Ctrl Pts',(-31.8623334207013,2.92325845681437,310.978489242329));
#18964=CARTESIAN_POINT('Ctrl Pts',(-35.1878838707564,3.17521124906162,311.137400534498));
#18965=CARTESIAN_POINT('Ctrl Pts',(-37.2007707017131,0.516066153386569,
311.296311826667));
#18966=CARTESIAN_POINT('Ctrl Pts',(-36.0555384594744,-2.61621889632282,
311.455223118837));
#18967=CARTESIAN_POINT('Ctrl Pts',(-32.8021594059117,-3.34990139408307,
311.614134411006));
#18968=CARTESIAN_POINT('Ctrl Pts',(-30.4233969219013,-1.0123267976642,311.773045703176));
#18969=CARTESIAN_POINT('Ctrl Pts',(-31.1001493488858,2.25337008914078,311.931956995345));
#18970=CARTESIAN_POINT('Ctrl Pts',(-34.2119547447221,3.4531304142085,312.090868287514));
#18971=CARTESIAN_POINT('Ctrl Pts',(-36.9058504038466,1.48699360254793,312.249779579683));
#18972=CARTESIAN_POINT('Ctrl Pts',(-36.7120109820576,-1.84245474240054,
312.408690871853));
#18973=CARTESIAN_POINT('Ctrl Pts',(-33.8081678526913,-3.48269119345687,
312.567602164022));
#18974=CARTESIAN_POINT('Ctrl Pts',(-30.8565903603703,-1.9299515573647,312.726513456192));
#18975=CARTESIAN_POINT('Ctrl Pts',(-30.5634139768938,1.39226111162581,312.885424748361));
#18976=CARTESIAN_POINT('Ctrl Pts',(-33.1972814217439,3.43790528342837,313.04433604053));
#18977=CARTESIAN_POINT('Ctrl Pts',(-36.3437220958687,2.33185256123783,313.2032473327));
#18978=CARTESIAN_POINT('Ctrl Pts',(-37.117354034625,-0.912609245665019,
313.362158624869));
#18979=CARTESIAN_POINT('Ctrl Pts',(-34.8103023649712,-3.31928347455001,
313.521069917038));
#18980=CARTESIAN_POINT('Ctrl Pts',(-31.5347668716017,-2.68516768541914,
313.679981209207));
#18981=CARTESIAN_POINT('Ctrl Pts',(-30.3003021687957,0.415311342082169,
313.838892501377));
#18982=CARTESIAN_POINT('Ctrl Pts',(-31.5842082505384,2.21850747685644,313.944833362823));
#18983=CARTESIAN_POINT('Ctrl Pts',(-32.4655386236531,2.64804502178688,313.997803793546));
#18984=CARTESIAN_POINT('Ctrl Pts',(-32.1589359556362,-2.24226614116358,
303.779827133596));
#18985=CARTESIAN_POINT('Ctrl Pts',(-31.4122420776788,-1.71043520097437,
303.832825034778));
#18986=CARTESIAN_POINT('Ctrl Pts',(-30.5065138065885,0.150282942568503,
303.938793366684));
#18987=CARTESIAN_POINT('Ctrl Pts',(-32.1232661683291,2.81785357286398,304.097732129314));
#18988=CARTESIAN_POINT('Ctrl Pts',(-35.240208767702,2.89661477808911,304.256643421483));
#18989=CARTESIAN_POINT('Ctrl Pts',(-36.9950467852155,0.322217471710304,
304.415554713652));
#18990=CARTESIAN_POINT('Ctrl Pts',(-35.7810918710838,-2.54874681567522,
304.574466005822));
#18991=CARTESIAN_POINT('Ctrl Pts',(-32.7102743720378,-3.08242030157264,
304.733377297991));
#18992=CARTESIAN_POINT('Ctrl Pts',(-30.5984736911756,-0.790326365078698,
304.89228859016));
#18993=CARTESIAN_POINT('Ctrl Pts',(-31.3815990280676,2.22647653523201,305.05119988233));
#18994=CARTESIAN_POINT('Ctrl Pts',(-34.3417748084469,3.20194327146731,305.210111174499));
#18995=CARTESIAN_POINT('Ctrl Pts',(-36.7650002791973,1.24183072580518,305.369022466668));
#18996=CARTESIAN_POINT('Ctrl Pts',(-36.4296376903316,-1.85683013748381,
305.527933758838));
#18997=CARTESIAN_POINT('Ctrl Pts',(-33.6431427417149,-3.25310553102805,
305.686845051007));
#18998=CARTESIAN_POINT('Ctrl Pts',(-30.9602358103902,-1.66687079802693,
305.845756343176));
#18999=CARTESIAN_POINT('Ctrl Pts',(-30.8406576935852,1.44758615073306,306.004667635346));
#19000=CARTESIAN_POINT('Ctrl Pts',(-33.394041236439,3.23486619413217,306.163578927515));
#19001=CARTESIAN_POINT('Ctrl Pts',(-36.2793921739056,2.05635575795594,306.322490219684));
#19002=CARTESIAN_POINT('Ctrl Pts',(-36.851362655713,-1.00746338456369,306.481401511853));
#19003=CARTESIAN_POINT('Ctrl Pts',(-34.5855584445221,-3.1476196454885,306.640312804023));
#19004=CARTESIAN_POINT('Ctrl Pts',(-31.5593147453325,-2.40197456056694,
306.799224096192));
#19005=CARTESIAN_POINT('Ctrl Pts',(-30.5471529837359,0.545849415763471,
306.958135388361));
#19006=CARTESIAN_POINT('Ctrl Pts',(-32.4770435552937,2.99322759649458,307.117046680531));
#19007=CARTESIAN_POINT('Ctrl Pts',(-35.5796237299738,2.69635415766267,307.2759579727));
#19008=CARTESIAN_POINT('Ctrl Pts',(-37.0103852316581,-0.0725913301762454,
307.434869264869));
#19009=CARTESIAN_POINT('Ctrl Pts',(-35.4575769654077,-2.77498361702619,
307.593780557039));
#19010=CARTESIAN_POINT('Ctrl Pts',(-32.3448449685662,-2.9332147775032,307.752691849208));
#19011=CARTESIAN_POINT('Ctrl Pts',(-30.5260049158656,-0.402215281660022,
307.911603141377));
#19012=CARTESIAN_POINT('Ctrl Pts',(-31.668606168612,2.49754332240978,308.070514433546));
#19013=CARTESIAN_POINT('Ctrl Pts',(-34.7250887798085,3.10750367538957,308.229425725716));
#19014=CARTESIAN_POINT('Ctrl Pts',(-36.8932076493054,0.868441784201422,
308.388337017885));
#19015=CARTESIAN_POINT('Ctrl Pts',(-36.1851875296823,-2.16682510603776,
308.547248310054));
#19016=CARTESIAN_POINT('Ctrl Pts',(-33.2501555920862,-3.21550289739198,
308.706159602224));
#19017=CARTESIAN_POINT('Ctrl Pts',(-30.779008501811,-1.31614257269836,308.865070894393));
#19018=CARTESIAN_POINT('Ctrl Pts',(-31.0373439102847,1.78988389233944,309.023982186562));
#19019=CARTESIAN_POINT('Ctrl Pts',(-33.7883146880825,3.25490858991212,309.182893478732));
#19020=CARTESIAN_POINT('Ctrl Pts',(-36.5097751653438,1.73576723523384,309.341804770901));
#19021=CARTESIAN_POINT('Ctrl Pts',(-36.7066353128315,-1.37476064072301,
309.50071606307));
#19022=CARTESIAN_POINT('Ctrl Pts',(-34.1984097642212,-3.22488014554912,
309.65962735524));
#19023=CARTESIAN_POINT('Ctrl Pts',(-31.2846904517741,-2.11836428347257,
309.818538647409));
#19024=CARTESIAN_POINT('Ctrl Pts',(-30.6368341947885,0.930310814818372,
309.977449939578));
#19025=CARTESIAN_POINT('Ctrl Pts',(-32.8488087179213,3.12605813504399,310.136361231748));
#19026=CARTESIAN_POINT('Ctrl Pts',(-35.8926310229921,2.45577210694828,310.295272523917));
#19027=CARTESIAN_POINT('Ctrl Pts',(-36.9776632350234,-0.46601547646978,
310.454183816086));
#19028=CARTESIAN_POINT('Ctrl Pts',(-35.1091258675886,-2.96055064275324,
310.613095108255));
#19029=CARTESIAN_POINT('Ctrl Pts',(-32.000131787285,-2.74079307715281,310.772006400425));
#19030=CARTESIAN_POINT('Ctrl Pts',(-30.5010696679198,-0.00822096648659592,
310.930917692594));
#19031=CARTESIAN_POINT('Ctrl Pts',(-31.9863099991538,2.73188829876952,311.089828984763));
#19032=CARTESIAN_POINT('Ctrl Pts',(-35.0941543775033,2.96734708394057,311.248740276933));
#19033=CARTESIAN_POINT('Ctrl Pts',(-36.9752682309223,0.48228205157203,311.407651569102));
#19034=CARTESIAN_POINT('Ctrl Pts',(-35.9050082425686,-2.44494898260645,
311.566562861271));
#19035=CARTESIAN_POINT('Ctrl Pts',(-32.864610583863,-3.13060119579715,311.725474153441));
#19036=CARTESIAN_POINT('Ctrl Pts',(-30.6415730072601,-0.946055155206282,
311.88438544561));
#19037=CARTESIAN_POINT('Ctrl Pts',(-31.2740220581244,2.10585395382022,312.043296737779));
#19038=CARTESIAN_POINT('Ctrl Pts',(-34.1821141322673,3.22707236190863,312.202208029949));
#19039=CARTESIAN_POINT('Ctrl Pts',(-36.6996547938234,1.38964805307454,312.361119322118));
#19040=CARTESIAN_POINT('Ctrl Pts',(-36.518505006335,-1.72183904575499,312.520030614287));
#19041=CARTESIAN_POINT('Ctrl Pts',(-33.8047610169571,-3.25469795441922,
312.678941906457));
#19042=CARTESIAN_POINT('Ctrl Pts',(-31.0464075790711,-1.80360791036664,
312.837853198626));
#19043=CARTESIAN_POINT('Ctrl Pts',(-30.7724238915776,1.30111719366316,312.996764490795));
#19044=CARTESIAN_POINT('Ctrl Pts',(-33.2338660662586,3.21284393933158,313.155675782965));
#19045=CARTESIAN_POINT('Ctrl Pts',(-36.1743260315335,2.17919859657001,313.314587075134));
#19046=CARTESIAN_POINT('Ctrl Pts',(-36.8973124086415,-0.852865580109559,
313.473498367303));
#19047=CARTESIAN_POINT('Ctrl Pts',(-34.7412911214056,-3.10198766834458,
313.632409659472));
#19048=CARTESIAN_POINT('Ctrl Pts',(-31.6801874869731,-2.50938406179264,
313.791320951642));
#19049=CARTESIAN_POINT('Ctrl Pts',(-30.5265366118757,0.388123121010992,
313.950232243811));
#19050=CARTESIAN_POINT('Ctrl Pts',(-31.7263922022207,2.07327361103796,314.056173105257));
#19051=CARTESIAN_POINT('Ctrl Pts',(-32.5500265709333,2.47469162118422,314.10914353598));
#19052=CARTESIAN_POINT('Ctrl Pts',(-32.2708199984643,-2.08519426307603,
303.891166876031));
#19053=CARTESIAN_POINT('Ctrl Pts',(-31.576432404589,-1.59061834942761,303.944164777214));
#19054=CARTESIAN_POINT('Ctrl Pts',(-30.7341508573133,0.139755546377488,
304.050133109119));
#19055=CARTESIAN_POINT('Ctrl Pts',(-32.2376488978119,2.6204615038584,304.209071871748));
#19056=CARTESIAN_POINT('Ctrl Pts',(-35.1362480904917,2.69370544679336,304.367983163918));
#19057=CARTESIAN_POINT('Ctrl Pts',(-36.7681588166858,0.299645974730056,
304.526894456087));
#19058=CARTESIAN_POINT('Ctrl Pts',(-35.6392420587194,-2.37020581121622,
304.685805748256));
#19059=CARTESIAN_POINT('Ctrl Pts',(-32.783536879743,-2.8664951993134,304.844717040425));
#19060=CARTESIAN_POINT('Ctrl Pts',(-30.8196689054406,-0.734963603189685,
305.003628332595));
#19061=CARTESIAN_POINT('Ctrl Pts',(-31.5479359161127,2.07051072703172,305.162539624764));
#19062=CARTESIAN_POINT('Ctrl Pts',(-34.3007498848151,2.97764552467167,305.321450916933));
#19063=CARTESIAN_POINT('Ctrl Pts',(-36.5542271848499,1.15483985492318,305.480362209103));
#19064=CARTESIAN_POINT('Ctrl Pts',(-36.2423569150743,-1.72675824653835,
305.639273501272));
#19065=CARTESIAN_POINT('Ctrl Pts',(-33.6510573479628,-3.02522384205495,
305.798184793441));
#19066=CARTESIAN_POINT('Ctrl Pts',(-31.1560894051021,-1.5501056549563,305.957096085611));
#19067=CARTESIAN_POINT('Ctrl Pts',(-31.0448877959025,1.34618200819396,306.11600737778));
#19068=CARTESIAN_POINT('Ctrl Pts',(-33.4194055292116,3.00826217994027,306.274918669949));
#19069=CARTESIAN_POINT('Ctrl Pts',(-36.1026361731191,1.91230699630863,306.433829962119));
#19070=CARTESIAN_POINT('Ctrl Pts',(-36.6345398331792,-0.936890064558189,
306.592741254288));
#19071=CARTESIAN_POINT('Ctrl Pts',(-34.5274563537948,-2.92712729618799,
306.751652546457));
#19072=CARTESIAN_POINT('Ctrl Pts',(-31.7132025574343,-2.23371502686548,
306.910563838626));
#19073=CARTESIAN_POINT('Ctrl Pts',(-30.7719432395324,0.507612387913404,
307.069475130796));
#19074=CARTESIAN_POINT('Ctrl Pts',(-32.5666439997592,2.78355048836999,307.228386422965));
#19075=CARTESIAN_POINT('Ctrl Pts',(-35.4518868628651,2.50747318418757,307.387297715134));
#19076=CARTESIAN_POINT('Ctrl Pts',(-36.7824227971917,-0.0675062707560861,
307.546209007304));
#19077=CARTESIAN_POINT('Ctrl Pts',(-35.3383895359296,-2.58059461012522,
307.705120299473));
#19078=CARTESIAN_POINT('Ctrl Pts',(-32.4437059909427,-2.72774159772379,
307.864031591642));
#19079=CARTESIAN_POINT('Ctrl Pts',(-30.7522766045202,-0.374039897602761,
308.022942883812));
#19080=CARTESIAN_POINT('Ctrl Pts',(-31.8148380611964,2.32258914857013,308.181854175981));
#19081=CARTESIAN_POINT('Ctrl Pts',(-34.6572125184726,2.88982147009876,308.34076546815));
#19082=CARTESIAN_POINT('Ctrl Pts',(-36.6734535637911,0.807606997665576,
308.49967676032));
#19083=CARTESIAN_POINT('Ctrl Pts',(-36.0150306119043,-2.01503791064446,
308.658588052489));
#19084=CARTESIAN_POINT('Ctrl Pts',(-33.2855991470718,-2.99025529193725,
308.817499344658));
#19085=CARTESIAN_POINT('Ctrl Pts',(-30.9875571612151,-1.22394611932934,
308.976410636827));
#19086=CARTESIAN_POINT('Ctrl Pts',(-31.2277960435716,1.66450161975047,309.135321928997));
#19087=CARTESIAN_POINT('Ctrl Pts',(-33.7860599260102,3.02690059575158,309.294233221166));
#19088=CARTESIAN_POINT('Ctrl Pts',(-36.3168807194012,1.61417586186566,309.453144513335));
#19089=CARTESIAN_POINT('Ctrl Pts',(-36.4999507139187,-1.27845796201997,
309.612055805505));
#19090=CARTESIAN_POINT('Ctrl Pts',(-34.1674276345002,-2.9989756591148,309.770967097674));
#19091=CARTESIAN_POINT('Ctrl Pts',(-31.4578158346379,-1.96997179322788,
309.929878389844));
#19092=CARTESIAN_POINT('Ctrl Pts',(-30.8553422363595,0.86514207137348,310.088789682013));
#19093=CARTESIAN_POINT('Ctrl Pts',(-32.9123668245796,2.90707618046325,310.247700974182));
#19094=CARTESIAN_POINT('Ctrl Pts',(-35.7429678365821,2.28374402789374,310.406612266351));
#19095=CARTESIAN_POINT('Ctrl Pts',(-36.7519929929832,-0.43337085647433,
310.565523558521));
#19096=CARTESIAN_POINT('Ctrl Pts',(-35.0143476138774,-2.75316257177733,
310.72443485069));
#19097=CARTESIAN_POINT('Ctrl Pts',(-32.1231401424832,-2.54879913487514,
310.883346142859));
#19098=CARTESIAN_POINT('Ctrl Pts',(-30.7290880833138,-0.00764508362324373,
311.042257435029));
#19099=CARTESIAN_POINT('Ctrl Pts',(-32.1102865776064,2.54051814072466,311.201168727198));
#19100=CARTESIAN_POINT('Ctrl Pts',(-35.0004248842504,2.75948291881953,311.360080019367));
#19101=CARTESIAN_POINT('Ctrl Pts',(-36.7497657601316,0.448497949757495,
311.518991311536));
#19102=CARTESIAN_POINT('Ctrl Pts',(-35.7544780256626,-2.27367906889009,
311.677902603706));
#19103=CARTESIAN_POINT('Ctrl Pts',(-32.9270617618141,-2.91130099751123,
311.836813895875));
#19104=CARTESIAN_POINT('Ctrl Pts',(-30.8597490926191,-0.879783512748368,
311.995725188045));
#19105=CARTESIAN_POINT('Ctrl Pts',(-31.447894767363,1.95833781849965,312.154636480214));
#19106=CARTESIAN_POINT('Ctrl Pts',(-34.1522735198124,3.00101430960874,312.313547772383));
#19107=CARTESIAN_POINT('Ctrl Pts',(-36.4934591838003,1.29230250360115,312.472459064552));
#19108=CARTESIAN_POINT('Ctrl Pts',(-36.3249990306125,-1.60122334910943,
312.631370356722));
#19109=CARTESIAN_POINT('Ctrl Pts',(-33.801354181223,-3.02670471538159,312.790281648891));
#19110=CARTESIAN_POINT('Ctrl Pts',(-31.2362247977721,-1.67726426336858,
312.949192941061));
#19111=CARTESIAN_POINT('Ctrl Pts',(-30.9814338062613,1.2099732757005,313.10810423323));
#19112=CARTESIAN_POINT('Ctrl Pts',(-33.2704507107733,2.98778259523479,313.267015525399));
#19113=CARTESIAN_POINT('Ctrl Pts',(-36.0049299671983,2.0265446319022,313.425926817568));
#19114=CARTESIAN_POINT('Ctrl Pts',(-36.6772707826581,-0.7931219145541,313.584838109738));
#19115=CARTESIAN_POINT('Ctrl Pts',(-34.6722798778402,-2.88469186213915,
313.743749401907));
#19116=CARTESIAN_POINT('Ctrl Pts',(-31.8256081023445,-2.33360043816614,
313.902660694076));
#19117=CARTESIAN_POINT('Ctrl Pts',(-30.7527710549558,0.360934899939814,
314.061571986246));
#19118=CARTESIAN_POINT('Ctrl Pts',(-31.868576153903,1.92803974521949,314.167512847692));
#19119=CARTESIAN_POINT('Ctrl Pts',(-32.6345145182136,2.30133822058156,314.220483278415));
#19120=CARTESIAN_POINT('Ctrl Pts',(-32.3827040412925,-1.92812238498848,
304.002506618465));
#19121=CARTESIAN_POINT('Ctrl Pts',(-31.7406227314992,-1.47080149788086,
304.055504519648));
#19122=CARTESIAN_POINT('Ctrl Pts',(-30.961787908038,0.129228150186471,304.161472851553));
#19123=CARTESIAN_POINT('Ctrl Pts',(-32.3520316272949,2.42306943485282,304.320411614183));
#19124=CARTESIAN_POINT('Ctrl Pts',(-35.0322874132814,2.49079611549761,304.479322906352));
#19125=CARTESIAN_POINT('Ctrl Pts',(-36.5412708481562,0.277074477749808,
304.638234198521));
#19126=CARTESIAN_POINT('Ctrl Pts',(-35.4973922463549,-2.19166480675722,
304.797145490691));
#19127=CARTESIAN_POINT('Ctrl Pts',(-32.8567993874481,-2.65057009705414,
304.95605678286));
#19128=CARTESIAN_POINT('Ctrl Pts',(-31.0408641197054,-0.679600841300668,
305.114968075029));
#19129=CARTESIAN_POINT('Ctrl Pts',(-31.7142728041579,1.91454491883143,305.273879367199));
#19130=CARTESIAN_POINT('Ctrl Pts',(-34.2597249611834,2.75334777787602,305.432790659368));
#19131=CARTESIAN_POINT('Ctrl Pts',(-36.3434540905024,1.06784898404117,305.591701951537));
#19132=CARTESIAN_POINT('Ctrl Pts',(-36.055076139817,-1.59668635559289,305.750613243707));
#19133=CARTESIAN_POINT('Ctrl Pts',(-33.6589719542107,-2.79734215308184,
305.909524535876));
#19134=CARTESIAN_POINT('Ctrl Pts',(-31.351942999814,-1.43334051188567,306.068435828045));
#19135=CARTESIAN_POINT('Ctrl Pts',(-31.2491178982198,1.24477786565487,306.227347120214));
#19136=CARTESIAN_POINT('Ctrl Pts',(-33.4447698219842,2.78165816574837,306.386258412384));
#19137=CARTESIAN_POINT('Ctrl Pts',(-35.9258801723326,1.76825823466132,306.545169704553));
#19138=CARTESIAN_POINT('Ctrl Pts',(-36.4177170106453,-0.866316744552692,
306.704080996722));
#19139=CARTESIAN_POINT('Ctrl Pts',(-34.4693542630674,-2.7066349468875,306.862992288892));
#19140=CARTESIAN_POINT('Ctrl Pts',(-31.8670903695361,-2.065455493164,307.021903581061));
#19141=CARTESIAN_POINT('Ctrl Pts',(-30.996733495329,0.469375360063339,307.18081487323));
#19142=CARTESIAN_POINT('Ctrl Pts',(-32.6562444442246,2.57387338024539,307.3397261654));
#19143=CARTESIAN_POINT('Ctrl Pts',(-35.3241499957564,2.31859221071245,307.498637457569));
#19144=CARTESIAN_POINT('Ctrl Pts',(-36.5544603627254,-0.0624212113359256,
307.657548749738));
#19145=CARTESIAN_POINT('Ctrl Pts',(-35.2192021064513,-2.38620560322425,
307.816460041908));
#19146=CARTESIAN_POINT('Ctrl Pts',(-32.5425670133193,-2.52226841794439,
307.975371334077));
#19147=CARTESIAN_POINT('Ctrl Pts',(-30.9785482931749,-0.345864513545499,
308.134282626246));
#19148=CARTESIAN_POINT('Ctrl Pts',(-31.9610699537809,2.14763497473048,308.293193918415));
#19149=CARTESIAN_POINT('Ctrl Pts',(-34.5893362571368,2.67213926480795,308.452105210585));
#19150=CARTESIAN_POINT('Ctrl Pts',(-36.4536994782767,0.746772211129729,
308.611016502754));
#19151=CARTESIAN_POINT('Ctrl Pts',(-35.8448736941263,-1.86325071525115,
308.769927794923));
#19152=CARTESIAN_POINT('Ctrl Pts',(-33.3210427020575,-2.76500768648252,
308.928839087093));
#19153=CARTESIAN_POINT('Ctrl Pts',(-31.1961058206193,-1.13174966596031,
309.087750379262));
#19154=CARTESIAN_POINT('Ctrl Pts',(-31.4182481768584,1.53911934716151,309.246661671431));
#19155=CARTESIAN_POINT('Ctrl Pts',(-33.7838051639379,2.79889260159105,309.405572963601));
#19156=CARTESIAN_POINT('Ctrl Pts',(-36.1239862734585,1.49258448849749,309.56448425577));
#19157=CARTESIAN_POINT('Ctrl Pts',(-36.293266115006,-1.18215528331693,309.723395547939));
#19158=CARTESIAN_POINT('Ctrl Pts',(-34.136445504779,-2.77307117268048,309.882306840109));
#19159=CARTESIAN_POINT('Ctrl Pts',(-31.6309412175016,-1.82157930298317,
310.041218132278));
#19160=CARTESIAN_POINT('Ctrl Pts',(-31.0738502779306,0.799973327928591,
310.200129424447));
#19161=CARTESIAN_POINT('Ctrl Pts',(-32.975924931238,2.68809422588251,310.359040716617));
#19162=CARTESIAN_POINT('Ctrl Pts',(-35.5933046501722,2.11171594883921,310.517952008786));
#19163=CARTESIAN_POINT('Ctrl Pts',(-36.526322750943,-0.400726236478883,
310.676863300955));
#19164=CARTESIAN_POINT('Ctrl Pts',(-34.9195693601661,-2.54577450080141,
310.835774593124));
#19165=CARTESIAN_POINT('Ctrl Pts',(-32.2461484976814,-2.35680519259746,
310.994685885294));
#19166=CARTESIAN_POINT('Ctrl Pts',(-30.9571064987078,-0.00706920075989126,
311.153597177463));
#19167=CARTESIAN_POINT('Ctrl Pts',(-32.2342631560589,2.3491479826798,311.312508469633));
#19168=CARTESIAN_POINT('Ctrl Pts',(-34.9066953909973,2.55161875369849,311.471419761802));
#19169=CARTESIAN_POINT('Ctrl Pts',(-36.5242632893408,0.414713847942957,
311.630331053971));
#19170=CARTESIAN_POINT('Ctrl Pts',(-35.6039478087568,-2.10240915517373,
311.78924234614));
#19171=CARTESIAN_POINT('Ctrl Pts',(-32.9895129397654,-2.69200079922531,
311.94815363831));
#19172=CARTESIAN_POINT('Ctrl Pts',(-31.077925177978,-0.813511870290452,
312.107064930479));
#19173=CARTESIAN_POINT('Ctrl Pts',(-31.6217674766015,1.81082168317909,312.265976222648));
#19174=CARTESIAN_POINT('Ctrl Pts',(-34.1224329073576,2.77495625730887,312.424887514818));
#19175=CARTESIAN_POINT('Ctrl Pts',(-36.2872635737771,1.19495695412777,312.583798806987));
#19176=CARTESIAN_POINT('Ctrl Pts',(-36.1314930548899,-1.48060765246388,
312.742710099156));
#19177=CARTESIAN_POINT('Ctrl Pts',(-33.7979473454889,-2.79871147634394,
312.901621391325));
#19178=CARTESIAN_POINT('Ctrl Pts',(-31.426042016473,-1.55092061637053,313.060532683495));
#19179=CARTESIAN_POINT('Ctrl Pts',(-31.1904437209451,1.11882935773785,313.219443975664));
#19180=CARTESIAN_POINT('Ctrl Pts',(-33.307035355288,2.762721251138,313.378355267833));
#19181=CARTESIAN_POINT('Ctrl Pts',(-35.8355339028631,1.8738906672344,313.537266560003));
#19182=CARTESIAN_POINT('Ctrl Pts',(-36.4572291566747,-0.733378248998641,
313.696177852172));
#19183=CARTESIAN_POINT('Ctrl Pts',(-34.6032686342748,-2.66739605593371,
313.855089144342));
#19184=CARTESIAN_POINT('Ctrl Pts',(-31.9710287177159,-2.15781681453964,
314.014000436511));
#19185=CARTESIAN_POINT('Ctrl Pts',(-30.9790054980359,0.333746678868638,
314.17291172868));
#19186=CARTESIAN_POINT('Ctrl Pts',(-32.0107601055854,1.782805879401,314.278852590126));
#19187=CARTESIAN_POINT('Ctrl Pts',(-32.7190024654939,2.1279848199789,314.331823020849));
#19188=CARTESIAN_POINT('',(-32.377264335587,-1.93219025172127,314.001151947217));
#19189=CARTESIAN_POINT('Ctrl Pts',(-32.3759974984059,-1.93375951905296,
314.));
#19190=CARTESIAN_POINT('Ctrl Pts',(-32.3257540111668,-1.90643624108857,
314.));
#19191=CARTESIAN_POINT('Ctrl Pts',(-32.2766866929433,-1.87724182519096,
314.));
#19192=CARTESIAN_POINT('Ctrl Pts',(-32.2289125290216,-1.84620625429721,
314.));
#19193=CARTESIAN_POINT('Ctrl Pts',(-32.1608191978532,-1.80197072543822,
314.));
#19194=CARTESIAN_POINT('Ctrl Pts',(-32.0953516584285,-1.75399746288308,
314.));
#19195=CARTESIAN_POINT('Ctrl Pts',(-32.0325845285674,-1.70265816671701,
314.));
#19196=CARTESIAN_POINT('Ctrl Pts',(-31.9677545339494,-1.6496315857421,314.));
#19197=CARTESIAN_POINT('Ctrl Pts',(-31.9058047707206,-1.59301373041818,
314.));
#19198=CARTESIAN_POINT('Ctrl Pts',(-31.8468374374935,-1.53316100944906,
314.));
#19199=CARTESIAN_POINT('Ctrl Pts',(-31.7880103872424,-1.47345067778871,
314.));
#19200=CARTESIAN_POINT('Ctrl Pts',(-31.7321510803983,-1.41052015262424,
314.));
#19201=CARTESIAN_POINT('Ctrl Pts',(-31.6793887798477,-1.34467971117326,
314.));
#19202=CARTESIAN_POINT('Ctrl Pts',(-31.6703793986152,-1.33343718324413,
314.));
#19203=CARTESIAN_POINT('Ctrl Pts',(-31.6614597242036,-1.32210872662661,
314.));
#19204=CARTESIAN_POINT('Ctrl Pts',(-31.6526411425254,-1.31070993397642,
314.));
#19205=CARTESIAN_POINT('Ctrl Pts',(-31.5997451171298,-1.24233716752603,
314.));
#19206=CARTESIAN_POINT('Ctrl Pts',(-31.5503933030584,-1.17132577496273,
314.));
#19207=CARTESIAN_POINT('Ctrl Pts',(-31.5046726718675,-1.09807055930981,
314.));
#19208=CARTESIAN_POINT('Ctrl Pts',(-31.4576849282052,-1.02278513114822,
314.));
#19209=CARTESIAN_POINT('Ctrl Pts',(-31.4145317574665,-0.945129216982495,
314.));
#19210=CARTESIAN_POINT('Ctrl Pts',(-31.3753363205634,-0.865483493531305,
314.));
#19211=CARTESIAN_POINT('Ctrl Pts',(-31.3361408836603,-0.785837770080116,
314.));
#19212=CARTESIAN_POINT('Ctrl Pts',(-31.3009026029221,-0.70420140232959,
314.));
#19213=CARTESIAN_POINT('Ctrl Pts',(-31.2697822646969,-0.620918813716327,
314.));
#19214=CARTESIAN_POINT('Ctrl Pts',(-31.2557264444749,-0.58330337764046,
314.));
#19215=CARTESIAN_POINT('Ctrl Pts',(-31.2425112341339,-0.545351703294952,
314.));
#19216=CARTESIAN_POINT('Ctrl Pts',(-31.2301544561367,-0.507093809149475,
314.));
#19217=CARTESIAN_POINT('Ctrl Pts',(-31.2260302587649,-0.494324857038999,
314.));
#19218=CARTESIAN_POINT('Ctrl Pts',(-31.2220017037552,-0.481521786356571,
314.));
#19219=CARTESIAN_POINT('Ctrl Pts',(-31.2180695050756,-0.468685693754918,
314.));
#19220=CARTESIAN_POINT('Ctrl Pts',(-31.2137669293524,-0.454640558981847,
314.));
#19221=CARTESIAN_POINT('Ctrl Pts',(-31.2095824026482,-0.44056456576873,
314.));
#19222=CARTESIAN_POINT('Ctrl Pts',(-31.2055177373976,-0.426463984545297,
314.));
#19223=CARTESIAN_POINT('Ctrl Pts',(-31.1801162677167,-0.338344677210859,
314.));
#19224=CARTESIAN_POINT('Ctrl Pts',(-31.159375381469,-0.249211163206453,
314.));
#19225=CARTESIAN_POINT('Ctrl Pts',(-31.1434172941268,-0.15946046529224,
314.));
#19226=CARTESIAN_POINT('Ctrl Pts',(-31.1275109139743,-0.0700005764364917,
314.));
#19227=CARTESIAN_POINT('Ctrl Pts',(-31.1163558477828,0.0200734083628238,
314.));
#19228=CARTESIAN_POINT('Ctrl Pts',(-31.1101146925889,0.110397933079268,
314.));
#19229=CARTESIAN_POINT('Ctrl Pts',(-31.1053794907591,0.178927691020232,
314.));
#19230=CARTESIAN_POINT('Ctrl Pts',(-31.103473686878,0.247602370572859,314.));
#19231=CARTESIAN_POINT('Ctrl Pts',(-31.1044872693873,0.316269774268565,
314.));
#19232=CARTESIAN_POINT('Ctrl Pts',(-31.1053453208484,0.374400380835571,
314.));
#19233=CARTESIAN_POINT('Ctrl Pts',(-31.1082958244446,0.432525934107557,
314.));
#19234=CARTESIAN_POINT('Ctrl Pts',(-31.1132828595529,0.490573353944516,
314.));
#19235=CARTESIAN_POINT('Ctrl Pts',(-31.1146016599839,0.505923749647501,
314.));
#19236=CARTESIAN_POINT('Ctrl Pts',(-31.1160629300108,0.521268682535076,
314.));
#19237=CARTESIAN_POINT('Ctrl Pts',(-31.1176657459376,0.536606800278575,
314.));
#19238=CARTESIAN_POINT('Ctrl Pts',(-31.1191964866191,0.551255195277842,
314.));
#19239=CARTESIAN_POINT('Ctrl Pts',(-31.1208555083163,0.565889202852191,
314.));
#19240=CARTESIAN_POINT('Ctrl Pts',(-31.122640833076,0.580502070227278,314.));
#19241=CARTESIAN_POINT('Ctrl Pts',(-31.1337692874301,0.671588370738572,
314.));
#19242=CARTESIAN_POINT('Ctrl Pts',(-31.1498074944257,0.761920145199774,
314.));
#19243=CARTESIAN_POINT('Ctrl Pts',(-31.1704487043523,0.851206941552089,
314.));
#19244=CARTESIAN_POINT('Ctrl Pts',(-31.191089914279,0.940493737904405,314.));
#19245=CARTESIAN_POINT('Ctrl Pts',(-31.2163344303304,1.02873630292022,314.));
#19246=CARTESIAN_POINT('Ctrl Pts',(-31.2459304858038,1.11565311734405,314.));
#19247=CARTESIAN_POINT('Ctrl Pts',(-31.272566814453,1.19387789416348,314.));
#19248=CARTESIAN_POINT('Ctrl Pts',(-31.302728718844,1.27102932581834,314.));
#19249=CARTESIAN_POINT('Ctrl Pts',(-31.3362676725216,1.34690078032736,314.));
#19250=CARTESIAN_POINT('Ctrl Pts',(-31.3538038375232,1.38657090116585,314.));
#19251=CARTESIAN_POINT('Ctrl Pts',(-31.3722637586092,1.42589103210099,314.));
#19252=CARTESIAN_POINT('Ctrl Pts',(-31.3916295511445,1.4648308304436,314.));
#19253=CARTESIAN_POINT('Ctrl Pts',(-31.4012682821441,1.48421192423163,314.));
#19254=CARTESIAN_POINT('Ctrl Pts',(-31.4111314543575,1.5034987888243,314.));
#19255=CARTESIAN_POINT('Ctrl Pts',(-31.4212170636299,1.52268760355645,314.));
#19256=CARTESIAN_POINT('Ctrl Pts',(-31.4302092303145,1.53979604151892,314.));
#19257=CARTESIAN_POINT('Ctrl Pts',(-31.4393797915133,1.55682916770076,314.));
#19258=CARTESIAN_POINT('Ctrl Pts',(-31.4487149028359,1.57376220373142,314.));
#19259=CARTESIAN_POINT('Ctrl Pts',(-31.4962690987775,1.6600211550678,314.));
#19260=CARTESIAN_POINT('Ctrl Pts',(-31.5481486823058,1.74380084509073,314.));
#19261=CARTESIAN_POINT('Ctrl Pts',(-31.604078655239,1.82477165044164,314.));
#19262=CARTESIAN_POINT('Ctrl Pts',(-31.6600086281722,1.90574245579256,314.));
#19263=CARTESIAN_POINT('Ctrl Pts',(-31.7199894123827,1.98390533447625,314.));
#19264=CARTESIAN_POINT('Ctrl Pts',(-31.7837997715045,2.05891647649168,314.));
#19265=CARTESIAN_POINT('Ctrl Pts',(-31.8048007147617,2.08360376486943,314.));
#19266=CARTESIAN_POINT('Ctrl Pts',(-31.8262168701635,2.10794949134823,314.));
#19267=CARTESIAN_POINT('Ctrl Pts',(-31.8480415044456,2.13194078872289,314.));
#19268=CARTESIAN_POINT('Ctrl Pts',(-31.86386898592,2.14933955975562,314.));
#19269=CARTESIAN_POINT('Ctrl Pts',(-31.879914532835,2.16655510974176,314.));
#19270=CARTESIAN_POINT('Ctrl Pts',(-31.8961553562769,2.18356159119131,314.));
#19271=CARTESIAN_POINT('Ctrl Pts',(-31.9644789868494,2.25510627364289,314.));
#19272=CARTESIAN_POINT('Ctrl Pts',(-32.0363142842366,2.32302056909005,314.));
#19273=CARTESIAN_POINT('Ctrl Pts',(-32.1114230096085,2.38697563761891,314.));
#19274=CARTESIAN_POINT('Ctrl Pts',(-32.1857753014975,2.45028660314906,314.));
#19275=CARTESIAN_POINT('Ctrl Pts',(-32.2633359044913,2.50971853132512,314.));
#19276=CARTESIAN_POINT('Ctrl Pts',(-32.3439167635066,2.56492639140002,314.));
#19277=CARTESIAN_POINT('Ctrl Pts',(-32.3842618400881,2.59256776144546,314.));
#19278=CARTESIAN_POINT('Ctrl Pts',(-32.4253646625726,2.6191497604752,314.));
#19279=CARTESIAN_POINT('Ctrl Pts',(-32.4672051712042,2.64462557919707,314.));
#19280=CARTESIAN_POINT('Ctrl Pts',(-32.4049121771464,-1.94920919778867,
314.));
#19281=CARTESIAN_POINT('Ctrl Pts',(-32.3960384479541,-1.94305782385895,
314.000383982406));
#19282=CARTESIAN_POINT('Ctrl Pts',(-32.3872067253983,-1.93684585282465,
314.000767964811));
#19283=CARTESIAN_POINT('Ctrl Pts',(-32.3784178331262,-1.93057386401469,
314.001151947217));
#19284=CARTESIAN_POINT('Origin',(-33.7561270252576,0.,294.));
#19285=CARTESIAN_POINT('',(-37.7561270252576,4.89858719658941E-16,294.));
#19286=CARTESIAN_POINT('Origin',(-33.7561270252576,0.,294.));
#19287=CARTESIAN_POINT('Origin',(-33.7561270252576,0.,294.));
#19288=CARTESIAN_POINT('',(-37.7561270252576,4.89858719658941E-16,274.));
#19289=CARTESIAN_POINT('Origin',(-33.7561270252576,0.,274.));
#19290=CARTESIAN_POINT('',(-37.7561270252576,4.89858719658941E-16,294.));
#19291=CARTESIAN_POINT('Origin',(-33.7561270252576,0.,274.));
#19292=CARTESIAN_POINT('Origin',(-33.7561270252576,0.,314.));
#19429=UNCERTAINTY_MEASURE_WITH_UNIT(LENGTH_MEASURE(0.01),#19444,
'DISTANCE_ACCURACY_VALUE',
'Maximum model space distance between geometric entities at asserted c
onnectivities');
#19433=UNCERTAINTY_MEASURE_WITH_UNIT(LENGTH_MEASURE(0.01),#19444,
'DISTANCE_ACCURACY_VALUE',
'Maximum model space distance between geometric entities at asserted c
onnectivities');
#19439=(
GEOMETRIC_REPRESENTATION_CONTEXT(3)
GLOBAL_UNCERTAINTY_ASSIGNED_CONTEXT((#19429))
GLOBAL_UNIT_ASSIGNED_CONTEXT((#19444,#19446,#19447))
REPRESENTATION_CONTEXT('','3D')
);
#19443=(
GEOMETRIC_REPRESENTATION_CONTEXT(3)
GLOBAL_UNCERTAINTY_ASSIGNED_CONTEXT((#19433))
GLOBAL_UNIT_ASSIGNED_CONTEXT((#19444,#19446,#19447))
REPRESENTATION_CONTEXT('','3D')
);
#19444=(
LENGTH_UNIT()
NAMED_UNIT(*)
SI_UNIT(.MILLI.,.METRE.)
);
#19446=(
NAMED_UNIT(*)
PLANE_ANGLE_UNIT()
SI_UNIT($,.RADIAN.)
);
#19447=(
NAMED_UNIT(*)
SI_UNIT($,.STERADIAN.)
SOLID_ANGLE_UNIT()
);
#19453=SHAPE_DEFINITION_REPRESENTATION(#19462,#19479);
#19462=PRODUCT_DEFINITION_SHAPE('',$,#19489);
#19479=SHAPE_REPRESENTATION('',(#2195),#19439);
#19483=PRODUCT_DEFINITION_CONTEXT('part definition',#19512,'design');
#19489=PRODUCT_DEFINITION('Screw','Screw',#19498,#19483);
#19498=PRODUCT_DEFINITION_FORMATION('',$,#19519);
#19512=APPLICATION_CONTEXT(
'Core Data for Automotive Mechanical Design Process');
#19513=PRODUCT_CONTEXT('part definition',#19512,'mechanical');
#19519=PRODUCT('Screw','Screw',$,(#19513));
#19525=PRESENTATION_STYLE_ASSIGNMENT((#19528));
#19528=SURFACE_STYLE_USAGE(.BOTH.,#19531);
#19531=SURFACE_SIDE_STYLE('',(#19534));
#19534=SURFACE_STYLE_FILL_AREA(#19537);
#19537=FILL_AREA_STYLE('Opaque(160,160,160)',(#19540));
#19540=FILL_AREA_STYLE_COLOUR('Opaque(160,160,160)',#19543);
#19543=COLOUR_RGB('Opaque(160,160,160)',0.627450980392157,0.627450980392157,
0.627450980392157);
ENDSEC;
END-ISO-10303-21;
